ISO-10303-21;
HEADER;
/* Generated by software containing ST-Developer
 * from STEP Tools, Inc. (www.steptools.com) 
 */

FILE_DESCRIPTION(
/* description */ ('STEP AP214'),
/* implementation_level */ '2;1');

FILE_NAME(
/* name */ 'Coupling Nut.step',
/* time_stamp */ '2026-10-05T23:18:41-07:00',
/* author */ (''),
/* organization */ (''),
/* preprocessor_version */ 'ST-DEVELOPER v20.2',
/* originating_system */ 'Autodesk Translation Framework v15.15.0.0',
/* authorisation */ '');

FILE_SCHEMA (('AUTOMOTIVE_DESIGN { 1 0 10303 214 3 1 1 }'));
ENDSEC;

DATA;
#10=MECHANICAL_DESIGN_GEOMETRIC_PRESENTATION_REPRESENTATION('',(#104),#221662);
#66=MANIFOLD_SOLID_BREP('Body1',#79326);
#78=SHAPE_REPRESENTATION_RELATIONSHIP('SRR','None',#221713,#91);
#91=ADVANCED_BREP_SHAPE_REPRESENTATION('',(#66),#221653);
#104=STYLED_ITEM('',(#221783),#66);
#183=B_SPLINE_SURFACE_WITH_KNOTS('',3,3,((#176366,#176367,#176368,#176369,
#176370,#176371,#176372,#176373,#176374,#176375,#176376,#176377,#176378,
#176379,#176380,#176381,#176382,#176383,#176384,#176385,#176386,#176387,
#176388,#176389,#176390,#176391,#176392,#176393,#176394,#176395,#176396,
#176397,#176398,#176399,#176400),(#176401,#176402,#176403,#176404,#176405,
#176406,#176407,#176408,#176409,#176410,#176411,#176412,#176413,#176414,
#176415,#176416,#176417,#176418,#176419,#176420,#176421,#176422,#176423,
#176424,#176425,#176426,#176427,#176428,#176429,#176430,#176431,#176432,
#176433,#176434,#176435),(#176436,#176437,#176438,#176439,#176440,#176441,
#176442,#176443,#176444,#176445,#176446,#176447,#176448,#176449,#176450,
#176451,#176452,#176453,#176454,#176455,#176456,#176457,#176458,#176459,
#176460,#176461,#176462,#176463,#176464,#176465,#176466,#176467,#176468,
#176469,#176470),(#176471,#176472,#176473,#176474,#176475,#176476,#176477,
#176478,#176479,#176480,#176481,#176482,#176483,#176484,#176485,#176486,
#176487,#176488,#176489,#176490,#176491,#176492,#176493,#176494,#176495,
#176496,#176497,#176498,#176499,#176500,#176501,#176502,#176503,#176504,
#176505)),.UNSPECIFIED.,.F.,.F.,.F.,(4,4),(4,1,1,1,1,1,1,1,1,1,1,1,1,1,
1,1,1,1,1,1,1,1,1,1,1,1,1,1,1,1,1,1,4),(0.,1.),(0.,0.031249999999992,0.062499999999984,
0.0937500000001036,0.125000000000096,0.156250000000088,0.187500000000079,
0.218750000000072,0.250000000000191,0.281250000000183,0.312500000000176,
0.343750000000167,0.375000000000159,0.406250000000151,0.437500000000271,
0.468750000000263,0.500000000000255,0.531250000000247,0.562500000000239,
0.593750000000231,0.62500000000035,0.656250000000342,0.687500000000335,
0.718750000000326,0.750000000000319,0.781250000000438,0.81250000000043,
0.843750000000422,0.875000000000414,0.906250000000406,0.937500000000398,
0.968750000000518,1.),.UNSPECIFIED.);
#184=B_SPLINE_SURFACE_WITH_KNOTS('',3,3,((#176773,#176774,#176775,#176776,
#176777,#176778,#176779,#176780,#176781,#176782,#176783,#176784,#176785,
#176786,#176787,#176788,#176789,#176790,#176791,#176792,#176793,#176794,
#176795,#176796,#176797,#176798,#176799,#176800,#176801,#176802,#176803,
#176804,#176805,#176806,#176807),(#176808,#176809,#176810,#176811,#176812,
#176813,#176814,#176815,#176816,#176817,#176818,#176819,#176820,#176821,
#176822,#176823,#176824,#176825,#176826,#176827,#176828,#176829,#176830,
#176831,#176832,#176833,#176834,#176835,#176836,#176837,#176838,#176839,
#176840,#176841,#176842),(#176843,#176844,#176845,#176846,#176847,#176848,
#176849,#176850,#176851,#176852,#176853,#176854,#176855,#176856,#176857,
#176858,#176859,#176860,#176861,#176862,#176863,#176864,#176865,#176866,
#176867,#176868,#176869,#176870,#176871,#176872,#176873,#176874,#176875,
#176876,#176877),(#176878,#176879,#176880,#176881,#176882,#176883,#176884,
#176885,#176886,#176887,#176888,#176889,#176890,#176891,#176892,#176893,
#176894,#176895,#176896,#176897,#176898,#176899,#176900,#176901,#176902,
#176903,#176904,#176905,#176906,#176907,#176908,#176909,#176910,#176911,
#176912)),.UNSPECIFIED.,.F.,.F.,.F.,(4,4),(4,1,1,1,1,1,1,1,1,1,1,1,1,1,
1,1,1,1,1,1,1,1,1,1,1,1,1,1,1,1,1,1,4),(0.,1.),(0.,0.031250000000078,0.0625000000000372,
0.0937500000001152,0.125000000000074,0.156250000000034,0.187500000000111,
0.218750000000071,0.250000000000148,0.281250000000108,0.312500000000186,
0.343750000000145,0.375000000000104,0.406250000000182,0.437500000000141,
0.468750000000219,0.500000000000178,0.531250000000256,0.562500000000216,
0.593750000000175,0.625000000000253,0.656250000000212,0.68750000000029,
0.718750000000249,0.750000000000208,0.781250000000286,0.812500000000245,
0.843750000000323,0.875000000000282,0.90625000000036,0.93750000000032,0.968750000000279,
1.),.UNSPECIFIED.);
#185=B_SPLINE_SURFACE_WITH_KNOTS('',3,3,((#176995,#176996,#176997,#176998,
#176999,#177000,#177001,#177002,#177003,#177004,#177005,#177006,#177007,
#177008,#177009,#177010,#177011,#177012,#177013,#177014,#177015,#177016,
#177017,#177018,#177019,#177020,#177021,#177022,#177023,#177024,#177025,
#177026,#177027,#177028,#177029,#177030,#177031,#177032,#177033,#177034,
#177035,#177036,#177037,#177038,#177039,#177040,#177041,#177042,#177043,
#177044,#177045,#177046,#177047,#177048,#177049,#177050,#177051,#177052,
#177053,#177054,#177055,#177056,#177057,#177058,#177059,#177060,#177061),
(#177062,#177063,#177064,#177065,#177066,#177067,#177068,#177069,#177070,
#177071,#177072,#177073,#177074,#177075,#177076,#177077,#177078,#177079,
#177080,#177081,#177082,#177083,#177084,#177085,#177086,#177087,#177088,
#177089,#177090,#177091,#177092,#177093,#177094,#177095,#177096,#177097,
#177098,#177099,#177100,#177101,#177102,#177103,#177104,#177105,#177106,
#177107,#177108,#177109,#177110,#177111,#177112,#177113,#177114,#177115,
#177116,#177117,#177118,#177119,#177120,#177121,#177122,#177123,#177124,
#177125,#177126,#177127,#177128),(#177129,#177130,#177131,#177132,#177133,
#177134,#177135,#177136,#177137,#177138,#177139,#177140,#177141,#177142,
#177143,#177144,#177145,#177146,#177147,#177148,#177149,#177150,#177151,
#177152,#177153,#177154,#177155,#177156,#177157,#177158,#177159,#177160,
#177161,#177162,#177163,#177164,#177165,#177166,#177167,#177168,#177169,
#177170,#177171,#177172,#177173,#177174,#177175,#177176,#177177,#177178,
#177179,#177180,#177181,#177182,#177183,#177184,#177185,#177186,#177187,
#177188,#177189,#177190,#177191,#177192,#177193,#177194,#177195),(#177196,
#177197,#177198,#177199,#177200,#177201,#177202,#177203,#177204,#177205,
#177206,#177207,#177208,#177209,#177210,#177211,#177212,#177213,#177214,
#177215,#177216,#177217,#177218,#177219,#177220,#177221,#177222,#177223,
#177224,#177225,#177226,#177227,#177228,#177229,#177230,#177231,#177232,
#177233,#177234,#177235,#177236,#177237,#177238,#177239,#177240,#177241,
#177242,#177243,#177244,#177245,#177246,#177247,#177248,#177249,#177250,
#177251,#177252,#177253,#177254,#177255,#177256,#177257,#177258,#177259,
#177260,#177261,#177262)),.UNSPECIFIED.,.F.,.F.,.F.,(4,4),(4,1,1,1,1,1,
1,1,1,1,1,1,1,1,1,1,1,1,1,1,1,1,1,1,1,1,1,1,1,1,1,1,1,1,1,1,1,1,1,1,1,1,
1,1,1,1,1,1,1,1,1,1,1,1,1,1,1,1,1,1,1,1,1,1,4),(0.,1.),(0.,0.015625,0.03125,
0.046875,0.0625,0.078125,0.09375,0.109375,0.125,0.140625,0.15625,0.171875,
0.1875,0.203125,0.21875,0.234375,0.25,0.265625,0.28125,0.296875,0.3125,
0.328125,0.34375,0.359375,0.375,0.390625,0.40625,0.421875,0.4375,0.453125,
0.46875,0.484375,0.5,0.515625,0.53125,0.546875,0.5625,0.578125,0.59375,
0.609375,0.625,0.640625,0.65625,0.671875,0.6875,0.703125,0.71875,0.734375,
0.75,0.765625,0.78125,0.796875,0.8125,0.828125,0.84375,0.859375,0.875,0.890625,
0.90625,0.921875,0.9375,0.953125,0.96875,0.984375,1.),.UNSPECIFIED.);
#186=B_SPLINE_SURFACE_WITH_KNOTS('',3,3,((#177270,#177271,#177272,#177273,
#177274),(#177275,#177276,#177277,#177278,#177279),(#177280,#177281,#177282,
#177283,#177284),(#177285,#177286,#177287,#177288,#177289)),
 .UNSPECIFIED.,.F.,.F.,.F.,(4,4),(4,1,4),(0.,1.),(0.,0.500000000000012,
1.),.UNSPECIFIED.);
#187=B_SPLINE_SURFACE_WITH_KNOTS('',3,1,((#177348,#177349),(#177350,#177351),
(#177352,#177353),(#177354,#177355),(#177356,#177357),(#177358,#177359),
(#177360,#177361),(#177362,#177363),(#177364,#177365),(#177366,#177367),
(#177368,#177369),(#177370,#177371)),.UNSPECIFIED.,.F.,.F.,.F.,(4,2,2,2,
2,4),(2,2),(0.0140497253938099,0.25,0.5,0.75,0.875,0.987103459251385),(0.,
0.071789856256767),.UNSPECIFIED.);
#188=B_SPLINE_SURFACE_WITH_KNOTS('',3,3,((#177430,#177431,#177432,#177433,
#177434),(#177435,#177436,#177437,#177438,#177439),(#177440,#177441,#177442,
#177443,#177444),(#177445,#177446,#177447,#177448,#177449)),
 .UNSPECIFIED.,.F.,.F.,.F.,(4,4),(4,1,4),(0.,1.),(0.,0.500000000000012,
1.),.UNSPECIFIED.);
#189=B_SPLINE_SURFACE_WITH_KNOTS('',3,3,((#177456,#177457,#177458,#177459,
#177460,#177461,#177462,#177463,#177464,#177465,#177466,#177467,#177468,
#177469,#177470,#177471,#177472,#177473,#177474,#177475,#177476,#177477,
#177478,#177479,#177480,#177481,#177482,#177483,#177484,#177485,#177486,
#177487,#177488,#177489,#177490,#177491,#177492,#177493,#177494,#177495,
#177496,#177497,#177498,#177499,#177500,#177501,#177502,#177503,#177504,
#177505,#177506,#177507,#177508,#177509,#177510,#177511,#177512,#177513,
#177514,#177515,#177516,#177517,#177518,#177519,#177520,#177521,#177522),
(#177523,#177524,#177525,#177526,#177527,#177528,#177529,#177530,#177531,
#177532,#177533,#177534,#177535,#177536,#177537,#177538,#177539,#177540,
#177541,#177542,#177543,#177544,#177545,#177546,#177547,#177548,#177549,
#177550,#177551,#177552,#177553,#177554,#177555,#177556,#177557,#177558,
#177559,#177560,#177561,#177562,#177563,#177564,#177565,#177566,#177567,
#177568,#177569,#177570,#177571,#177572,#177573,#177574,#177575,#177576,
#177577,#177578,#177579,#177580,#177581,#177582,#177583,#177584,#177585,
#177586,#177587,#177588,#177589),(#177590,#177591,#177592,#177593,#177594,
#177595,#177596,#177597,#177598,#177599,#177600,#177601,#177602,#177603,
#177604,#177605,#177606,#177607,#177608,#177609,#177610,#177611,#177612,
#177613,#177614,#177615,#177616,#177617,#177618,#177619,#177620,#177621,
#177622,#177623,#177624,#177625,#177626,#177627,#177628,#177629,#177630,
#177631,#177632,#177633,#177634,#177635,#177636,#177637,#177638,#177639,
#177640,#177641,#177642,#177643,#177644,#177645,#177646,#177647,#177648,
#177649,#177650,#177651,#177652,#177653,#177654,#177655,#177656),(#177657,
#177658,#177659,#177660,#177661,#177662,#177663,#177664,#177665,#177666,
#177667,#177668,#177669,#177670,#177671,#177672,#177673,#177674,#177675,
#177676,#177677,#177678,#177679,#177680,#177681,#177682,#177683,#177684,
#177685,#177686,#177687,#177688,#177689,#177690,#177691,#177692,#177693,
#177694,#177695,#177696,#177697,#177698,#177699,#177700,#177701,#177702,
#177703,#177704,#177705,#177706,#177707,#177708,#177709,#177710,#177711,
#177712,#177713,#177714,#177715,#177716,#177717,#177718,#177719,#177720,
#177721,#177722,#177723)),.UNSPECIFIED.,.F.,.F.,.F.,(4,4),(4,1,1,1,1,1,
1,1,1,1,1,1,1,1,1,1,1,1,1,1,1,1,1,1,1,1,1,1,1,1,1,1,1,1,1,1,1,1,1,1,1,1,
1,1,1,1,1,1,1,1,1,1,1,1,1,1,1,1,1,1,1,1,1,1,4),(0.,1.),(0.,0.015625,0.03125,
0.046875,0.0625,0.078125,0.09375,0.109375,0.125,0.140625,0.15625,0.171875,
0.1875,0.203125,0.21875,0.234375,0.25,0.265625,0.28125,0.296875,0.3125,
0.328125,0.34375,0.359375,0.375,0.390625,0.40625,0.421875,0.4375,0.453125,
0.46875,0.484375,0.5,0.515625,0.53125,0.546875,0.5625,0.578125,0.59375,
0.609375,0.625,0.640625,0.65625,0.671875,0.6875,0.703125,0.71875,0.734375,
0.75,0.765625,0.78125,0.796875,0.8125,0.828125,0.84375,0.859375,0.875,0.890625,
0.90625,0.921875,0.9375,0.953125,0.96875,0.984375,1.),.UNSPECIFIED.);
#190=B_SPLINE_SURFACE_WITH_KNOTS('',3,3,((#177724,#177725,#177726,#177727,
#177728,#177729,#177730,#177731,#177732,#177733,#177734,#177735,#177736,
#177737,#177738,#177739,#177740,#177741,#177742,#177743,#177744,#177745,
#177746,#177747,#177748,#177749,#177750,#177751,#177752,#177753,#177754,
#177755,#177756,#177757,#177758),(#177759,#177760,#177761,#177762,#177763,
#177764,#177765,#177766,#177767,#177768,#177769,#177770,#177771,#177772,
#177773,#177774,#177775,#177776,#177777,#177778,#177779,#177780,#177781,
#177782,#177783,#177784,#177785,#177786,#177787,#177788,#177789,#177790,
#177791,#177792,#177793),(#177794,#177795,#177796,#177797,#177798,#177799,
#177800,#177801,#177802,#177803,#177804,#177805,#177806,#177807,#177808,
#177809,#177810,#177811,#177812,#177813,#177814,#177815,#177816,#177817,
#177818,#177819,#177820,#177821,#177822,#177823,#177824,#177825,#177826,
#177827,#177828),(#177829,#177830,#177831,#177832,#177833,#177834,#177835,
#177836,#177837,#177838,#177839,#177840,#177841,#177842,#177843,#177844,
#177845,#177846,#177847,#177848,#177849,#177850,#177851,#177852,#177853,
#177854,#177855,#177856,#177857,#177858,#177859,#177860,#177861,#177862,
#177863)),.UNSPECIFIED.,.F.,.F.,.F.,(4,4),(4,1,1,1,1,1,1,1,1,1,1,1,1,1,
1,1,1,1,1,1,1,1,1,1,1,1,1,1,1,1,1,1,4),(0.,1.),(0.,0.031250000000078,0.0625000000000372,
0.0937500000001152,0.125000000000074,0.156250000000034,0.187500000000111,
0.218750000000071,0.250000000000148,0.281250000000108,0.312500000000186,
0.343750000000145,0.375000000000104,0.406250000000182,0.437500000000141,
0.468750000000219,0.500000000000178,0.531250000000256,0.562500000000216,
0.593750000000175,0.625000000000253,0.656250000000212,0.68750000000029,
0.718750000000249,0.750000000000208,0.781250000000286,0.812500000000245,
0.843750000000323,0.875000000000282,0.90625000000036,0.93750000000032,0.968750000000279,
1.),.UNSPECIFIED.);
#288=FACE_BOUND('',#24771,.T.);
#289=FACE_BOUND('',#24781,.T.);
#290=FACE_BOUND('',#24783,.T.);
#1776=(
BOUNDED_CURVE()
B_SPLINE_CURVE(2,(#176260,#176261,#176262),.UNSPECIFIED.,.F.,.F.)
B_SPLINE_CURVE_WITH_KNOTS((3,3),(1.60808462077175,3.73981215786375),
 .UNSPECIFIED.)
CURVE()
GEOMETRIC_REPRESENTATION_ITEM()
RATIONAL_B_SPLINE_CURVE((1.37704917963476,1.5195025430206,1.37704917962903))
REPRESENTATION_ITEM('')
);
#1777=(
BOUNDED_CURVE()
B_SPLINE_CURVE(2,(#176266,#176267,#176268),.UNSPECIFIED.,.F.,.F.)
B_SPLINE_CURVE_WITH_KNOTS((3,3),(1.60809643499364,3.73983031850846),
 .UNSPECIFIED.)
CURVE()
GEOMETRIC_REPRESENTATION_ITEM()
RATIONAL_B_SPLINE_CURVE((1.37705242397036,1.51950612297573,1.37705242396606))
REPRESENTATION_ITEM('')
);
#1778=(
BOUNDED_CURVE()
B_SPLINE_CURVE(2,(#176272,#176273,#176274),.UNSPECIFIED.,.F.,.F.)
B_SPLINE_CURVE_WITH_KNOTS((3,3),(-3.73983031850955,-1.60809643499435),
 .UNSPECIFIED.)
CURVE()
GEOMETRIC_REPRESENTATION_ITEM()
RATIONAL_B_SPLINE_CURVE((1.37705242396626,1.51950612297595,1.37705242397056))
REPRESENTATION_ITEM('')
);
#1779=(
BOUNDED_CURVE()
B_SPLINE_CURVE(2,(#176278,#176279,#176280),.UNSPECIFIED.,.F.,.F.)
B_SPLINE_CURVE_WITH_KNOTS((3,3),(1.60808462077176,3.73981215785305),
 .UNSPECIFIED.)
CURVE()
GEOMETRIC_REPRESENTATION_ITEM()
RATIONAL_B_SPLINE_CURVE((1.37704917963477,1.51950254301989,1.37704917963046))
REPRESENTATION_ITEM('')
);
#1780=(
BOUNDED_CURVE()
B_SPLINE_CURVE(2,(#176284,#176285,#176286),.UNSPECIFIED.,.F.,.F.)
B_SPLINE_CURVE_WITH_KNOTS((3,3),(1.6080964349947,3.73983031851011),
 .UNSPECIFIED.)
CURVE()
GEOMETRIC_REPRESENTATION_ITEM()
RATIONAL_B_SPLINE_CURVE((1.37705242397066,1.51950612297606,1.37705242396636))
REPRESENTATION_ITEM('')
);
#1781=(
BOUNDED_CURVE()
B_SPLINE_CURVE(2,(#176295,#176296,#176297),.UNSPECIFIED.,.F.,.F.)
B_SPLINE_CURVE_WITH_KNOTS((3,3),(1.60809643499431,3.73983031850951),
 .UNSPECIFIED.)
CURVE()
GEOMETRIC_REPRESENTATION_ITEM()
RATIONAL_B_SPLINE_CURVE((1.37705242397056,1.51950612297595,1.37705242396626))
REPRESENTATION_ITEM('')
);
#1782=(
BOUNDED_CURVE()
B_SPLINE_CURVE(2,(#176302,#176303,#176304),.UNSPECIFIED.,.F.,.F.)
B_SPLINE_CURVE_WITH_KNOTS((3,3),(1.76947846838518,3.98831685496983),
 .UNSPECIFIED.)
CURVE()
GEOMETRIC_REPRESENTATION_ITEM()
RATIONAL_B_SPLINE_CURVE((1.42161885175909,1.56868287088003,1.4216188517602))
REPRESENTATION_ITEM('')
);
#1783=(
BOUNDED_CURVE()
B_SPLINE_CURVE(2,(#176308,#176309,#176310),.UNSPECIFIED.,.F.,.F.)
B_SPLINE_CURVE_WITH_KNOTS((3,3),(-3.98831685495251,-1.76947846838545),
 .UNSPECIFIED.)
CURVE()
GEOMETRIC_REPRESENTATION_ITEM()
RATIONAL_B_SPLINE_CURVE((1.42161885176135,1.56868287087821,1.42161885175878))
REPRESENTATION_ITEM('')
);
#1784=(
BOUNDED_CURVE()
B_SPLINE_CURVE(2,(#176314,#176315,#176316),.UNSPECIFIED.,.F.,.F.)
B_SPLINE_CURVE_WITH_KNOTS((3,3),(1.76947846838546,3.98831685495253),
 .UNSPECIFIED.)
CURVE()
GEOMETRIC_REPRESENTATION_ITEM()
RATIONAL_B_SPLINE_CURVE((1.42161885175877,1.56868287087821,1.42161885176135))
REPRESENTATION_ITEM('')
);
#1785=(
BOUNDED_CURVE()
B_SPLINE_CURVE(2,(#176320,#176321,#176322),.UNSPECIFIED.,.F.,.F.)
B_SPLINE_CURVE_WITH_KNOTS((3,3),(1.76947846838366,3.98831685496745),
 .UNSPECIFIED.)
CURVE()
GEOMETRIC_REPRESENTATION_ITEM()
RATIONAL_B_SPLINE_CURVE((1.42161885175867,1.56868287087957,1.42161885175978))
REPRESENTATION_ITEM('')
);
#1786=(
BOUNDED_CURVE()
B_SPLINE_CURVE(2,(#176326,#176327,#176328),.UNSPECIFIED.,.F.,.F.)
B_SPLINE_CURVE_WITH_KNOTS((3,3),(-3.98831685495252,-1.76947846838541),
 .UNSPECIFIED.)
CURVE()
GEOMETRIC_REPRESENTATION_ITEM()
RATIONAL_B_SPLINE_CURVE((1.42161885176135,1.56868287087821,1.42161885175877))
REPRESENTATION_ITEM('')
);
#1787=(
BOUNDED_CURVE()
B_SPLINE_CURVE(2,(#176337,#176338,#176339),.UNSPECIFIED.,.F.,.F.)
B_SPLINE_CURVE_WITH_KNOTS((3,3),(-3.98831685495253,-1.7694784683854),
 .UNSPECIFIED.)
CURVE()
GEOMETRIC_REPRESENTATION_ITEM()
RATIONAL_B_SPLINE_CURVE((1.42161885176135,1.56868287087822,1.42161885175877))
REPRESENTATION_ITEM('')
);
#1939=CONICAL_SURFACE('',#80684,12.750003108,0.785398266415682);
#1940=CONICAL_SURFACE('',#80686,15.,0.7853981625);
#1941=CONICAL_SURFACE('',#80695,15.,0.7853981625);
#2211=CYLINDRICAL_SURFACE('',#80668,13.0486498132185);
#2212=CYLINDRICAL_SURFACE('',#80669,13.0486498132185);
#2213=CYLINDRICAL_SURFACE('',#80670,13.0486498132185);
#2214=CYLINDRICAL_SURFACE('',#80671,12.25);
#2215=CYLINDRICAL_SURFACE('',#80673,12.25);
#2216=CYLINDRICAL_SURFACE('',#80674,12.25);
#2217=CYLINDRICAL_SURFACE('',#80675,12.25);
#2218=CYLINDRICAL_SURFACE('',#80676,12.25);
#2219=CYLINDRICAL_SURFACE('',#80678,10.5);
#2220=CYLINDRICAL_SURFACE('',#80681,12.25);
#2221=CYLINDRICAL_SURFACE('',#80683,13.0486498132185);
#2222=CYLINDRICAL_SURFACE('',#80704,16.);
#2223=CYLINDRICAL_SURFACE('',#80708,16.);
#2224=CYLINDRICAL_SURFACE('',#80709,16.);
#2225=CYLINDRICAL_SURFACE('',#80712,16.);
#2226=CYLINDRICAL_SURFACE('',#80713,16.);
#2227=CYLINDRICAL_SURFACE('',#80714,16.);
#3116=LINE('',#174769,#10183);
#3117=LINE('',#174847,#10184);
#3118=LINE('',#174927,#10185);
#3119=LINE('',#175093,#10186);
#3120=LINE('',#175123,#10187);
#3121=LINE('',#175188,#10188);
#3122=LINE('',#175253,#10189);
#3123=LINE('',#175334,#10190);
#3124=LINE('',#175494,#10191);
#3125=LINE('',#175659,#10192);
#3126=LINE('',#175816,#10193);
#3127=LINE('',#175831,#10194);
#3128=LINE('',#176150,#10195);
#3129=LINE('',#176290,#10196);
#3130=LINE('',#176332,#10197);
#3131=LINE('',#176342,#10198);
#3132=LINE('',#176343,#10199);
#3133=LINE('',#176345,#10200);
#3134=LINE('',#176346,#10201);
#3135=LINE('',#176348,#10202);
#3136=LINE('',#176350,#10203);
#3137=LINE('',#176352,#10204);
#3138=LINE('',#176354,#10205);
#3139=LINE('',#176356,#10206);
#3140=LINE('',#176358,#10207);
#3141=LINE('',#176359,#10208);
#3142=LINE('',#176362,#10209);
#3143=LINE('',#176772,#10210);
#3144=LINE('',#177269,#10211);
#10183=VECTOR('',#88953,13.0486498132185);
#10184=VECTOR('',#88954,10.);
#10185=VECTOR('',#88957,13.0486498132185);
#10186=VECTOR('',#88960,13.0486498132185);
#10187=VECTOR('',#88963,12.25);
#10188=VECTOR('',#88964,10.);
#10189=VECTOR('',#88965,12.25);
#10190=VECTOR('',#88970,12.25);
#10191=VECTOR('',#88973,12.25);
#10192=VECTOR('',#88976,12.25);
#10193=VECTOR('',#88979,12.25);
#10194=VECTOR('',#88986,10.5);
#10195=VECTOR('',#88997,12.750003108);
#10196=VECTOR('',#89012,15.);
#10197=VECTOR('',#89031,15.);
#10198=VECTOR('',#89040,1000.);
#10199=VECTOR('',#89041,1000.);
#10200=VECTOR('',#89044,1000.);
#10201=VECTOR('',#89045,1000.);
#10202=VECTOR('',#89048,1000.);
#10203=VECTOR('',#89051,1000.);
#10204=VECTOR('',#89054,1000.);
#10205=VECTOR('',#89057,1000.);
#10206=VECTOR('',#89060,1000.);
#10207=VECTOR('',#89063,1000.);
#10208=VECTOR('',#89064,1000.);
#10209=VECTOR('',#89069,1000.);
#10210=VECTOR('',#89076,10.);
#10211=VECTOR('',#89077,10.);
#16971=PLANE('',#80705);
#16972=PLANE('',#80706);
#16973=PLANE('',#80707);
#16974=PLANE('',#80710);
#16975=PLANE('',#80711);
#16976=PLANE('',#80715);
#16977=PLANE('',#80716);
#16978=PLANE('',#80717);
#16979=PLANE('',#80718);
#20686=FACE_OUTER_BOUND('',#24744,.T.);
#20687=FACE_OUTER_BOUND('',#24745,.T.);
#20688=FACE_OUTER_BOUND('',#24746,.T.);
#20689=FACE_OUTER_BOUND('',#24747,.T.);
#20690=FACE_OUTER_BOUND('',#24748,.T.);
#20691=FACE_OUTER_BOUND('',#24749,.T.);
#20692=FACE_OUTER_BOUND('',#24750,.T.);
#20693=FACE_OUTER_BOUND('',#24751,.T.);
#20694=FACE_OUTER_BOUND('',#24752,.T.);
#20695=FACE_OUTER_BOUND('',#24753,.T.);
#20696=FACE_OUTER_BOUND('',#24754,.T.);
#20697=FACE_OUTER_BOUND('',#24755,.T.);
#20698=FACE_OUTER_BOUND('',#24756,.T.);
#20699=FACE_OUTER_BOUND('',#24757,.T.);
#20700=FACE_OUTER_BOUND('',#24758,.T.);
#20701=FACE_OUTER_BOUND('',#24759,.T.);
#20702=FACE_OUTER_BOUND('',#24760,.T.);
#20703=FACE_OUTER_BOUND('',#24761,.T.);
#20704=FACE_OUTER_BOUND('',#24762,.T.);
#20705=FACE_OUTER_BOUND('',#24763,.T.);
#20706=FACE_OUTER_BOUND('',#24764,.T.);
#20707=FACE_OUTER_BOUND('',#24765,.T.);
#20708=FACE_OUTER_BOUND('',#24766,.T.);
#20709=FACE_OUTER_BOUND('',#24767,.T.);
#20710=FACE_OUTER_BOUND('',#24768,.T.);
#20711=FACE_OUTER_BOUND('',#24769,.T.);
#20712=FACE_OUTER_BOUND('',#24770,.T.);
#20713=FACE_OUTER_BOUND('',#24772,.T.);
#20714=FACE_OUTER_BOUND('',#24773,.T.);
#20715=FACE_OUTER_BOUND('',#24774,.T.);
#20716=FACE_OUTER_BOUND('',#24775,.T.);
#20717=FACE_OUTER_BOUND('',#24776,.T.);
#20718=FACE_OUTER_BOUND('',#24777,.T.);
#20719=FACE_OUTER_BOUND('',#24778,.T.);
#20720=FACE_OUTER_BOUND('',#24779,.T.);
#20721=FACE_OUTER_BOUND('',#24780,.T.);
#20722=FACE_OUTER_BOUND('',#24782,.T.);
#24744=EDGE_LOOP('',(#56375,#56376,#56377,#56378,#56379));
#24745=EDGE_LOOP('',(#56380,#56381,#56382,#56383));
#24746=EDGE_LOOP('',(#56384,#56385,#56386,#56387));
#24747=EDGE_LOOP('',(#56388,#56389,#56390,#56391,#56392,#56393,#56394,#56395,
#56396,#56397,#56398,#56399));
#24748=EDGE_LOOP('',(#56400,#56401,#56402,#56403));
#24749=EDGE_LOOP('',(#56404,#56405,#56406,#56407,#56408));
#24750=EDGE_LOOP('',(#56409,#56410,#56411,#56412,#56413));
#24751=EDGE_LOOP('',(#56414,#56415,#56416));
#24752=EDGE_LOOP('',(#56417,#56418,#56419,#56420));
#24753=EDGE_LOOP('',(#56421,#56422,#56423,#56424,#56425,#56426));
#24754=EDGE_LOOP('',(#56427,#56428,#56429,#56430));
#24755=EDGE_LOOP('',(#56431,#56432,#56433,#56434,#56435,#56436,#56437,#56438,
#56439,#56440));
#24756=EDGE_LOOP('',(#56441,#56442,#56443,#56444,#56445,#56446,#56447,#56448,
#56449,#56450,#56451,#56452,#56453,#56454,#56455,#56456));
#24757=EDGE_LOOP('',(#56457,#56458,#56459,#56460,#56461,#56462,#56463,#56464,
#56465,#56466,#56467,#56468,#56469,#56470,#56471,#56472));
#24758=EDGE_LOOP('',(#56473,#56474,#56475,#56476,#56477));
#24759=EDGE_LOOP('',(#56478,#56479,#56480,#56481));
#24760=EDGE_LOOP('',(#56482,#56483,#56484,#56485));
#24761=EDGE_LOOP('',(#56486,#56487,#56488,#56489));
#24762=EDGE_LOOP('',(#56490,#56491,#56492,#56493));
#24763=EDGE_LOOP('',(#56494,#56495,#56496,#56497));
#24764=EDGE_LOOP('',(#56498,#56499,#56500,#56501));
#24765=EDGE_LOOP('',(#56502,#56503,#56504,#56505));
#24766=EDGE_LOOP('',(#56506,#56507,#56508,#56509));
#24767=EDGE_LOOP('',(#56510,#56511,#56512,#56513));
#24768=EDGE_LOOP('',(#56514,#56515,#56516,#56517,#56518));
#24769=EDGE_LOOP('',(#56519,#56520,#56521,#56522));
#24770=EDGE_LOOP('',(#56523));
#24771=EDGE_LOOP('',(#56524));
#24772=EDGE_LOOP('',(#56525,#56526,#56527,#56528,#56529,#56530,#56531));
#24773=EDGE_LOOP('',(#56532,#56533,#56534,#56535,#56536));
#24774=EDGE_LOOP('',(#56537,#56538,#56539,#56540,#56541,#56542,#56543,#56544,
#56545,#56546,#56547));
#24775=EDGE_LOOP('',(#56548,#56549,#56550));
#24776=EDGE_LOOP('',(#56551,#56552,#56553,#56554));
#24777=EDGE_LOOP('',(#56555,#56556,#56557));
#24778=EDGE_LOOP('',(#56558,#56559,#56560,#56561,#56562,#56563,#56564,#56565,
#56566,#56567,#56568,#56569));
#24779=EDGE_LOOP('',(#56570,#56571,#56572,#56573,#56574,#56575,#56576));
#24780=EDGE_LOOP('',(#56577));
#24781=EDGE_LOOP('',(#56578));
#24782=EDGE_LOOP('',(#56579));
#24783=EDGE_LOOP('',(#56580));
#30194=B_SPLINE_CURVE_WITH_KNOTS('',3,(#174771,#174772,#174773,#174774,
#174775,#174776,#174777,#174778,#174779,#174780,#174781,#174782,#174783,
#174784,#174785,#174786,#174787,#174788,#174789,#174790,#174791,#174792,
#174793,#174794,#174795,#174796,#174797,#174798,#174799,#174800,#174801,
#174802,#174803,#174804,#174805,#174806,#174807,#174808,#174809,#174810),
 .UNSPECIFIED.,.F.,.F.,(4,2,2,2,2,2,2,2,2,2,2,2,2,2,2,2,2,2,2,4),(16.4121932386951,
16.5930208425103,16.8461078239737,17.0995968965712,17.3585819104816,17.5388688400622,
17.7351706126336,17.9578257108876,18.1560633677355,18.4119469970658,18.5365531367551,
18.7858967699952,19.0446361984666,19.2963636739384,19.55282938767,19.7628209649916,
19.9947900143882,20.2506006554381,20.3828496027218,20.5152088298456),
 .UNSPECIFIED.);
#30195=B_SPLINE_CURVE_WITH_KNOTS('',3,(#174812,#174813,#174814,#174815,
#174816,#174817,#174818,#174819,#174820,#174821,#174822,#174823,#174824,
#174825,#174826,#174827,#174828,#174829,#174830,#174831,#174832,#174833,
#174834,#174835,#174836,#174837,#174838,#174839,#174840,#174841,#174842,
#174843,#174844,#174845),.UNSPECIFIED.,.F.,.F.,(4,2,2,2,2,2,2,2,2,2,2,2,
2,2,2,2,4),(-3.6474313045369,-3.33257853570554,-3.227803824618,-2.94609671662879,
-2.68640335638716,-2.43382900975872,-2.07865629233525,-1.82329744429604,
-1.69779781579172,-1.49131358643697,-1.27057756142443,-1.11563261308778,
-0.88437607370081,-0.690814598987342,-0.518873862845574,-0.260515535696464,
-0.000141823912015449),.UNSPECIFIED.);
#30196=B_SPLINE_CURVE_WITH_KNOTS('',3,(#174848,#174849,#174850,#174851,
#174852,#174853,#174854,#174855,#174856,#174857,#174858,#174859,#174860,
#174861,#174862,#174863,#174864,#174865,#174866,#174867,#174868,#174869,
#174870,#174871,#174872,#174873,#174874,#174875,#174876,#174877,#174878,
#174879,#174880,#174881,#174882,#174883,#174884,#174885,#174886,#174887,
#174888,#174889,#174890,#174891,#174892,#174893,#174894,#174895,#174896,
#174897,#174898,#174899,#174900,#174901,#174902,#174903,#174904,#174905,
#174906,#174907,#174908,#174909,#174910,#174911,#174912,#174913,#174914,
#174915,#174916,#174917,#174918,#174919,#174920,#174921,#174922,#174923),
 .UNSPECIFIED.,.F.,.F.,(4,2,2,2,2,2,2,2,2,2,2,2,2,2,2,2,2,2,2,2,2,2,2,2,
2,2,2,2,2,2,2,2,2,2,2,2,2,4),(0.00016549378706301,0.131853006236288,0.261698990576789,
0.517935066297707,0.716387983891709,0.935197434746891,1.10002486633248,
1.35980835922816,1.48446952560043,1.71312228306834,1.93117096309254,2.15262213646806,
2.32001636811431,2.54132664418812,2.66830819062656,2.92738142725857,3.15039093059539,
3.40877332402121,3.5279082179231,3.78654252090004,3.91245989974845,4.17113821618592,
4.39785287753683,4.52271772135692,4.75314615630485,5.01177835618428,5.26798072414789,
5.52059832272264,5.77934187635112,6.01221566186675,6.2089902580178,6.43228727960982,
6.55702649342403,6.85144774364401,7.05924514976984,7.31290959162113,7.56649104411875,
7.75004480391499),.UNSPECIFIED.);
#30197=B_SPLINE_CURVE_WITH_KNOTS('',3,(#174928,#174929,#174930,#174931,
#174932,#174933,#174934,#174935,#174936,#174937,#174938,#174939,#174940,
#174941,#174942,#174943,#174944,#174945,#174946,#174947,#174948,#174949,
#174950,#174951,#174952,#174953,#174954,#174955,#174956,#174957,#174958,
#174959,#174960,#174961,#174962,#174963,#174964,#174965,#174966,#174967,
#174968,#174969,#174970,#174971,#174972,#174973,#174974,#174975,#174976,
#174977,#174978,#174979,#174980,#174981,#174982,#174983,#174984,#174985,
#174986,#174987,#174988,#174989,#174990,#174991,#174992,#174993,#174994,
#174995,#174996,#174997,#174998,#174999,#175000,#175001,#175002,#175003,
#175004,#175005,#175006,#175007,#175008,#175009),.UNSPECIFIED.,.F.,.F.,
(4,2,2,2,2,2,2,2,2,2,2,2,2,2,2,2,2,2,2,2,2,2,2,2,2,2,2,2,2,2,2,2,2,2,2,
2,2,2,2,2,4),(8.20592890423442,8.38225901240072,8.58683139065276,8.84279381561286,
9.0951465132682,9.35392458008801,9.58374870993814,9.78041991532572,10.0036274478047,
10.2573713007949,10.3819176450443,10.6913316732546,10.8165222413783,11.0495245517201,
11.3082425310969,11.4351743696995,11.6938511186544,11.9424279723859,12.069447778218,
12.1989595233584,12.4572536185707,12.7210408379567,12.8463169911851,13.0577955603349,
13.3169325646344,13.442420483011,13.6682306643446,13.8691273183975,14.1287661136922,
14.2540792835159,14.4824506400339,14.6773644422413,14.8960058930337,15.1180021367018,
15.3775153577096,15.5047943278521,15.7168300382009,15.9908120819898,16.1159914931326,
16.3579030196544,16.4121932386951),.UNSPECIFIED.);
#30198=B_SPLINE_CURVE_WITH_KNOTS('',3,(#175010,#175011,#175012,#175013,
#175014,#175015,#175016,#175017,#175018,#175019,#175020,#175021,#175022,
#175023,#175024,#175025,#175026,#175027,#175028,#175029,#175030,#175031,
#175032,#175033,#175034,#175035,#175036,#175037,#175038,#175039,#175040,
#175041,#175042,#175043,#175044,#175045,#175046,#175047,#175048,#175049,
#175050,#175051,#175052,#175053,#175054,#175055,#175056,#175057,#175058,
#175059,#175060,#175061,#175062,#175063,#175064,#175065,#175066,#175067,
#175068,#175069,#175070,#175071,#175072,#175073,#175074,#175075,#175076,
#175077,#175078,#175079,#175080,#175081,#175082,#175083,#175084,#175085,
#175086,#175087,#175088,#175089),.UNSPECIFIED.,.F.,.F.,(4,2,2,2,2,2,2,2,
2,2,2,2,2,2,2,2,2,2,2,2,2,2,2,2,2,2,2,2,2,2,2,2,2,2,2,2,2,2,2,4),(7.75004480391499,
7.82559307735231,8.02118525258592,8.28072501906034,8.53379530147537,8.78758376914345,
9.04716113331003,9.26718216598056,9.48610231574621,9.68024537017959,9.90991871172859,
10.0351114292772,10.2947553276189,10.4946157112935,10.7212580175289,10.8466614421288,
11.1058000116479,11.315608428921,11.5469143693834,11.6982130176188,11.9566159027608,
12.0810892128377,12.3325158027635,12.5428800202823,12.7596011729384,13.018863254076,
13.2712859568414,13.5242570694265,13.7833183753977,13.9461601162603,14.1487791549318,
14.4077051927678,14.6664417651085,14.7937668432316,14.9917838884636,15.2409388250797,
15.365460191223,15.692537035722,15.8184776621585,15.9564624294639),
 .UNSPECIFIED.);
#30199=B_SPLINE_CURVE_WITH_KNOTS('',3,(#175095,#175096,#175097,#175098,
#175099,#175100,#175101,#175102,#175103,#175104),.UNSPECIFIED.,.F.,.F.,
(4,2,2,2,4),(0.00012251398680704,0.222884378529215,0.446676969347221,0.675563919564766,
0.912296554340543),.UNSPECIFIED.);
#30200=B_SPLINE_CURVE_WITH_KNOTS('',3,(#175106,#175107,#175108,#175109),
 .UNSPECIFIED.,.F.,.F.,(4,4),(0.,1.),.UNSPECIFIED.);
#30201=B_SPLINE_CURVE_WITH_KNOTS('',3,(#175110,#175111,#175112,#175113,
#175114,#175115,#175116,#175117,#175118,#175119),.UNSPECIFIED.,.F.,.F.,
(4,2,2,2,4),(-0.912452539736231,-0.684829823365555,-0.456379958242761,-0.343466785291313,
-6.86284440254452E-5),.UNSPECIFIED.);
#30202=B_SPLINE_CURVE_WITH_KNOTS('',3,(#175125,#175126,#175127,#175128,
#175129,#175130,#175131,#175132,#175133,#175134,#175135,#175136,#175137,
#175138,#175139,#175140,#175141,#175142,#175143,#175144,#175145,#175146,
#175147,#175148,#175149,#175150,#175151,#175152,#175153,#175154,#175155,
#175156,#175157,#175158,#175159,#175160,#175161,#175162,#175163,#175164),
 .UNSPECIFIED.,.F.,.F.,(4,2,2,2,2,2,2,2,2,2,2,2,2,2,2,2,2,2,2,4),(-3.85213857003362,
-3.81351780802066,-3.57037494324692,-3.33336412591946,-3.0942360656147,
-2.85103108402327,-2.66918050910776,-2.42599071864031,-2.18949413218482,
-1.95059174770184,-1.70741763335434,-1.54072919441616,-1.29745630963647,
-1.1796044847409,-0.936390049858489,-0.746647776807323,-0.564050922972708,
-0.425460046457917,-0.21305312129021,-9.9999999880751E-7),.UNSPECIFIED.);
#30203=B_SPLINE_CURVE_WITH_KNOTS('',3,(#175166,#175167,#175168,#175169,
#175170,#175171,#175172,#175173,#175174,#175175),.UNSPECIFIED.,.F.,.F.,
(4,2,2,2,4),(-0.856199781211949,-0.642101402330201,-0.428204524303596,-0.321759740087164,
0.),.UNSPECIFIED.);
#30204=B_SPLINE_CURVE_WITH_KNOTS('',3,(#175177,#175178,#175179,#175180,
#175181,#175182,#175183,#175184,#175185,#175186),.UNSPECIFIED.,.F.,.F.,
(4,2,2,2,4),(-1.24857216709431,-0.938370073706321,-0.624319392609352,-0.314072407460326,
-1.91505823752094E-6),.UNSPECIFIED.);
#30205=B_SPLINE_CURVE_WITH_KNOTS('',3,(#175190,#175191,#175192,#175193,
#175194,#175195,#175196,#175197,#175198,#175199),.UNSPECIFIED.,.F.,.F.,
(4,2,2,2,4),(-1.24672715675223,-0.93314257651352,-0.623377583747238,-0.309803734768785,
-7.91147253157414E-5),.UNSPECIFIED.);
#30206=B_SPLINE_CURVE_WITH_KNOTS('',3,(#175201,#175202,#175203,#175204,
#175205,#175206,#175207,#175208,#175209,#175210),.UNSPECIFIED.,.F.,.F.,
(4,2,2,2,4),(-0.85620344504851,-0.534443747738202,-0.427999096338968,-0.214103034436511,
-6.19686688838123E-6),.UNSPECIFIED.);
#30207=B_SPLINE_CURVE_WITH_KNOTS('',3,(#175212,#175213,#175214,#175215,
#175216,#175217,#175218,#175219,#175220,#175221,#175222,#175223,#175224,
#175225,#175226,#175227,#175228,#175229,#175230,#175231,#175232,#175233,
#175234,#175235,#175236,#175237,#175238,#175239,#175240,#175241,#175242,
#175243,#175244,#175245,#175246,#175247,#175248,#175249,#175250,#175251),
 .UNSPECIFIED.,.F.,.F.,(4,2,2,2,2,2,2,2,2,2,2,2,2,2,2,2,2,2,2,4),(-22.6866943890527,
-22.5303032047481,-22.3763846167728,-22.0766259920643,-21.874826864479,
-21.6366463018233,-21.4013557329154,-21.1773704733836,-20.9343396078115,
-20.8169433024953,-20.606787502898,-20.3635497033644,-20.2099007632458,
-19.9667622500637,-19.8236447234393,-19.5805449222105,-19.4401009849293,
-19.1970125819126,-19.0572964760453,-18.834521337081),.UNSPECIFIED.);
#30208=B_SPLINE_CURVE_WITH_KNOTS('',3,(#175255,#175256,#175257,#175258,
#175259,#175260,#175261,#175262,#175263,#175264,#175265,#175266,#175267,
#175268,#175269,#175270,#175271,#175272,#175273,#175274,#175275,#175276,
#175277,#175278,#175279,#175280,#175281,#175282,#175283,#175284,#175285,
#175286,#175287,#175288,#175289,#175290,#175291,#175292,#175293,#175294,
#175295,#175296,#175297,#175298,#175299,#175300,#175301,#175302,#175303,
#175304,#175305,#175306,#175307,#175308,#175309,#175310,#175311,#175312,
#175313,#175314,#175315,#175316,#175317,#175318,#175319,#175320,#175321,
#175322,#175323,#175324,#175325,#175326,#175327,#175328,#175329,#175330),
 .UNSPECIFIED.,.F.,.F.,(4,2,2,2,2,2,2,2,2,2,2,2,2,2,2,2,2,2,2,2,2,2,2,2,
2,2,2,2,2,2,2,2,2,2,2,2,2,4),(-18.834521337081,-18.8142112428211,-18.6930610625541,
-18.4498270202033,-18.2105484733472,-17.9729461594295,-17.7431487367217,
-17.5442087098032,-17.4253111128454,-17.1905951849816,-16.9473337588043,
-16.7732130783734,-16.5300185480996,-16.2909841113175,-16.0542185594088,
-15.8253352177396,-15.6305501116955,-15.3873225387848,-15.1480794265471,
-14.9107046837507,-14.6809797436391,-14.4834330965413,-14.2402014100838,
-14.0009428884633,-13.7634982178047,-13.5337512383856,-13.3357958936231,
-13.0925628681154,-12.853301565187,-12.6158460453357,-12.3726617626798,
-12.1855926241435,-11.9423727181238,-11.8245607822377,-11.5812786032023,
-11.3433366492245,-11.2260753874151,-11.1297961553119),.UNSPECIFIED.);
#30209=B_SPLINE_CURVE_WITH_KNOTS('',3,(#175335,#175336,#175337,#175338,
#175339,#175340,#175341,#175342,#175343,#175344,#175345,#175346,#175347,
#175348,#175349,#175350,#175351,#175352,#175353,#175354,#175355,#175356,
#175357,#175358,#175359,#175360,#175361,#175362,#175363,#175364,#175365,
#175366,#175367,#175368,#175369,#175370,#175371,#175372,#175373,#175374,
#175375,#175376,#175377,#175378,#175379,#175380,#175381,#175382,#175383,
#175384,#175385,#175386,#175387,#175388,#175389,#175390,#175391,#175392,
#175393,#175394,#175395,#175396,#175397,#175398,#175399,#175400,#175401,
#175402,#175403,#175404,#175405,#175406,#175407,#175408,#175409,#175410,
#175411,#175412,#175413,#175414),.UNSPECIFIED.,.F.,.F.,(4,2,2,2,2,2,2,2,
2,2,2,2,2,2,2,2,2,2,2,2,2,2,2,2,2,2,2,2,2,2,2,2,2,2,2,2,2,2,2,4),(-11.556536076899,
-11.4599091059737,-11.3426764930753,-11.1047897385837,-10.8615067205227,
-10.7436737873529,-10.5004512226842,-10.3121637978976,-10.0689968772169,
-9.83134858415051,-9.59206264015326,-9.34882015260983,-9.22766368519635,
-8.9845680610119,-8.843924548653,-8.6008153678,-8.45696131749682,-8.21380668176722,
-8.05705534469272,-7.81379525350039,-7.69704438167437,-7.45394461400543,
-7.31199668399831,-7.06886954234882,-6.91997962388108,-6.67677155065413,
-6.49576195805203,-6.25255623119234,-6.01622745272294,-5.77741013639552,
-5.53424261099661,-5.37197812846586,-5.12870441503673,-5.0113059354371,
-4.76813077786016,-4.60232369259186,-4.35904771161803,-4.24128069760431,
-3.99807056728671,-3.85213857003362),.UNSPECIFIED.);
#30210=B_SPLINE_CURVE_WITH_KNOTS('',3,(#175415,#175416,#175417,#175418,
#175419,#175420,#175421,#175422,#175423,#175424,#175425,#175426,#175427,
#175428,#175429,#175430,#175431,#175432,#175433,#175434,#175435,#175436,
#175437,#175438,#175439,#175440,#175441,#175442,#175443,#175444,#175445,
#175446,#175447,#175448,#175449,#175450,#175451,#175452,#175453,#175454,
#175455,#175456,#175457,#175458,#175459,#175460,#175461,#175462,#175463,
#175464,#175465,#175466,#175467,#175468,#175469,#175470,#175471,#175472,
#175473,#175474,#175475,#175476,#175477,#175478,#175479,#175480,#175481,
#175482,#175483,#175484,#175485,#175486,#175487,#175488,#175489,#175490),
 .UNSPECIFIED.,.F.,.F.,(4,2,2,2,2,2,2,2,2,2,2,2,2,2,2,2,2,2,2,2,2,2,2,2,
2,2,2,2,2,2,2,2,2,2,2,2,2,4),(-11.1297961553119,-10.9829100940662,-10.8230475417878,
-10.5797749840848,-10.4626462024022,-10.2194975040537,-10.0647874730273,
-9.82153667980929,-9.60379690366332,-9.48630400015833,-9.25101963163764,
-9.02527872492806,-8.78940634808324,-8.55085145790989,-8.30771488641139,
-8.15596340970547,-7.91273314934468,-7.71509397891962,-7.48536686971287,
-7.24797705560601,-7.00873489582634,-6.76550808682275,-6.57009088441412,
-6.34046536874229,-6.1034716395441,-5.86434868796832,-5.62114284806789,
-5.43991081232665,-5.19671060384064,-4.96033806115533,-4.72149865938757,
-4.47833071347064,-4.31490529075738,-4.07163241624487,-3.95410997527723,
-3.71092437494605,-3.53930859415792,-3.4252187051346),.UNSPECIFIED.);
#30211=B_SPLINE_CURVE_WITH_KNOTS('',3,(#175495,#175496,#175497,#175498,
#175499,#175500,#175501,#175502,#175503,#175504,#175505,#175506,#175507,
#175508,#175509,#175510,#175511,#175512,#175513,#175514,#175515,#175516,
#175517,#175518,#175519,#175520,#175521,#175522,#175523,#175524,#175525,
#175526,#175527,#175528,#175529,#175530,#175531,#175532,#175533,#175534,
#175535,#175536,#175537,#175538,#175539,#175540,#175541,#175542,#175543,
#175544,#175545,#175546,#175547,#175548,#175549,#175550,#175551,#175552,
#175553,#175554,#175555,#175556,#175557,#175558,#175559,#175560,#175561,
#175562,#175563,#175564,#175565,#175566,#175567,#175568,#175569,#175570,
#175571,#175572,#175573,#175574,#175575,#175576),.UNSPECIFIED.,.F.,.F.,
(4,2,2,2,2,2,2,2,2,2,2,2,2,2,2,2,2,2,2,2,2,2,2,2,2,2,2,2,2,2,2,2,2,2,2,
2,2,2,2,2,4),(-19.2607415147143,-19.2489929067448,-19.0136586011244,-18.7895409073619,
-18.5497501962804,-18.4323267611571,-18.2193903806131,-17.9761525636568,
-17.857981437046,-17.6147127766078,-17.4445175126809,-17.2013362482858,
-17.054552499899,-16.9362847960168,-16.6680676760938,-16.4249963674093,
-16.2863690742156,-16.0432880999595,-15.9221398697641,-15.6789072259686,
-15.4396337893472,-15.2020777881446,-14.9722964554593,-14.7736460914282,
-14.5304165486609,-14.3785045838873,-14.1353690015121,-14.0183188143693,
-13.7750525066905,-13.6158393249603,-13.3726799597151,-13.2554372067625,
-13.0451087988904,-12.858355020038,-12.6151371326671,-12.465210290949,-12.2220782456079,
-12.1050826480636,-11.8618144997283,-11.7030704694281,-11.556536076899),
 .UNSPECIFIED.);
#30212=B_SPLINE_CURVE_WITH_KNOTS('',3,(#175578,#175579,#175580,#175581,
#175582,#175583,#175584,#175585,#175586,#175587,#175588,#175589,#175590,
#175591,#175592,#175593,#175594,#175595,#175596,#175597,#175598,#175599,
#175600,#175601,#175602,#175603,#175604,#175605,#175606,#175607,#175608,
#175609),.UNSPECIFIED.,.F.,.F.,(4,2,2,2,2,2,2,2,2,2,2,2,2,2,2,4),(-3.4252187051346,
-3.296042216674,-3.17775013519778,-2.9345032039866,-2.82052273167594,-2.58476260927433,
-2.37502283991358,-2.13188994584829,-1.89482091514807,-1.65567382322027,
-1.41246801058212,-1.22857993508971,-0.985427993245079,-0.748545735313343,
-0.373606352085642,-8.37234906265989E-5),.UNSPECIFIED.);
#30213=B_SPLINE_CURVE_WITH_KNOTS('',3,(#175610,#175611,#175612,#175613,
#175614,#175615,#175616,#175617,#175618,#175619,#175620,#175621,#175622,
#175623,#175624,#175625,#175626,#175627,#175628,#175629,#175630,#175631,
#175632,#175633,#175634,#175635,#175636,#175637,#175638,#175639,#175640,
#175641,#175642,#175643,#175644,#175645,#175646,#175647,#175648,#175649,
#175650,#175651,#175652,#175653,#175654,#175655),.UNSPECIFIED.,.F.,.F.,
(4,2,2,2,2,2,2,2,2,2,2,2,2,2,2,2,2,2,2,2,2,2,4),(-15.8342194625049,-15.6977127043355,
-15.5773804110908,-15.3642468765764,-15.09931918308,-14.9294000167655,-14.7206652063124,
-14.486715371738,-14.3080704995446,-14.2094573881803,-13.9895882638501,
-13.8413026265143,-13.5246285120497,-13.2854001451967,-13.0588788494565,
-12.8566029430652,-12.6243630241051,-12.4564523076755,-12.2472506528897,
-12.0126776113488,-11.8406732046349,-11.6300509401454,-11.5541786166363),
 .UNSPECIFIED.);
#30214=B_SPLINE_CURVE_WITH_KNOTS('',3,(#175661,#175662,#175663,#175664,
#175665,#175666,#175667,#175668,#175669,#175670,#175671,#175672,#175673,
#175674,#175675,#175676,#175677,#175678,#175679,#175680,#175681,#175682,
#175683,#175684,#175685,#175686,#175687,#175688,#175689,#175690,#175691,
#175692),.UNSPECIFIED.,.F.,.F.,(4,2,2,2,2,2,2,2,2,2,2,2,2,2,2,4),(-4.28434131557169,
-4.09277740304251,-3.61917124043791,-3.44763569882389,-3.18732168462545,
-2.69760137878484,-2.47655354496899,-2.23097942144452,-1.99516744125324,
-1.79887978653663,-1.30903271099472,-1.1395483035054,-0.874036589805563,
-0.50662520338749,-0.275259912498234,-6.25946676278E-5),.UNSPECIFIED.);
#30215=B_SPLINE_CURVE_WITH_KNOTS('',3,(#175693,#175694,#175695,#175696,
#175697,#175698,#175699,#175700,#175701,#175702,#175703,#175704,#175705,
#175706,#175707,#175708,#175709,#175710,#175711,#175712,#175713,#175714,
#175715,#175716,#175717,#175718,#175719,#175720,#175721,#175722,#175723,
#175724,#175725,#175726,#175727,#175728,#175729,#175730),.UNSPECIFIED.,
 .F.,.F.,(4,2,2,2,2,2,2,2,2,2,2,2,2,2,2,2,2,2,4),(-22.6845908560294,-22.56357533318,
-22.4433332062268,-22.2076672947508,-22.0518282119736,-21.8491460788328,
-21.6061246150425,-21.488733935936,-21.2790179348323,-21.0357861008617,
-20.917655920078,-20.6743899393749,-20.5046475501176,-20.261470665812,-20.1147815859423,
-19.8716721347519,-19.7302899931803,-19.4872020908436,-19.2607415147143),
 .UNSPECIFIED.);
#30216=B_SPLINE_CURVE_WITH_KNOTS('',3,(#175731,#175732,#175733,#175734,
#175735,#175736,#175737,#175738,#175739,#175740,#175741,#175742,#175743,
#175744,#175745,#175746,#175747,#175748,#175749,#175750,#175751,#175752,
#175753,#175754,#175755,#175756,#175757,#175758,#175759,#175760,#175761,
#175762,#175763,#175764,#175765,#175766,#175767,#175768,#175769,#175770,
#175771,#175772,#175773,#175774,#175775,#175776,#175777,#175778,#175779,
#175780,#175781,#175782,#175783,#175784,#175785,#175786,#175787,#175788,
#175789,#175790,#175791,#175792,#175793,#175794,#175795,#175796,#175797,
#175798,#175799,#175800,#175801,#175802,#175803,#175804,#175805,#175806,
#175807,#175808,#175809,#175810,#175811,#175812),.UNSPECIFIED.,.F.,.F.,
(4,2,2,2,2,2,2,2,2,2,2,2,2,2,2,2,2,2,2,2,2,2,2,2,2,2,2,2,2,2,2,2,2,2,2,
2,2,2,2,2,4),(-11.5541786166363,-11.3950854156062,-11.2096775121344,-11.0043226829807,
-10.8500288973595,-10.6890213298879,-10.5864939249941,-10.3829386240887,
-10.2358179688788,-10.0716509837532,-9.89159841404206,-9.65709860754171,
-9.50826552548869,-9.38376704948463,-9.17323910044889,-8.94728758877424,
-8.72851366280805,-8.52549599229854,-8.29298891156297,-8.12584946479877,
-7.91594018917861,-7.70031586754289,-7.49769126456504,-7.18422374900822,
-6.97475394587394,-6.80146565745864,-6.56728466583071,-6.35934118054618,
-6.18839009038117,-5.9560804906308,-5.75359007713891,-5.52928078721657,
-5.31018117475273,-5.10068372756452,-4.93164167344563,-4.70453244843515,
-4.49159153330761,-4.34455457508952,-4.20783168701383,-3.97233424177691,
-3.85128105488488),.UNSPECIFIED.);
#30217=B_SPLINE_CURVE_WITH_KNOTS('',3,(#175819,#175820,#175821,#175822,
#175823,#175824,#175825,#175826),.UNSPECIFIED.,.F.,.F.,(4,2,2,4),(-12.5667441018124,
-12.3948644827148,-12.2315918217553,-11.9950102098449),.UNSPECIFIED.);
#30218=B_SPLINE_CURVE_WITH_KNOTS('',3,(#175834,#175835,#175836,#175837,
#175838,#175839,#175840,#175841,#175842,#175843,#175844,#175845,#175846,
#175847,#175848,#175849,#175850,#175851,#175852,#175853,#175854,#175855,
#175856,#175857,#175858,#175859,#175860,#175861,#175862,#175863,#175864,
#175865,#175866,#175867,#175868,#175869,#175870,#175871,#175872,#175873,
#175874,#175875,#175876,#175877,#175878,#175879,#175880,#175881,#175882,
#175883,#175884,#175885,#175886,#175887,#175888,#175889,#175890,#175891,
#175892,#175893),.UNSPECIFIED.,.F.,.F.,(4,2,2,2,2,2,2,2,2,2,2,2,2,2,2,2,
2,2,2,2,2,2,2,2,2,2,2,2,2,4),(-11.9950102098449,-11.9174453923583,-11.7508299267779,
-11.3974252645589,-11.14570121458,-10.9105100626791,-10.6766139949695,-10.1854286940875,
-10.0159923559882,-9.84730729538404,-9.50844590120323,-9.01935539408419,
-8.86994604666456,-8.62945896795752,-8.37107887875824,-7.87982978978599,
-7.6994348954704,-7.35438717316835,-7.09964540659805,-6.78873130182614,
-6.5189806395568,-6.28324949672827,-6.04828226034808,-5.82497750860391,
-5.35946271865167,-5.19008739133567,-4.91855369030482,-4.5495935508187,
-4.31459941285212,-4.28434131557169),.UNSPECIFIED.);
#30219=B_SPLINE_CURVE_WITH_KNOTS('',3,(#175895,#175896,#175897,#175898,
#175899,#175900,#175901,#175902,#175903,#175904,#175905,#175906,#175907,
#175908,#175909,#175910,#175911,#175912,#175913,#175914,#175915,#175916,
#175917,#175918,#175919,#175920,#175921,#175922,#175923,#175924,#175925,
#175926,#175927,#175928,#175929,#175930,#175931,#175932,#175933,#175934,
#175935,#175936,#175937,#175938,#175939,#175940,#175941,#175942),
 .UNSPECIFIED.,.F.,.F.,(4,2,2,2,2,2,2,2,2,2,2,2,2,2,2,2,2,2,2,2,2,2,2,4),
(-3.85128105488488,-3.79021381602281,-3.62604742867229,-3.47891163529719,
-3.27535403509337,-3.17283585566507,-3.01183230825087,-2.85751291683218,
-2.65215108768188,-2.46499690997713,-2.22947181361531,-2.01689531266768,
-1.86831310131458,-1.73170963183605,-1.50097799364476,-1.31366423476826,
-1.14712140893274,-1.00476385207455,-0.802106911930033,-0.57926903885878,
-0.353938107479744,-0.181471048650026,-0.108959320929375,-1.00000000013978E-6),
 .UNSPECIFIED.);
#30220=B_SPLINE_CURVE_WITH_KNOTS('',3,(#175944,#175945,#175946,#175947,
#175948,#175949,#175950,#175951,#175952,#175953,#175954,#175955,#175956,
#175957,#175958,#175959,#175960,#175961),.UNSPECIFIED.,.F.,.F.,(4,2,2,2,
2,2,2,2,4),(-1.56872780698315,-1.4440306336282,-1.12597350523365,-0.975660481160978,
-0.784391357145661,-0.591408591724091,-0.401362373433468,-0.0876302679175364,
-4.3266993764275E-5),.UNSPECIFIED.);
#30221=B_SPLINE_CURVE_WITH_KNOTS('',3,(#175964,#175965,#175966,#175967,
#175968,#175969,#175970,#175971,#175972,#175973,#175974,#175975,#175976,
#175977,#175978,#175979,#175980,#175981,#175982,#175983,#175984,#175985,
#175986,#175987,#175988,#175989,#175990,#175991,#175992,#175993,#175994,
#175995,#175996,#175997,#175998,#175999,#176000,#176001,#176002,#176003,
#176004,#176005,#176006,#176007,#176008,#176009,#176010,#176011,#176012,
#176013,#176014,#176015,#176016,#176017,#176018,#176019,#176020,#176021,
#176022,#176023,#176024,#176025,#176026,#176027,#176028,#176029,#176030,
#176031,#176032,#176033,#176034,#176035,#176036,#176037,#176038,#176039,
#176040,#176041,#176042,#176043,#176044,#176045),.UNSPECIFIED.,.F.,.F.,
(4,2,2,2,2,2,2,2,2,2,2,2,2,2,2,2,2,2,2,2,2,2,2,2,2,2,2,2,2,2,2,2,2,2,2,
2,2,2,2,2,4),(9.99999996770772E-7,0.216096709673407,0.429552939762468,0.571271952022262,
0.755836106170213,1.01820485320077,1.21703629447801,1.44716350412417,1.64325668657453,
1.84994165032243,2.04724835673668,2.22529775200564,2.48438121460585,2.63947162473055,
2.89870671827172,3.04835514620737,3.17388312085714,3.45727180697445,3.6684611276535,
3.85144843842677,4.11123903335375,4.36451230583652,4.61753038314871,4.86090458780383,
5.0908854501483,5.31127319319499,5.50839114872044,5.73729202430653,5.86251219157969,
6.12172543232554,6.3278151707646,6.45314931926401,6.71822856253032,6.97657492212759,
7.1060792710105,7.23313600922317,7.48178953492956,7.74046648497742,7.86739147753993,
8.12610096263681,8.20592890423442),.UNSPECIFIED.);
#30222=B_SPLINE_CURVE_WITH_KNOTS('',3,(#176046,#176047,#176048,#176049,
#176050,#176051,#176052,#176053,#176054,#176055,#176056,#176057,#176058,
#176059,#176060,#176061,#176062,#176063,#176064,#176065,#176066,#176067,
#176068,#176069,#176070,#176071,#176072,#176073,#176074,#176075,#176076,
#176077,#176078,#176079,#176080,#176081,#176082,#176083,#176084,#176085,
#176086,#176087,#176088,#176089,#176090,#176091,#176092,#176093,#176094,
#176095,#176096,#176097,#176098,#176099,#176100,#176101,#176102,#176103,
#176104,#176105,#176106,#176107,#176108,#176109,#176110,#176111,#176112,
#176113,#176114,#176115,#176116,#176117,#176118,#176119,#176120,#176121,
#176122,#176123,#176124,#176125,#176126,#176127,#176128,#176129),
 .UNSPECIFIED.,.F.,.F.,(4,2,2,2,2,2,2,2,2,2,2,2,2,2,2,2,2,2,2,2,2,2,2,2,
2,2,2,2,2,2,2,2,2,2,2,2,2,2,2,2,2,4),(15.9564624294639,15.9706790833614,
16.2291128145473,16.3883470222381,16.6013963628145,16.8272802503908,17.0859867465911,
17.2118389039018,17.4705312770014,17.6971467409743,17.8221896050243,18.0699274003179,
18.3291189666377,18.4560722250234,18.677144832226,18.8380375686119,19.0633228435152,
19.2690179009758,19.4884396484015,19.6419673542867,19.9017917209588,20.0763305486744,
20.2904388264911,20.5396306120903,20.6645338341068,20.9229592234423,21.1820326854096,
21.3095426955538,21.5133942780727,21.7723438890345,21.8970975613754,22.1291363525681,
22.3287446861619,22.5911219866707,22.7158489770712,22.9425177394998,23.1403660822531,
23.3884095378057,23.5767981126961,23.7214216510108,23.9407025478493,24.1621317186099),
 .UNSPECIFIED.);
#30223=B_SPLINE_CURVE_WITH_KNOTS('',3,(#176133,#176134,#176135,#176136,
#176137,#176138,#176139,#176140,#176141,#176142,#176143,#176144,#176145,
#176146,#176147,#176148),.UNSPECIFIED.,.F.,.F.,(4,2,2,2,2,2,2,4),(-5.34036980583782,
-5.1030202497345,-4.85331064879726,-4.37225443792772,-3.88453013968305,
-3.63186010168836,-3.38655743616596,-3.33078402932135),.UNSPECIFIED.);
#30224=B_SPLINE_CURVE_WITH_KNOTS('',3,(#176152,#176153,#176154,#176155,
#176156,#176157,#176158,#176159,#176160,#176161,#176162,#176163,#176164,
#176165,#176166,#176167,#176168,#176169,#176170,#176171,#176172,#176173),
 .UNSPECIFIED.,.F.,.F.,(4,2,2,2,2,2,2,2,2,2,4),(-3.33078402932135,-3.1457787811171,
-2.66969336894367,-2.42517438029747,-2.18777430400242,-1.69235110047304,
-1.45012215012257,-1.21210349141667,-0.975414798511056,-0.48839821058214,
-4.75981067057991E-5),.UNSPECIFIED.);
#30225=B_SPLINE_CURVE_WITH_KNOTS('',3,(#176175,#176176,#176177,#176178,
#176179,#176180,#176181,#176182,#176183,#176184,#176185,#176186,#176187,
#176188,#176189,#176190,#176191,#176192,#176193,#176194,#176195,#176196,
#176197,#176198,#176199,#176200,#176201,#176202,#176203,#176204,#176205,
#176206,#176207,#176208,#176209,#176210,#176211,#176212,#176213,#176214,
#176215,#176216,#176217,#176218,#176219,#176220,#176221,#176222,#176223,
#176224,#176225,#176226,#176227,#176228,#176229,#176230,#176231,#176232,
#176233,#176234,#176235,#176236,#176237,#176238,#176239,#176240,#176241),
 .UNSPECIFIED.,.F.,.F.,(4,3,3,3,3,3,3,3,3,3,3,3,3,3,3,3,3,3,3,3,3,3,4),
(0.,0.0532797188798471,0.106117363864542,0.124999999999999,0.176897081798013,
0.229324525544414,0.249999999999997,0.30186133202288,0.353569755832338,
0.405192326669397,0.456691995603922,0.499999999999998,0.55129671836749,
0.60294632648651,0.65479461109988,0.70698774344366,0.749999999999999,0.803309497919045,
0.856238158519042,0.875,0.929869764524203,0.984191399199238,0.999999665677159),
 .UNSPECIFIED.);
#30226=B_SPLINE_CURVE_WITH_KNOTS('',3,(#176243,#176244,#176245,#176246,
#176247,#176248,#176249,#176250,#176251,#176252),.UNSPECIFIED.,.F.,.F.,
(4,2,2,2,4),(-1.36676107014523,-1.02924695186398,-0.680886324591757,-0.344531536147177,
-6.48039110289688E-5),.UNSPECIFIED.);
#30227=B_SPLINE_CURVE_WITH_KNOTS('',3,(#176253,#176254,#176255,#176256),
 .UNSPECIFIED.,.F.,.F.,(4,4),(-0.000734763449220644,0.),.UNSPECIFIED.);
#30228=B_SPLINE_CURVE_WITH_KNOTS('',3,(#176506,#176507,#176508,#176509,
#176510,#176511,#176512,#176513,#176514,#176515,#176516,#176517,#176518,
#176519,#176520,#176521,#176522,#176523,#176524,#176525,#176526,#176527,
#176528,#176529,#176530,#176531,#176532,#176533,#176534,#176535,#176536,
#176537,#176538,#176539,#176540,#176541,#176542,#176543,#176544,#176545,
#176546,#176547,#176548,#176549,#176550,#176551,#176552,#176553,#176554,
#176555,#176556,#176557,#176558,#176559,#176560,#176561,#176562,#176563,
#176564,#176565,#176566,#176567,#176568,#176569,#176570,#176571,#176572,
#176573,#176574,#176575,#176576,#176577,#176578,#176579,#176580,#176581,
#176582,#176583,#176584,#176585,#176586,#176587,#176588,#176589,#176590,
#176591,#176592,#176593,#176594,#176595,#176596,#176597,#176598,#176599,
#176600,#176601,#176602,#176603,#176604,#176605,#176606,#176607,#176608,
#176609,#176610,#176611,#176612,#176613,#176614,#176615,#176616,#176617,
#176618,#176619,#176620,#176621,#176622,#176623,#176624,#176625,#176626,
#176627,#176628,#176629,#176630,#176631,#176632,#176633,#176634,#176635,
#176636,#176637,#176638,#176639,#176640,#176641,#176642,#176643,#176644,
#176645,#176646,#176647,#176648,#176649,#176650,#176651,#176652,#176653,
#176654,#176655,#176656,#176657,#176658,#176659,#176660,#176661,#176662,
#176663,#176664,#176665,#176666,#176667,#176668,#176669,#176670,#176671,
#176672,#176673,#176674,#176675,#176676,#176677,#176678,#176679,#176680,
#176681,#176682,#176683,#176684,#176685,#176686,#176687,#176688,#176689,
#176690,#176691,#176692,#176693,#176694,#176695,#176696,#176697,#176698,
#176699,#176700,#176701,#176702,#176703,#176704,#176705,#176706,#176707,
#176708,#176709,#176710,#176711,#176712,#176713,#176714,#176715,#176716,
#176717,#176718,#176719,#176720,#176721,#176722,#176723,#176724,#176725,
#176726,#176727,#176728,#176729,#176730,#176731,#176732,#176733,#176734,
#176735,#176736,#176737,#176738,#176739,#176740,#176741,#176742,#176743,
#176744,#176745,#176746,#176747,#176748,#176749,#176750,#176751,#176752,
#176753,#176754,#176755,#176756,#176757,#176758,#176759,#176760,#176761,
#176762,#176763,#176764,#176765,#176766,#176767,#176768,#176769,#176770,
#176771),.UNSPECIFIED.,.F.,.F.,(4,2,2,2,2,2,2,2,2,2,2,2,2,2,2,2,2,2,2,2,
2,2,2,2,2,2,2,2,2,2,2,2,2,2,2,2,2,2,2,2,2,2,2,2,2,2,2,2,2,2,2,2,2,2,2,2,
2,2,2,2,2,2,2,2,2,2,2,2,2,2,2,2,2,2,2,2,2,2,2,2,2,2,2,2,2,2,2,2,2,2,2,2,
2,2,2,2,2,2,2,2,2,2,2,2,2,2,2,2,2,2,2,2,2,2,2,2,2,2,2,2,2,2,2,2,2,2,2,2,
2,2,2,2,4),(0.00790828593609008,0.135265930619079,0.267467598036355,0.533750941535481,
0.880175746938389,1.1338405443315,1.41070844372411,1.59304779965695,1.75172475124652,
1.94683177568559,2.11230163182156,2.21836502601455,2.42774980582893,2.62554209451856,
2.76879627869621,2.84874851608012,2.95782638710911,3.1420718245399,3.25663249533483,
3.37303209236669,3.45626245649945,3.52892154030204,3.68573723948832,3.80006718543718,
3.88555502975854,4.0320423160462,4.10567934099106,4.17075031359099,4.33697733739522,
4.47525084585826,4.54230650264742,4.69174783611453,4.75810010013034,4.81934275757705,
4.98087758791925,5.06503448417813,5.13211067183557,5.30211215786814,5.38411998545328,
5.44913118286113,5.62478643836323,5.6979080046166,5.76285686104845,5.91135455861418,
6.04924818147376,6.11297581444621,6.23609931889428,6.31387423831546,6.38379383181836,
6.5431982006822,6.65173531534229,6.73360986229017,6.84907769003456,6.96565700724283,
7.06231030062707,7.25738516515829,7.36934772486594,7.49480537614529,7.61574046453119,
7.85193160654754,7.97320619022983,8.08119356140715,8.19959932847115,8.5129309706179,
8.65863771376222,8.89993699829434,9.15208629185396,9.39091843112858,9.89069339159353,
10.1407981290889,10.5878862308056,10.6956897527359,10.9247151895919,11.1721558027748,
11.3026325812458,11.4126909898134,11.5387554878034,11.7749564773706,11.8944454341237,
12.0206020487927,12.1515122339321,12.3960074971869,12.4881436837981,12.6185243384004,
12.6893649949368,12.8337678291243,13.000390380818,13.0719084854457,13.1514103473186,
13.29001535684,13.3604822047163,13.4504758627378,13.6181390237592,13.6835566992388,
13.7534189922822,13.9354044526173,14.0011047363716,14.0851743832152,14.2450851183931,
14.3093195873102,14.3835274618411,14.5778616591905,14.6415990299127,14.7210498163087,
14.8716723114075,14.9401038812815,15.0236827439956,15.2210626466111,15.2872680425288,
15.3680469481223,15.5054195894244,15.5905449268311,15.7067042853767,15.8567162573542,
15.9290186069713,16.035971248706,16.1380071526865,16.2541495814732,16.4512230290027,
16.5501048959706,16.6242393523664,16.6962956772534,16.8009353513907,16.9202921968447,
17.1807747200293,17.2823328953094,17.4399142909722,17.6184675397991,17.8672454811379,
17.9911585604127,18.2371160348155,18.5095082696298,18.7892894936131),
 .UNSPECIFIED.);
#30229=B_SPLINE_CURVE_WITH_KNOTS('',3,(#176913,#176914,#176915,#176916,
#176917,#176918,#176919,#176920,#176921,#176922,#176923,#176924,#176925,
#176926,#176927,#176928,#176929,#176930,#176931,#176932,#176933,#176934,
#176935,#176936,#176937,#176938,#176939,#176940,#176941,#176942,#176943,
#176944,#176945,#176946,#176947,#176948,#176949,#176950,#176951,#176952,
#176953,#176954,#176955,#176956,#176957,#176958,#176959,#176960,#176961,
#176962,#176963,#176964,#176965,#176966,#176967,#176968,#176969,#176970,
#176971,#176972,#176973,#176974,#176975,#176976,#176977,#176978,#176979,
#176980,#176981,#176982,#176983,#176984,#176985,#176986,#176987,#176988,
#176989,#176990,#176991,#176992,#176993,#176994),.UNSPECIFIED.,.F.,.F.,
(4,2,2,2,2,2,2,2,2,2,2,2,2,2,2,2,2,2,2,2,2,2,2,2,2,2,2,2,2,2,2,2,2,2,2,
2,2,2,2,2,4),(-14.2732703759233,-13.8912273375714,-13.6142499111935,-13.3975932237184,
-13.1227155432504,-12.7070233843852,-12.382403721359,-12.1293949736052,
-11.8703642014978,-11.5353850377401,-11.1414389161118,-10.8461410004745,
-10.5760851451527,-10.2292125849178,-9.73704557043714,-9.39335342119085,
-9.12378600305438,-8.81489519476552,-8.39716574474396,-8.04541518664136,
-7.7772102046378,-7.50917494412834,-7.15370825667384,-6.69461619344525,
-6.35436303694603,-6.06376512695785,-5.6829615871504,-5.09892163725548,
-4.68369409177525,-4.3593566671839,-4.01204603447841,-3.53687730817834,
-3.08826224434253,-2.75857559248875,-2.45520533882891,-2.06641699456192,
-1.51781117594086,-1.13911402161876,-0.846466340154513,-0.481778164862169,
-7.79037809214993E-5),.UNSPECIFIED.);
#30230=B_SPLINE_CURVE_WITH_KNOTS('',3,(#177263,#177264,#177265,#177266,
#177267,#177268),.UNSPECIFIED.,.F.,.F.,(4,2,4),(-0.0902565459305608,-0.0451906733529908,
-0.000194550672436811),.UNSPECIFIED.);
#30231=B_SPLINE_CURVE_WITH_KNOTS('',3,(#177290,#177291,#177292,#177293,
#177294,#177295,#177296,#177297,#177298,#177299,#177300,#177301,#177302,
#177303,#177304,#177305,#177306,#177307,#177308,#177309,#177310,#177311,
#177312,#177313,#177314,#177315,#177316,#177317,#177318,#177319,#177320,
#177321,#177322,#177323,#177324,#177325,#177326,#177327,#177328,#177329,
#177330,#177331,#177332,#177333,#177334,#177335,#177336,#177337,#177338,
#177339,#177340,#177341,#177342,#177343,#177344,#177345,#177346,#177347),
 .UNSPECIFIED.,.F.,.F.,(4,3,3,3,3,3,3,3,3,3,3,3,3,3,3,3,3,3,3,4),(-1.28896142245236,
-1.09309231307544,-1.04016081898322,-0.9801834909399,-0.885023600728055,
-0.791562904179352,-0.670254571060442,-0.644748735287768,-0.634093103877705,
-0.626279232157149,-0.469588976340557,-0.352102611119503,-0.310009489205423,
-0.249406568727739,-0.188707985006066,-0.17575239527642,-0.142257802210763,
-0.0813352071442708,-0.0211767799228357,-1.50340976189325E-6),
 .UNSPECIFIED.);
#30232=B_SPLINE_CURVE_WITH_KNOTS('',3,(#177372,#177373,#177374,#177375,
#177376,#177377,#177378,#177379,#177380,#177381,#177382,#177383,#177384,
#177385,#177386,#177387,#177388,#177389,#177390,#177391,#177392,#177393,
#177394,#177395,#177396,#177397,#177398,#177399,#177400,#177401,#177402,
#177403,#177404,#177405,#177406,#177407,#177408,#177409,#177410,#177411,
#177412,#177413,#177414,#177415,#177416,#177417,#177418,#177419,#177420,
#177421,#177422,#177423,#177424,#177425,#177426,#177427,#177428,#177429),
 .UNSPECIFIED.,.F.,.F.,(4,3,3,3,3,3,3,3,3,3,3,3,3,3,3,3,3,3,3,4),(0.000196331256316104,
0.195854367373606,0.245817836587432,0.308742496769627,0.403496982747047,
0.491306783782293,0.608890768308108,0.644062191156899,0.654689003664205,
0.654735110821007,0.813710421230246,0.932829188307881,0.979410739453054,
1.03972898458091,1.1001348124034,1.11172797209159,1.14748205288158,1.20898204679902,
1.26971077107191,1.29001475424264),.UNSPECIFIED.);
#30233=B_SPLINE_CURVE_WITH_KNOTS('',3,(#177450,#177451,#177452,#177453,
#177454,#177455),.UNSPECIFIED.,.F.,.F.,(4,2,4),(-0.0900560505430899,-0.0451018402846952,
-1.01924371517976E-5),.UNSPECIFIED.);
#31249=CIRCLE('',#80672,12.25);
#31250=CIRCLE('',#80677,12.25);
#31251=CIRCLE('',#80679,10.5);
#31252=CIRCLE('',#80680,10.5);
#31253=CIRCLE('',#80682,12.25);
#31254=CIRCLE('',#80685,13.25000025523);
#31255=CIRCLE('',#80687,16.);
#31256=CIRCLE('',#80688,16.);
#31257=CIRCLE('',#80689,16.);
#31258=CIRCLE('',#80690,16.);
#31259=CIRCLE('',#80691,16.);
#31260=CIRCLE('',#80692,14.);
#31261=CIRCLE('',#80693,16.);
#31262=CIRCLE('',#80694,16.);
#31263=CIRCLE('',#80696,16.);
#31264=CIRCLE('',#80697,16.);
#31265=CIRCLE('',#80698,16.);
#31266=CIRCLE('',#80699,16.);
#31267=CIRCLE('',#80700,16.);
#31268=CIRCLE('',#80701,14.);
#31269=CIRCLE('',#80702,16.);
#31270=CIRCLE('',#80703,16.);
#34765=VERTEX_POINT('',#174767);
#34766=VERTEX_POINT('',#174768);
#34767=VERTEX_POINT('',#174770);
#34768=VERTEX_POINT('',#174811);
#34769=VERTEX_POINT('',#174846);
#34770=VERTEX_POINT('',#174925);
#34771=VERTEX_POINT('',#174926);
#34772=VERTEX_POINT('',#175091);
#34773=VERTEX_POINT('',#175092);
#34774=VERTEX_POINT('',#175094);
#34775=VERTEX_POINT('',#175105);
#34776=VERTEX_POINT('',#175121);
#34777=VERTEX_POINT('',#175122);
#34778=VERTEX_POINT('',#175124);
#34779=VERTEX_POINT('',#175165);
#34780=VERTEX_POINT('',#175176);
#34781=VERTEX_POINT('',#175187);
#34782=VERTEX_POINT('',#175189);
#34783=VERTEX_POINT('',#175200);
#34784=VERTEX_POINT('',#175211);
#34785=VERTEX_POINT('',#175252);
#34786=VERTEX_POINT('',#175332);
#34787=VERTEX_POINT('',#175333);
#34788=VERTEX_POINT('',#175492);
#34789=VERTEX_POINT('',#175493);
#34790=VERTEX_POINT('',#175577);
#34791=VERTEX_POINT('',#175657);
#34792=VERTEX_POINT('',#175658);
#34793=VERTEX_POINT('',#175660);
#34794=VERTEX_POINT('',#175814);
#34795=VERTEX_POINT('',#175815);
#34796=VERTEX_POINT('',#175817);
#34797=VERTEX_POINT('',#175828);
#34798=VERTEX_POINT('',#175830);
#34799=VERTEX_POINT('',#175894);
#34800=VERTEX_POINT('',#175943);
#34801=VERTEX_POINT('',#176131);
#34802=VERTEX_POINT('',#176132);
#34803=VERTEX_POINT('',#176149);
#34804=VERTEX_POINT('',#176174);
#34805=VERTEX_POINT('',#176242);
#34806=VERTEX_POINT('',#176258);
#34807=VERTEX_POINT('',#176259);
#34808=VERTEX_POINT('',#176263);
#34809=VERTEX_POINT('',#176265);
#34810=VERTEX_POINT('',#176269);
#34811=VERTEX_POINT('',#176271);
#34812=VERTEX_POINT('',#176275);
#34813=VERTEX_POINT('',#176277);
#34814=VERTEX_POINT('',#176281);
#34815=VERTEX_POINT('',#176283);
#34816=VERTEX_POINT('',#176287);
#34817=VERTEX_POINT('',#176289);
#34818=VERTEX_POINT('',#176292);
#34819=VERTEX_POINT('',#176294);
#34820=VERTEX_POINT('',#176300);
#34821=VERTEX_POINT('',#176301);
#34822=VERTEX_POINT('',#176305);
#34823=VERTEX_POINT('',#176307);
#34824=VERTEX_POINT('',#176311);
#34825=VERTEX_POINT('',#176313);
#34826=VERTEX_POINT('',#176317);
#34827=VERTEX_POINT('',#176319);
#34828=VERTEX_POINT('',#176323);
#34829=VERTEX_POINT('',#176325);
#34830=VERTEX_POINT('',#176329);
#34831=VERTEX_POINT('',#176331);
#34832=VERTEX_POINT('',#176334);
#34833=VERTEX_POINT('',#176336);
#43020=EDGE_CURVE('',#34765,#34766,#3116,.T.);
#43021=EDGE_CURVE('',#34767,#34766,#30194,.F.);
#43022=EDGE_CURVE('',#34768,#34767,#30195,.T.);
#43023=EDGE_CURVE('',#34769,#34768,#3117,.T.);
#43024=EDGE_CURVE('',#34769,#34765,#30196,.T.);
#43025=EDGE_CURVE('',#34770,#34771,#3118,.T.);
#43026=EDGE_CURVE('',#34766,#34771,#30197,.F.);
#43027=EDGE_CURVE('',#34765,#34770,#30198,.T.);
#43028=EDGE_CURVE('',#34772,#34773,#3119,.T.);
#43029=EDGE_CURVE('',#34772,#34774,#30199,.T.);
#43030=EDGE_CURVE('',#34774,#34775,#30200,.T.);
#43031=EDGE_CURVE('',#34773,#34775,#30201,.T.);
#43032=EDGE_CURVE('',#34776,#34777,#3120,.T.);
#43033=EDGE_CURVE('',#34777,#34778,#30202,.T.);
#43034=EDGE_CURVE('',#34778,#34779,#30203,.T.);
#43035=EDGE_CURVE('',#34779,#34780,#30204,.T.);
#43036=EDGE_CURVE('',#34780,#34781,#3121,.T.);
#43037=EDGE_CURVE('',#34781,#34782,#30205,.T.);
#43038=EDGE_CURVE('',#34782,#34783,#30206,.T.);
#43039=EDGE_CURVE('',#34783,#34784,#30207,.T.);
#43040=EDGE_CURVE('',#34784,#34785,#3122,.T.);
#43041=EDGE_CURVE('',#34785,#34785,#31249,.T.);
#43042=EDGE_CURVE('',#34784,#34776,#30208,.T.);
#43043=EDGE_CURVE('',#34786,#34787,#3123,.T.);
#43044=EDGE_CURVE('',#34787,#34777,#30209,.T.);
#43045=EDGE_CURVE('',#34776,#34786,#30210,.T.);
#43046=EDGE_CURVE('',#34788,#34789,#3124,.T.);
#43047=EDGE_CURVE('',#34789,#34787,#30211,.T.);
#43048=EDGE_CURVE('',#34786,#34790,#30212,.T.);
#43049=EDGE_CURVE('',#34790,#34788,#30213,.T.);
#43050=EDGE_CURVE('',#34791,#34792,#3125,.T.);
#43051=EDGE_CURVE('',#34793,#34792,#30214,.F.);
#43052=EDGE_CURVE('',#34793,#34789,#30215,.T.);
#43053=EDGE_CURVE('',#34788,#34791,#30216,.T.);
#43054=EDGE_CURVE('',#34794,#34795,#3126,.T.);
#43055=EDGE_CURVE('',#34794,#34796,#31250,.T.);
#43056=EDGE_CURVE('',#34795,#34796,#30217,.F.);
#43057=EDGE_CURVE('',#34797,#34797,#31251,.T.);
#43058=EDGE_CURVE('',#34797,#34798,#3127,.T.);
#43059=EDGE_CURVE('',#34798,#34798,#31252,.T.);
#43060=EDGE_CURVE('',#34792,#34795,#30218,.F.);
#43061=EDGE_CURVE('',#34791,#34799,#30219,.T.);
#43062=EDGE_CURVE('',#34799,#34800,#30220,.T.);
#43063=EDGE_CURVE('',#34800,#34794,#31253,.T.);
#43064=EDGE_CURVE('',#34771,#34773,#30221,.F.);
#43065=EDGE_CURVE('',#34770,#34772,#30222,.T.);
#43066=EDGE_CURVE('',#34801,#34802,#30223,.T.);
#43067=EDGE_CURVE('',#34802,#34803,#3128,.T.);
#43068=EDGE_CURVE('',#34803,#34803,#31254,.T.);
#43069=EDGE_CURVE('',#34802,#34796,#30224,.T.);
#43070=EDGE_CURVE('',#34804,#34800,#30225,.T.);
#43071=EDGE_CURVE('',#34804,#34805,#30226,.T.);
#43072=EDGE_CURVE('',#34805,#34801,#30227,.T.);
#43073=EDGE_CURVE('',#34806,#34807,#1776,.T.);
#43074=EDGE_CURVE('',#34806,#34808,#31255,.T.);
#43075=EDGE_CURVE('',#34809,#34808,#1777,.T.);
#43076=EDGE_CURVE('',#34809,#34810,#31256,.T.);
#43077=EDGE_CURVE('',#34811,#34810,#1778,.T.);
#43078=EDGE_CURVE('',#34811,#34812,#31257,.T.);
#43079=EDGE_CURVE('',#34813,#34812,#1779,.F.);
#43080=EDGE_CURVE('',#34814,#34813,#31258,.T.);
#43081=EDGE_CURVE('',#34815,#34814,#1780,.T.);
#43082=EDGE_CURVE('',#34816,#34815,#31259,.T.);
#43083=EDGE_CURVE('',#34816,#34817,#3129,.T.);
#43084=EDGE_CURVE('',#34817,#34817,#31260,.T.);
#43085=EDGE_CURVE('',#34818,#34816,#31261,.T.);
#43086=EDGE_CURVE('',#34819,#34818,#1781,.T.);
#43087=EDGE_CURVE('',#34807,#34819,#31262,.T.);
#43088=EDGE_CURVE('',#34820,#34821,#1782,.F.);
#43089=EDGE_CURVE('',#34821,#34822,#31263,.T.);
#43090=EDGE_CURVE('',#34822,#34823,#1783,.T.);
#43091=EDGE_CURVE('',#34823,#34824,#31264,.T.);
#43092=EDGE_CURVE('',#34824,#34825,#1784,.T.);
#43093=EDGE_CURVE('',#34825,#34826,#31265,.T.);
#43094=EDGE_CURVE('',#34826,#34827,#1785,.T.);
#43095=EDGE_CURVE('',#34828,#34827,#31266,.T.);
#43096=EDGE_CURVE('',#34828,#34829,#1786,.T.);
#43097=EDGE_CURVE('',#34830,#34829,#31267,.T.);
#43098=EDGE_CURVE('',#34830,#34831,#3130,.T.);
#43099=EDGE_CURVE('',#34831,#34831,#31268,.T.);
#43100=EDGE_CURVE('',#34832,#34830,#31269,.T.);
#43101=EDGE_CURVE('',#34832,#34833,#1787,.T.);
#43102=EDGE_CURVE('',#34820,#34833,#31270,.T.);
#43103=EDGE_CURVE('',#34809,#34832,#3131,.T.);
#43104=EDGE_CURVE('',#34810,#34829,#3132,.T.);
#43105=EDGE_CURVE('',#34818,#34823,#3133,.T.);
#43106=EDGE_CURVE('',#34819,#34822,#3134,.T.);
#43107=EDGE_CURVE('',#34811,#34828,#3135,.T.);
#43108=EDGE_CURVE('',#34808,#34833,#3136,.T.);
#43109=EDGE_CURVE('',#34812,#34827,#3137,.T.);
#43110=EDGE_CURVE('',#34806,#34820,#3138,.T.);
#43111=EDGE_CURVE('',#34807,#34821,#3139,.T.);
#43112=EDGE_CURVE('',#34814,#34825,#3140,.T.);
#43113=EDGE_CURVE('',#34815,#34824,#3141,.T.);
#43114=EDGE_CURVE('',#34813,#34826,#3142,.T.);
#43115=EDGE_CURVE('',#34801,#34768,#30228,.T.);
#43116=EDGE_CURVE('',#34768,#34793,#3143,.T.);
#43117=EDGE_CURVE('',#34804,#34769,#30229,.T.);
#43118=EDGE_CURVE('',#34782,#34774,#30230,.T.);
#43119=EDGE_CURVE('',#34790,#34769,#3144,.T.);
#43120=EDGE_CURVE('',#34774,#34781,#30231,.T.);
#43121=EDGE_CURVE('',#34775,#34780,#30232,.T.);
#43122=EDGE_CURVE('',#34775,#34779,#30233,.T.);
#56375=ORIENTED_EDGE('',*,*,#43020,.T.);
#56376=ORIENTED_EDGE('',*,*,#43021,.F.);
#56377=ORIENTED_EDGE('',*,*,#43022,.F.);
#56378=ORIENTED_EDGE('',*,*,#43023,.F.);
#56379=ORIENTED_EDGE('',*,*,#43024,.T.);
#56380=ORIENTED_EDGE('',*,*,#43025,.T.);
#56381=ORIENTED_EDGE('',*,*,#43026,.F.);
#56382=ORIENTED_EDGE('',*,*,#43020,.F.);
#56383=ORIENTED_EDGE('',*,*,#43027,.T.);
#56384=ORIENTED_EDGE('',*,*,#43028,.F.);
#56385=ORIENTED_EDGE('',*,*,#43029,.T.);
#56386=ORIENTED_EDGE('',*,*,#43030,.T.);
#56387=ORIENTED_EDGE('',*,*,#43031,.F.);
#56388=ORIENTED_EDGE('',*,*,#43032,.T.);
#56389=ORIENTED_EDGE('',*,*,#43033,.T.);
#56390=ORIENTED_EDGE('',*,*,#43034,.T.);
#56391=ORIENTED_EDGE('',*,*,#43035,.T.);
#56392=ORIENTED_EDGE('',*,*,#43036,.T.);
#56393=ORIENTED_EDGE('',*,*,#43037,.T.);
#56394=ORIENTED_EDGE('',*,*,#43038,.T.);
#56395=ORIENTED_EDGE('',*,*,#43039,.T.);
#56396=ORIENTED_EDGE('',*,*,#43040,.T.);
#56397=ORIENTED_EDGE('',*,*,#43041,.F.);
#56398=ORIENTED_EDGE('',*,*,#43040,.F.);
#56399=ORIENTED_EDGE('',*,*,#43042,.T.);
#56400=ORIENTED_EDGE('',*,*,#43043,.T.);
#56401=ORIENTED_EDGE('',*,*,#43044,.T.);
#56402=ORIENTED_EDGE('',*,*,#43032,.F.);
#56403=ORIENTED_EDGE('',*,*,#43045,.T.);
#56404=ORIENTED_EDGE('',*,*,#43046,.T.);
#56405=ORIENTED_EDGE('',*,*,#43047,.T.);
#56406=ORIENTED_EDGE('',*,*,#43043,.F.);
#56407=ORIENTED_EDGE('',*,*,#43048,.T.);
#56408=ORIENTED_EDGE('',*,*,#43049,.T.);
#56409=ORIENTED_EDGE('',*,*,#43050,.T.);
#56410=ORIENTED_EDGE('',*,*,#43051,.F.);
#56411=ORIENTED_EDGE('',*,*,#43052,.T.);
#56412=ORIENTED_EDGE('',*,*,#43046,.F.);
#56413=ORIENTED_EDGE('',*,*,#43053,.T.);
#56414=ORIENTED_EDGE('',*,*,#43054,.F.);
#56415=ORIENTED_EDGE('',*,*,#43055,.T.);
#56416=ORIENTED_EDGE('',*,*,#43056,.F.);
#56417=ORIENTED_EDGE('',*,*,#43057,.T.);
#56418=ORIENTED_EDGE('',*,*,#43058,.T.);
#56419=ORIENTED_EDGE('',*,*,#43059,.T.);
#56420=ORIENTED_EDGE('',*,*,#43058,.F.);
#56421=ORIENTED_EDGE('',*,*,#43054,.T.);
#56422=ORIENTED_EDGE('',*,*,#43060,.F.);
#56423=ORIENTED_EDGE('',*,*,#43050,.F.);
#56424=ORIENTED_EDGE('',*,*,#43061,.T.);
#56425=ORIENTED_EDGE('',*,*,#43062,.T.);
#56426=ORIENTED_EDGE('',*,*,#43063,.T.);
#56427=ORIENTED_EDGE('',*,*,#43028,.T.);
#56428=ORIENTED_EDGE('',*,*,#43064,.F.);
#56429=ORIENTED_EDGE('',*,*,#43025,.F.);
#56430=ORIENTED_EDGE('',*,*,#43065,.T.);
#56431=ORIENTED_EDGE('',*,*,#43066,.T.);
#56432=ORIENTED_EDGE('',*,*,#43067,.T.);
#56433=ORIENTED_EDGE('',*,*,#43068,.F.);
#56434=ORIENTED_EDGE('',*,*,#43067,.F.);
#56435=ORIENTED_EDGE('',*,*,#43069,.T.);
#56436=ORIENTED_EDGE('',*,*,#43055,.F.);
#56437=ORIENTED_EDGE('',*,*,#43063,.F.);
#56438=ORIENTED_EDGE('',*,*,#43070,.F.);
#56439=ORIENTED_EDGE('',*,*,#43071,.T.);
#56440=ORIENTED_EDGE('',*,*,#43072,.T.);
#56441=ORIENTED_EDGE('',*,*,#43073,.F.);
#56442=ORIENTED_EDGE('',*,*,#43074,.T.);
#56443=ORIENTED_EDGE('',*,*,#43075,.F.);
#56444=ORIENTED_EDGE('',*,*,#43076,.T.);
#56445=ORIENTED_EDGE('',*,*,#43077,.F.);
#56446=ORIENTED_EDGE('',*,*,#43078,.T.);
#56447=ORIENTED_EDGE('',*,*,#43079,.F.);
#56448=ORIENTED_EDGE('',*,*,#43080,.F.);
#56449=ORIENTED_EDGE('',*,*,#43081,.F.);
#56450=ORIENTED_EDGE('',*,*,#43082,.F.);
#56451=ORIENTED_EDGE('',*,*,#43083,.T.);
#56452=ORIENTED_EDGE('',*,*,#43084,.T.);
#56453=ORIENTED_EDGE('',*,*,#43083,.F.);
#56454=ORIENTED_EDGE('',*,*,#43085,.F.);
#56455=ORIENTED_EDGE('',*,*,#43086,.F.);
#56456=ORIENTED_EDGE('',*,*,#43087,.F.);
#56457=ORIENTED_EDGE('',*,*,#43088,.T.);
#56458=ORIENTED_EDGE('',*,*,#43089,.T.);
#56459=ORIENTED_EDGE('',*,*,#43090,.T.);
#56460=ORIENTED_EDGE('',*,*,#43091,.T.);
#56461=ORIENTED_EDGE('',*,*,#43092,.T.);
#56462=ORIENTED_EDGE('',*,*,#43093,.T.);
#56463=ORIENTED_EDGE('',*,*,#43094,.T.);
#56464=ORIENTED_EDGE('',*,*,#43095,.F.);
#56465=ORIENTED_EDGE('',*,*,#43096,.T.);
#56466=ORIENTED_EDGE('',*,*,#43097,.F.);
#56467=ORIENTED_EDGE('',*,*,#43098,.T.);
#56468=ORIENTED_EDGE('',*,*,#43099,.F.);
#56469=ORIENTED_EDGE('',*,*,#43098,.F.);
#56470=ORIENTED_EDGE('',*,*,#43100,.F.);
#56471=ORIENTED_EDGE('',*,*,#43101,.T.);
#56472=ORIENTED_EDGE('',*,*,#43102,.F.);
#56473=ORIENTED_EDGE('',*,*,#43076,.F.);
#56474=ORIENTED_EDGE('',*,*,#43103,.T.);
#56475=ORIENTED_EDGE('',*,*,#43100,.T.);
#56476=ORIENTED_EDGE('',*,*,#43097,.T.);
#56477=ORIENTED_EDGE('',*,*,#43104,.F.);
#56478=ORIENTED_EDGE('',*,*,#43086,.T.);
#56479=ORIENTED_EDGE('',*,*,#43105,.T.);
#56480=ORIENTED_EDGE('',*,*,#43090,.F.);
#56481=ORIENTED_EDGE('',*,*,#43106,.F.);
#56482=ORIENTED_EDGE('',*,*,#43077,.T.);
#56483=ORIENTED_EDGE('',*,*,#43104,.T.);
#56484=ORIENTED_EDGE('',*,*,#43096,.F.);
#56485=ORIENTED_EDGE('',*,*,#43107,.F.);
#56486=ORIENTED_EDGE('',*,*,#43075,.T.);
#56487=ORIENTED_EDGE('',*,*,#43108,.T.);
#56488=ORIENTED_EDGE('',*,*,#43101,.F.);
#56489=ORIENTED_EDGE('',*,*,#43103,.F.);
#56490=ORIENTED_EDGE('',*,*,#43095,.T.);
#56491=ORIENTED_EDGE('',*,*,#43109,.F.);
#56492=ORIENTED_EDGE('',*,*,#43078,.F.);
#56493=ORIENTED_EDGE('',*,*,#43107,.T.);
#56494=ORIENTED_EDGE('',*,*,#43102,.T.);
#56495=ORIENTED_EDGE('',*,*,#43108,.F.);
#56496=ORIENTED_EDGE('',*,*,#43074,.F.);
#56497=ORIENTED_EDGE('',*,*,#43110,.T.);
#56498=ORIENTED_EDGE('',*,*,#43088,.F.);
#56499=ORIENTED_EDGE('',*,*,#43110,.F.);
#56500=ORIENTED_EDGE('',*,*,#43073,.T.);
#56501=ORIENTED_EDGE('',*,*,#43111,.T.);
#56502=ORIENTED_EDGE('',*,*,#43081,.T.);
#56503=ORIENTED_EDGE('',*,*,#43112,.T.);
#56504=ORIENTED_EDGE('',*,*,#43092,.F.);
#56505=ORIENTED_EDGE('',*,*,#43113,.F.);
#56506=ORIENTED_EDGE('',*,*,#43089,.F.);
#56507=ORIENTED_EDGE('',*,*,#43111,.F.);
#56508=ORIENTED_EDGE('',*,*,#43087,.T.);
#56509=ORIENTED_EDGE('',*,*,#43106,.T.);
#56510=ORIENTED_EDGE('',*,*,#43080,.T.);
#56511=ORIENTED_EDGE('',*,*,#43114,.T.);
#56512=ORIENTED_EDGE('',*,*,#43093,.F.);
#56513=ORIENTED_EDGE('',*,*,#43112,.F.);
#56514=ORIENTED_EDGE('',*,*,#43091,.F.);
#56515=ORIENTED_EDGE('',*,*,#43105,.F.);
#56516=ORIENTED_EDGE('',*,*,#43085,.T.);
#56517=ORIENTED_EDGE('',*,*,#43082,.T.);
#56518=ORIENTED_EDGE('',*,*,#43113,.T.);
#56519=ORIENTED_EDGE('',*,*,#43079,.T.);
#56520=ORIENTED_EDGE('',*,*,#43109,.T.);
#56521=ORIENTED_EDGE('',*,*,#43094,.F.);
#56522=ORIENTED_EDGE('',*,*,#43114,.F.);
#56523=ORIENTED_EDGE('',*,*,#43084,.F.);
#56524=ORIENTED_EDGE('',*,*,#43068,.T.);
#56525=ORIENTED_EDGE('',*,*,#43066,.F.);
#56526=ORIENTED_EDGE('',*,*,#43115,.T.);
#56527=ORIENTED_EDGE('',*,*,#43116,.T.);
#56528=ORIENTED_EDGE('',*,*,#43051,.T.);
#56529=ORIENTED_EDGE('',*,*,#43060,.T.);
#56530=ORIENTED_EDGE('',*,*,#43056,.T.);
#56531=ORIENTED_EDGE('',*,*,#43069,.F.);
#56532=ORIENTED_EDGE('',*,*,#43117,.T.);
#56533=ORIENTED_EDGE('',*,*,#43023,.T.);
#56534=ORIENTED_EDGE('',*,*,#43115,.F.);
#56535=ORIENTED_EDGE('',*,*,#43072,.F.);
#56536=ORIENTED_EDGE('',*,*,#43071,.F.);
#56537=ORIENTED_EDGE('',*,*,#43039,.F.);
#56538=ORIENTED_EDGE('',*,*,#43038,.F.);
#56539=ORIENTED_EDGE('',*,*,#43118,.T.);
#56540=ORIENTED_EDGE('',*,*,#43029,.F.);
#56541=ORIENTED_EDGE('',*,*,#43065,.F.);
#56542=ORIENTED_EDGE('',*,*,#43027,.F.);
#56543=ORIENTED_EDGE('',*,*,#43024,.F.);
#56544=ORIENTED_EDGE('',*,*,#43119,.F.);
#56545=ORIENTED_EDGE('',*,*,#43048,.F.);
#56546=ORIENTED_EDGE('',*,*,#43045,.F.);
#56547=ORIENTED_EDGE('',*,*,#43042,.F.);
#56548=ORIENTED_EDGE('',*,*,#43120,.F.);
#56549=ORIENTED_EDGE('',*,*,#43118,.F.);
#56550=ORIENTED_EDGE('',*,*,#43037,.F.);
#56551=ORIENTED_EDGE('',*,*,#43121,.F.);
#56552=ORIENTED_EDGE('',*,*,#43030,.F.);
#56553=ORIENTED_EDGE('',*,*,#43120,.T.);
#56554=ORIENTED_EDGE('',*,*,#43036,.F.);
#56555=ORIENTED_EDGE('',*,*,#43035,.F.);
#56556=ORIENTED_EDGE('',*,*,#43122,.F.);
#56557=ORIENTED_EDGE('',*,*,#43121,.T.);
#56558=ORIENTED_EDGE('',*,*,#43052,.F.);
#56559=ORIENTED_EDGE('',*,*,#43116,.F.);
#56560=ORIENTED_EDGE('',*,*,#43022,.T.);
#56561=ORIENTED_EDGE('',*,*,#43021,.T.);
#56562=ORIENTED_EDGE('',*,*,#43026,.T.);
#56563=ORIENTED_EDGE('',*,*,#43064,.T.);
#56564=ORIENTED_EDGE('',*,*,#43031,.T.);
#56565=ORIENTED_EDGE('',*,*,#43122,.T.);
#56566=ORIENTED_EDGE('',*,*,#43034,.F.);
#56567=ORIENTED_EDGE('',*,*,#43033,.F.);
#56568=ORIENTED_EDGE('',*,*,#43044,.F.);
#56569=ORIENTED_EDGE('',*,*,#43047,.F.);
#56570=ORIENTED_EDGE('',*,*,#43049,.F.);
#56571=ORIENTED_EDGE('',*,*,#43119,.T.);
#56572=ORIENTED_EDGE('',*,*,#43117,.F.);
#56573=ORIENTED_EDGE('',*,*,#43070,.T.);
#56574=ORIENTED_EDGE('',*,*,#43062,.F.);
#56575=ORIENTED_EDGE('',*,*,#43061,.F.);
#56576=ORIENTED_EDGE('',*,*,#43053,.F.);
#56577=ORIENTED_EDGE('',*,*,#43041,.T.);
#56578=ORIENTED_EDGE('',*,*,#43057,.F.);
#56579=ORIENTED_EDGE('',*,*,#43099,.T.);
#56580=ORIENTED_EDGE('',*,*,#43059,.F.);
#76116=ADVANCED_FACE('',(#20686),#2211,.F.);
#76117=ADVANCED_FACE('',(#20687),#2212,.F.);
#76118=ADVANCED_FACE('',(#20688),#2213,.F.);
#76119=ADVANCED_FACE('',(#20689),#2214,.F.);
#76120=ADVANCED_FACE('',(#20690),#2215,.F.);
#76121=ADVANCED_FACE('',(#20691),#2216,.F.);
#76122=ADVANCED_FACE('',(#20692),#2217,.F.);
#76123=ADVANCED_FACE('',(#20693),#2218,.F.);
#76124=ADVANCED_FACE('',(#20694),#2219,.F.);
#76125=ADVANCED_FACE('',(#20695),#2220,.F.);
#76126=ADVANCED_FACE('',(#20696),#2221,.F.);
#76127=ADVANCED_FACE('',(#20697),#1939,.F.);
#76128=ADVANCED_FACE('',(#20698),#1940,.T.);
#76129=ADVANCED_FACE('',(#20699),#1941,.T.);
#76130=ADVANCED_FACE('',(#20700),#2222,.T.);
#76131=ADVANCED_FACE('',(#20701),#16971,.T.);
#76132=ADVANCED_FACE('',(#20702),#16972,.T.);
#76133=ADVANCED_FACE('',(#20703),#16973,.T.);
#76134=ADVANCED_FACE('',(#20704),#2223,.T.);
#76135=ADVANCED_FACE('',(#20705),#2224,.T.);
#76136=ADVANCED_FACE('',(#20706),#16974,.T.);
#76137=ADVANCED_FACE('',(#20707),#16975,.T.);
#76138=ADVANCED_FACE('',(#20708),#2225,.T.);
#76139=ADVANCED_FACE('',(#20709),#2226,.T.);
#76140=ADVANCED_FACE('',(#20710),#2227,.T.);
#76141=ADVANCED_FACE('',(#20711),#16976,.T.);
#76142=ADVANCED_FACE('',(#20712,#288),#16977,.T.);
#76143=ADVANCED_FACE('',(#20713),#183,.F.);
#76144=ADVANCED_FACE('',(#20714),#184,.F.);
#76145=ADVANCED_FACE('',(#20715),#185,.F.);
#76146=ADVANCED_FACE('',(#20716),#186,.F.);
#76147=ADVANCED_FACE('',(#20717),#187,.F.);
#76148=ADVANCED_FACE('',(#20718),#188,.F.);
#76149=ADVANCED_FACE('',(#20719),#189,.F.);
#76150=ADVANCED_FACE('',(#20720),#190,.F.);
#76151=ADVANCED_FACE('',(#20721,#289),#16978,.F.);
#76152=ADVANCED_FACE('',(#20722,#290),#16979,.F.);
#79326=CLOSED_SHELL('',(#76116,#76117,#76118,#76119,#76120,#76121,#76122,
#76123,#76124,#76125,#76126,#76127,#76128,#76129,#76130,#76131,#76132,#76133,
#76134,#76135,#76136,#76137,#76138,#76139,#76140,#76141,#76142,#76143,#76144,
#76145,#76146,#76147,#76148,#76149,#76150,#76151,#76152));
#80667=AXIS2_PLACEMENT_3D('',#174765,#88949,#88950);
#80668=AXIS2_PLACEMENT_3D('',#174766,#88951,#88952);
#80669=AXIS2_PLACEMENT_3D('',#174924,#88955,#88956);
#80670=AXIS2_PLACEMENT_3D('',#175090,#88958,#88959);
#80671=AXIS2_PLACEMENT_3D('',#175120,#88961,#88962);
#80672=AXIS2_PLACEMENT_3D('',#175254,#88966,#88967);
#80673=AXIS2_PLACEMENT_3D('',#175331,#88968,#88969);
#80674=AXIS2_PLACEMENT_3D('',#175491,#88971,#88972);
#80675=AXIS2_PLACEMENT_3D('',#175656,#88974,#88975);
#80676=AXIS2_PLACEMENT_3D('',#175813,#88977,#88978);
#80677=AXIS2_PLACEMENT_3D('',#175818,#88980,#88981);
#80678=AXIS2_PLACEMENT_3D('',#175827,#88982,#88983);
#80679=AXIS2_PLACEMENT_3D('',#175829,#88984,#88985);
#80680=AXIS2_PLACEMENT_3D('',#175832,#88987,#88988);
#80681=AXIS2_PLACEMENT_3D('',#175833,#88989,#88990);
#80682=AXIS2_PLACEMENT_3D('',#175962,#88991,#88992);
#80683=AXIS2_PLACEMENT_3D('',#175963,#88993,#88994);
#80684=AXIS2_PLACEMENT_3D('',#176130,#88995,#88996);
#80685=AXIS2_PLACEMENT_3D('',#176151,#88998,#88999);
#80686=AXIS2_PLACEMENT_3D('',#176257,#89000,#89001);
#80687=AXIS2_PLACEMENT_3D('',#176264,#89002,#89003);
#80688=AXIS2_PLACEMENT_3D('',#176270,#89004,#89005);
#80689=AXIS2_PLACEMENT_3D('',#176276,#89006,#89007);
#80690=AXIS2_PLACEMENT_3D('',#176282,#89008,#89009);
#80691=AXIS2_PLACEMENT_3D('',#176288,#89010,#89011);
#80692=AXIS2_PLACEMENT_3D('',#176291,#89013,#89014);
#80693=AXIS2_PLACEMENT_3D('',#176293,#89015,#89016);
#80694=AXIS2_PLACEMENT_3D('',#176298,#89017,#89018);
#80695=AXIS2_PLACEMENT_3D('',#176299,#89019,#89020);
#80696=AXIS2_PLACEMENT_3D('',#176306,#89021,#89022);
#80697=AXIS2_PLACEMENT_3D('',#176312,#89023,#89024);
#80698=AXIS2_PLACEMENT_3D('',#176318,#89025,#89026);
#80699=AXIS2_PLACEMENT_3D('',#176324,#89027,#89028);
#80700=AXIS2_PLACEMENT_3D('',#176330,#89029,#89030);
#80701=AXIS2_PLACEMENT_3D('',#176333,#89032,#89033);
#80702=AXIS2_PLACEMENT_3D('',#176335,#89034,#89035);
#80703=AXIS2_PLACEMENT_3D('',#176340,#89036,#89037);
#80704=AXIS2_PLACEMENT_3D('',#176341,#89038,#89039);
#80705=AXIS2_PLACEMENT_3D('',#176344,#89042,#89043);
#80706=AXIS2_PLACEMENT_3D('',#176347,#89046,#89047);
#80707=AXIS2_PLACEMENT_3D('',#176349,#89049,#89050);
#80708=AXIS2_PLACEMENT_3D('',#176351,#89052,#89053);
#80709=AXIS2_PLACEMENT_3D('',#176353,#89055,#89056);
#80710=AXIS2_PLACEMENT_3D('',#176355,#89058,#89059);
#80711=AXIS2_PLACEMENT_3D('',#176357,#89061,#89062);
#80712=AXIS2_PLACEMENT_3D('',#176360,#89065,#89066);
#80713=AXIS2_PLACEMENT_3D('',#176361,#89067,#89068);
#80714=AXIS2_PLACEMENT_3D('',#176363,#89070,#89071);
#80715=AXIS2_PLACEMENT_3D('',#176364,#89072,#89073);
#80716=AXIS2_PLACEMENT_3D('',#176365,#89074,#89075);
#80717=AXIS2_PLACEMENT_3D('',#177864,#89078,#89079);
#80718=AXIS2_PLACEMENT_3D('',#177865,#89080,#89081);
#88949=DIRECTION('axis',(0.,0.,1.));
#88950=DIRECTION('refdir',(1.,0.,0.));
#88951=DIRECTION('center_axis',(-1.,0.,0.));
#88952=DIRECTION('ref_axis',(0.,0.,1.));
#88953=DIRECTION('',(-1.,0.,0.));
#88954=DIRECTION('',(-0.999999999965599,-7.79366993348666E-6,-2.83899568731E-6));
#88955=DIRECTION('center_axis',(-1.,0.,0.));
#88956=DIRECTION('ref_axis',(0.,0.,1.));
#88957=DIRECTION('',(-1.,0.,0.));
#88958=DIRECTION('center_axis',(-1.,0.,0.));
#88959=DIRECTION('ref_axis',(0.,0.,1.));
#88960=DIRECTION('',(-1.,0.,0.));
#88961=DIRECTION('center_axis',(1.,0.,0.));
#88962=DIRECTION('ref_axis',(0.,0.,-1.));
#88963=DIRECTION('',(1.,0.,0.));
#88964=DIRECTION('',(0.999999999992329,-8.06779582213464E-7,3.83300064466167E-6));
#88965=DIRECTION('',(1.,0.,0.));
#88966=DIRECTION('center_axis',(-1.,0.,0.));
#88967=DIRECTION('ref_axis',(0.,1.,0.));
#88968=DIRECTION('center_axis',(1.,0.,0.));
#88969=DIRECTION('ref_axis',(0.,0.,-1.));
#88970=DIRECTION('',(1.,0.,0.));
#88971=DIRECTION('center_axis',(1.,0.,0.));
#88972=DIRECTION('ref_axis',(0.,0.,-1.));
#88973=DIRECTION('',(1.,0.,0.));
#88974=DIRECTION('center_axis',(1.,0.,0.));
#88975=DIRECTION('ref_axis',(0.,0.,-1.));
#88976=DIRECTION('',(1.,0.,0.));
#88977=DIRECTION('center_axis',(1.,0.,0.));
#88978=DIRECTION('ref_axis',(0.,0.,-1.));
#88979=DIRECTION('',(1.,0.,0.));
#88980=DIRECTION('center_axis',(-1.,0.,0.));
#88981=DIRECTION('ref_axis',(0.,-0.957773424896036,-0.287524027801011));
#88982=DIRECTION('center_axis',(1.,0.,0.));
#88983=DIRECTION('ref_axis',(0.,0.,-1.));
#88984=DIRECTION('center_axis',(-1.,0.,0.));
#88985=DIRECTION('ref_axis',(0.,1.,0.));
#88986=DIRECTION('',(1.,0.,0.));
#88987=DIRECTION('center_axis',(1.,0.,0.));
#88988=DIRECTION('ref_axis',(0.,-1.,0.));
#88989=DIRECTION('center_axis',(1.,0.,0.));
#88990=DIRECTION('ref_axis',(0.,0.,-1.));
#88991=DIRECTION('center_axis',(-1.,0.,0.));
#88992=DIRECTION('ref_axis',(0.,-0.957773424896036,-0.287524027801011));
#88993=DIRECTION('center_axis',(-1.,0.,0.));
#88994=DIRECTION('ref_axis',(0.,0.,1.));
#88995=DIRECTION('center_axis',(-1.,0.,8.90699599727784E-17));
#88996=DIRECTION('ref_axis',(8.90699599727784E-17,0.,1.));
#88997=DIRECTION('',(-0.707106708341652,-8.65956145444752E-17,-0.707106854031435));
#88998=DIRECTION('center_axis',(1.,0.,0.));
#88999=DIRECTION('ref_axis',(0.,1.,0.));
#89000=DIRECTION('center_axis',(1.,0.,-6.83634867380023E-18));
#89001=DIRECTION('ref_axis',(-6.83634867380023E-18,0.,-1.));
#89002=DIRECTION('center_axis',(-1.,0.,0.));
#89003=DIRECTION('ref_axis',(0.,0.906250000000018,-0.422742164327108));
#89004=DIRECTION('center_axis',(-1.,0.,0.));
#89005=DIRECTION('ref_axis',(0.,0.087019546441882,-0.99620660434322));
#89006=DIRECTION('center_axis',(-1.,0.,0.));
#89007=DIRECTION('ref_axis',(0.,-0.819230453558104,-0.573464440016103));
#89008=DIRECTION('center_axis',(1.,0.,0.));
#89009=DIRECTION('ref_axis',(0.,-0.819230453558104,0.573464440016103));
#89010=DIRECTION('center_axis',(1.,0.,0.));
#89011=DIRECTION('ref_axis',(0.,0.087019546441882,0.99620660434322));
#89012=DIRECTION('',(-0.707106781821139,8.65956055458343E-17,-0.707106780551956));
#89013=DIRECTION('center_axis',(1.,0.,0.));
#89014=DIRECTION('ref_axis',(0.,-1.,0.));
#89015=DIRECTION('center_axis',(1.,0.,0.));
#89016=DIRECTION('ref_axis',(0.,0.087019546441882,0.99620660434322));
#89017=DIRECTION('center_axis',(1.,0.,0.));
#89018=DIRECTION('ref_axis',(0.,0.906250000000018,0.422742164327108));
#89019=DIRECTION('center_axis',(-1.,0.,-1.02545230107003E-16));
#89020=DIRECTION('ref_axis',(-1.02545230107003E-16,0.,1.));
#89021=DIRECTION('center_axis',(1.,0.,0.));
#89022=DIRECTION('ref_axis',(0.,0.906250000000018,0.422742164327108));
#89023=DIRECTION('center_axis',(1.,0.,0.));
#89024=DIRECTION('ref_axis',(0.,0.087019546441882,0.99620660434322));
#89025=DIRECTION('center_axis',(1.,0.,0.));
#89026=DIRECTION('ref_axis',(0.,-0.819230453558104,0.573464440016103));
#89027=DIRECTION('center_axis',(-1.,0.,0.));
#89028=DIRECTION('ref_axis',(0.,-0.819230453558104,-0.573464440016103));
#89029=DIRECTION('center_axis',(-1.,0.,0.));
#89030=DIRECTION('ref_axis',(0.,0.087019546441882,-0.99620660434322));
#89031=DIRECTION('',(0.707106781821139,8.65956055458343E-17,0.707106780551956));
#89032=DIRECTION('center_axis',(1.,0.,0.));
#89033=DIRECTION('ref_axis',(0.,1.,0.));
#89034=DIRECTION('center_axis',(-1.,0.,0.));
#89035=DIRECTION('ref_axis',(0.,0.087019546441882,-0.99620660434322));
#89036=DIRECTION('center_axis',(-1.,0.,0.));
#89037=DIRECTION('ref_axis',(0.,0.906250000000018,-0.422742164327108));
#89038=DIRECTION('center_axis',(1.,0.,0.));
#89039=DIRECTION('ref_axis',(0.,0.,-1.));
#89040=DIRECTION('',(1.,0.,0.));
#89041=DIRECTION('',(1.,0.,0.));
#89042=DIRECTION('center_axis',(0.,0.500000000000017,0.866025403784429));
#89043=DIRECTION('ref_axis',(1.,0.,0.));
#89044=DIRECTION('',(1.,0.,0.));
#89045=DIRECTION('',(1.,0.,0.));
#89046=DIRECTION('center_axis',(0.,-0.500000000000017,-0.866025403784429));
#89047=DIRECTION('ref_axis',(0.,-0.866025403784429,0.500000000000017));
#89048=DIRECTION('',(1.,0.,0.));
#89049=DIRECTION('center_axis',(0.,0.500000000000017,-0.866025403784429));
#89050=DIRECTION('ref_axis',(-1.,0.,0.));
#89051=DIRECTION('',(1.,0.,0.));
#89052=DIRECTION('center_axis',(1.,0.,0.));
#89053=DIRECTION('ref_axis',(0.,0.,-1.));
#89054=DIRECTION('',(1.,0.,0.));
#89055=DIRECTION('center_axis',(1.,0.,0.));
#89056=DIRECTION('ref_axis',(0.,0.,-1.));
#89057=DIRECTION('',(1.,0.,0.));
#89058=DIRECTION('center_axis',(0.,1.,0.));
#89059=DIRECTION('ref_axis',(1.,0.,0.));
#89060=DIRECTION('',(1.,0.,0.));
#89061=DIRECTION('center_axis',(0.,-0.500000000000017,0.866025403784429));
#89062=DIRECTION('ref_axis',(-1.,0.,0.));
#89063=DIRECTION('',(1.,0.,0.));
#89064=DIRECTION('',(1.,0.,0.));
#89065=DIRECTION('center_axis',(1.,0.,0.));
#89066=DIRECTION('ref_axis',(0.,0.,-1.));
#89067=DIRECTION('center_axis',(1.,0.,0.));
#89068=DIRECTION('ref_axis',(0.,0.,-1.));
#89069=DIRECTION('',(1.,0.,0.));
#89070=DIRECTION('center_axis',(1.,0.,0.));
#89071=DIRECTION('ref_axis',(0.,-5.35449122399261E-13,1.));
#89072=DIRECTION('center_axis',(0.,-1.,0.));
#89073=DIRECTION('ref_axis',(0.,0.,-1.));
#89074=DIRECTION('center_axis',(-1.,0.,0.));
#89075=DIRECTION('ref_axis',(0.,0.,1.));
#89076=DIRECTION('',(-0.461790830635515,-0.303368053954474,0.833496882166236));
#89077=DIRECTION('',(-0.461753481727668,0.303366050431034,-0.833518303073334));
#89078=DIRECTION('center_axis',(1.,0.,0.));
#89079=DIRECTION('ref_axis',(0.,1.,0.));
#89080=DIRECTION('center_axis',(-1.,0.,0.));
#89081=DIRECTION('ref_axis',(0.,0.,1.));
#174765=CARTESIAN_POINT('',(0.,0.,0.));
#174766=CARTESIAN_POINT('Origin',(-23.90845228375,74.9968912574536,72.9873550812444));
#174767=CARTESIAN_POINT('',(-23.2177969711981,74.9968912574536,59.9387052680259));
#174768=CARTESIAN_POINT('',(-23.5174110875174,74.9968912574536,59.9387052680259));
#174769=CARTESIAN_POINT('',(-23.90845228375,74.9968912574536,59.9387052680259));
#174770=CARTESIAN_POINT('',(-24.4189072313413,74.9968582940746,86.0360048944213));
#174771=CARTESIAN_POINT('Ctrl Pts',(-23.5174110875174,74.9968912574536,
59.9387052680259));
#174772=CARTESIAN_POINT('Ctrl Pts',(-23.5306316897371,74.3947093830811,
59.9387052680259));
#174773=CARTESIAN_POINT('Ctrl Pts',(-23.5438009327752,73.793028183032,59.9803906448424));
#174774=CARTESIAN_POINT('Ctrl Pts',(-23.5751921994059,72.3608197445332,
60.1799448633758));
#174775=CARTESIAN_POINT('Ctrl Pts',(-23.5935749184201,71.5387148881984,
60.3770562255265));
#174776=CARTESIAN_POINT('Ctrl Pts',(-23.6306843757188,69.9428310814621,
60.9276138359542));
#174777=CARTESIAN_POINT('Ctrl Pts',(-23.6489357223363,69.1728925676118,
61.2800101514938));
#174778=CARTESIAN_POINT('Ctrl Pts',(-23.6862170214012,67.6961427337877,
62.1378741299171));
#174779=CARTESIAN_POINT('Ctrl Pts',(-23.7053154597809,66.9947011771143,
62.6443806601604));
#174780=CARTESIAN_POINT('Ctrl Pts',(-23.7372605442535,65.8985267731378,
63.6146285486161));
#174781=CARTESIAN_POINT('Ctrl Pts',(-23.7502862986929,65.4766725502222,
64.0434367410376));
#174782=CARTESIAN_POINT('Ctrl Pts',(-23.7777995451244,64.6603512478079,
64.9966630206717));
#174783=CARTESIAN_POINT('Ctrl Pts',(-23.7922833732239,64.2728028609773,
65.5248392427358));
#174784=CARTESIAN_POINT('Ctrl Pts',(-23.8229194172938,63.5337098738831,
66.7093534474452));
#174785=CARTESIAN_POINT('Ctrl Pts',(-23.8389795075283,63.1953279007174,
67.3712230547026));
#174786=CARTESIAN_POINT('Ctrl Pts',(-23.8698174699092,62.6654826054796,
68.6699413541111));
#174787=CARTESIAN_POINT('Ctrl Pts',(-23.8844820424246,62.4627426292908,
69.2996974587134));
#174788=CARTESIAN_POINT('Ctrl Pts',(-23.9176950045324,62.109553889035,70.7712848286564));
#174789=CARTESIAN_POINT('Ctrl Pts',(-23.9362135892086,61.9923040633228,
71.6179945676372));
#174790=CARTESIAN_POINT('Ctrl Pts',(-23.964236598216,61.942036872041,72.8849992863093));
#174791=CARTESIAN_POINT('Ctrl Pts',(-23.973449779398,61.9453912131552,73.3004782105993));
#174792=CARTESIAN_POINT('Ctrl Pts',(-24.0009465645323,62.0148930288987,
74.5447443855187));
#174793=CARTESIAN_POINT('Ctrl Pts',(-24.0189709350315,62.1403795210907,
75.3680792306046));
#174794=CARTESIAN_POINT('Ctrl Pts',(-24.0563699443479,62.5538671926331,
77.0100297541816));
#174795=CARTESIAN_POINT('Ctrl Pts',(-24.0754984434071,62.8467982285305,
77.8232629944303));
#174796=CARTESIAN_POINT('Ctrl Pts',(-24.1128050945005,63.5787378125085,
79.3589157490377));
#174797=CARTESIAN_POINT('Ctrl Pts',(-24.131294169336,64.0118682653229,80.0796236908367));
#174798=CARTESIAN_POINT('Ctrl Pts',(-24.1688946314926,65.0198641919139,
81.4405602344044));
#174799=CARTESIAN_POINT('Ctrl Pts',(-24.1875288663165,65.5948118402807,
82.0757351216293));
#174800=CARTESIAN_POINT('Ctrl Pts',(-24.2218130943148,66.745942130525,83.1204114609486));
#174801=CARTESIAN_POINT('Ctrl Pts',(-24.23740864815,67.3011544652776,83.5482557034675));
#174802=CARTESIAN_POINT('Ctrl Pts',(-24.2700005819463,68.5362341373696,
84.3506630736698));
#174803=CARTESIAN_POINT('Ctrl Pts',(-24.2868300007145,69.2206272059027,
84.7133789293529));
#174804=CARTESIAN_POINT('Ctrl Pts',(-24.3227853064787,70.7187769706881,
85.3442055799435));
#174805=CARTESIAN_POINT('Ctrl Pts',(-24.3417755229759,71.5350002648146,
85.5972454112807));
#174806=CARTESIAN_POINT('Ctrl Pts',(-24.3701818801963,72.8017543034024,
85.8575872429789));
#174807=CARTESIAN_POINT('Ctrl Pts',(-24.3798493266896,73.237675649591,85.9243818645359));
#174808=CARTESIAN_POINT('Ctrl Pts',(-24.3993200275243,74.1149668455025,
86.0136375501037));
#174809=CARTESIAN_POINT('Ctrl Pts',(-24.4091108195205,74.5557662227505,
86.0360037801385));
#174810=CARTESIAN_POINT('Ctrl Pts',(-24.4189072313413,74.9968582940747,
86.0360048944213));
#174811=CARTESIAN_POINT('',(-25.2173493892328,79.4629869826027,60.7268819234023));
#174812=CARTESIAN_POINT('Ctrl Pts',(-25.2179534601443,79.4630374617318,
60.7268167557867));
#174813=CARTESIAN_POINT('Ctrl Pts',(-25.1949255782283,80.4489154598281,
61.0859425267927));
#174814=CARTESIAN_POINT('Ctrl Pts',(-25.1723485468283,81.3878867153683,
61.562672966569));
#174815=CARTESIAN_POINT('Ctrl Pts',(-25.1418319224898,82.5496720747983,
62.3410093153827));
#174816=CARTESIAN_POINT('Ctrl Pts',(-25.1341597941251,82.8318350663601,
62.5469129762632));
#174817=CARTESIAN_POINT('Ctrl Pts',(-25.1058958914059,83.8409298929905,
63.3472530552093));
#174818=CARTESIAN_POINT('Ctrl Pts',(-25.0856284897418,84.511359906732,64.0082978439567));
#174819=CARTESIAN_POINT('Ctrl Pts',(-25.0463381621833,85.6523246677436,
65.4059328422703));
#174820=CARTESIAN_POINT('Ctrl Pts',(-25.027232400678,86.1315603731781,66.1291213643972));
#174821=CARTESIAN_POINT('Ctrl Pts',(-24.9900396375443,86.9286890065907,
67.6387170859581));
#174822=CARTESIAN_POINT('Ctrl Pts',(-24.9718326777449,87.2487759197293,
68.4193091338106));
#174823=CARTESIAN_POINT('Ctrl Pts',(-24.9272869194746,87.8326974023058,
70.3586157341816));
#174824=CARTESIAN_POINT('Ctrl Pts',(-24.9018234838558,88.0181608402933,
71.5331436490753));
#174825=CARTESIAN_POINT('Ctrl Pts',(-24.8571030316205,88.0603938351231,
73.5672948670293));
#174826=CARTESIAN_POINT('Ctrl Pts',(-24.8383743123942,87.9947871936716,
74.4177895566877));
#174827=CARTESIAN_POINT('Ctrl Pts',(-24.8106986129751,87.7741381142733,
75.6676798065923));
#174828=CARTESIAN_POINT('Ctrl Pts',(-24.8016093736651,87.6816712847804,
76.0758065751895));
#174829=CARTESIAN_POINT('Ctrl Pts',(-24.7773198416252,87.385647964188,77.1418062935282));
#174830=CARTESIAN_POINT('Ctrl Pts',(-24.7620753388422,87.1493723837374,
77.7892260852975));
#174831=CARTESIAN_POINT('Ctrl Pts',(-24.7308380021253,86.5571700848344,
79.0839389629231));
#174832=CARTESIAN_POINT('Ctrl Pts',(-24.7149083735725,86.195172121125,79.7258182827827));
#174833=CARTESIAN_POINT('Ctrl Pts',(-24.6873016319441,85.4903137590593,
80.7605121739211));
#174834=CARTESIAN_POINT('Ctrl Pts',(-24.6758558722288,85.1745290711364,
81.1696271952864));
#174835=CARTESIAN_POINT('Ctrl Pts',(-24.6475001697504,84.3290860728388,
82.1400231901871));
#174836=CARTESIAN_POINT('Ctrl Pts',(-24.6307810261104,83.772354714319,82.6751014390908));
#174837=CARTESIAN_POINT('Ctrl Pts',(-24.599585770867,82.6689003170912,83.5620240742505));
#174838=CARTESIAN_POINT('Ctrl Pts',(-24.5852411678047,82.1368548866381,
83.9282997510593));
#174839=CARTESIAN_POINT('Ctrl Pts',(-24.5583913263161,81.085177231511,84.5428023818064));
#174840=CARTESIAN_POINT('Ctrl Pts',(-24.5458806664955,80.5719400938607,
84.7989772586651));
#174841=CARTESIAN_POINT('Ctrl Pts',(-24.5143902223458,79.249545675383,85.3535788429129));
#174842=CARTESIAN_POINT('Ctrl Pts',(-24.4951894160072,78.4245499633485,
85.6071693181083));
#174843=CARTESIAN_POINT('Ctrl Pts',(-24.4570936740858,76.7300922849556,
85.9494606259938));
#174844=CARTESIAN_POINT('Ctrl Pts',(-24.4381782821791,75.8645543327958,
86.036007086387));
#174845=CARTESIAN_POINT('Ctrl Pts',(-24.4189072313414,74.9968582940746,
86.0360048944213));
#174846=CARTESIAN_POINT('',(-24.9173192207092,79.4630659019012,60.7267130748814));
#174847=CARTESIAN_POINT('',(-24.9176605481234,79.4630324820554,60.7268149418411));
#174848=CARTESIAN_POINT('Ctrl Pts',(-24.9171176851385,79.4630266224176,
60.7268128073552));
#174849=CARTESIAN_POINT('Ctrl Pts',(-24.907479882823,79.8753728640667,60.8770177568019));
#174850=CARTESIAN_POINT('Ctrl Pts',(-24.8978319043974,80.2798785853172,
61.0479289126257));
#174851=CARTESIAN_POINT('Ctrl Pts',(-24.8785453377169,81.0645998434556,
61.4271900252295));
#174852=CARTESIAN_POINT('Ctrl Pts',(-24.8689206935574,81.4445900685363,
61.6347482191992));
#174853=CARTESIAN_POINT('Ctrl Pts',(-24.840349563971,82.5416901570323,62.3068854017982));
#174854=CARTESIAN_POINT('Ctrl Pts',(-24.821762902311,83.2242721675299,62.8233682841019));
#174855=CARTESIAN_POINT('Ctrl Pts',(-24.7882924710906,84.3372637008269,
63.8515965314164));
#174856=CARTESIAN_POINT('Ctrl Pts',(-24.7735463269596,84.7882160198035,
64.3366558744028));
#174857=CARTESIAN_POINT('Ctrl Pts',(-24.7428192805704,85.6549656223796,
65.4239947985609));
#174858=CARTESIAN_POINT('Ctrl Pts',(-24.7269426546624,86.0608893983088,
66.0312845368707));
#174859=CARTESIAN_POINT('Ctrl Pts',(-24.6987033488005,86.6799171820225,
67.1498996693163));
#174860=CARTESIAN_POINT('Ctrl Pts',(-24.6864856504174,86.9152660426622,
67.646819458865));
#174861=CARTESIAN_POINT('Ctrl Pts',(-24.6551612930385,87.4390675705398,
68.96131540558));
#174862=CARTESIAN_POINT('Ctrl Pts',(-24.6363747440106,87.6787068724131,
69.7954432923412));
#174863=CARTESIAN_POINT('Ctrl Pts',(-24.6080786233649,87.9084778632656,
71.0558328275135));
#174864=CARTESIAN_POINT('Ctrl Pts',(-24.598861742352,87.9634238082213,71.4678552598435));
#174865=CARTESIAN_POINT('Ctrl Pts',(-24.5727907796244,88.063181685535,72.6410378365364));
#174866=CARTESIAN_POINT('Ctrl Pts',(-24.5562271243097,88.0611130529392,
73.4044777942705));
#174867=CARTESIAN_POINT('Ctrl Pts',(-24.5235275316636,87.9269505313888,
74.8870509312707));
#174868=CARTESIAN_POINT('Ctrl Pts',(-24.507401032424,87.8011257772416,75.6040034445301));
#174869=CARTESIAN_POINT('Ctrl Pts',(-24.4751432975777,87.4285472490523,
77.0204440402907));
#174870=CARTESIAN_POINT('Ctrl Pts',(-24.4591568287965,87.1806075424267,
77.7169362046151));
#174871=CARTESIAN_POINT('Ctrl Pts',(-24.4306825968416,86.6442142364001,
78.8965270434755));
#174872=CARTESIAN_POINT('Ctrl Pts',(-24.4183384755492,86.3809768706051,
79.3889984866159));
#174873=CARTESIAN_POINT('Ctrl Pts',(-24.3898062791471,85.6984170606593,
80.489923224599));
#174874=CARTESIAN_POINT('Ctrl Pts',(-24.3738573236368,85.2573577437238,
81.0826630754251));
#174875=CARTESIAN_POINT('Ctrl Pts',(-24.3484360912179,84.4881558658776,
81.9518531013098));
#174876=CARTESIAN_POINT('Ctrl Pts',(-24.3391233173508,84.1924687290483,
82.2549158317457));
#174877=CARTESIAN_POINT('Ctrl Pts',(-24.3107674447563,83.2503363923736,
83.1309876363149));
#174878=CARTESIAN_POINT('Ctrl Pts',(-24.2920534731176,82.561299893995,83.6547055024374));
#174879=CARTESIAN_POINT('Ctrl Pts',(-24.2569824435957,81.1923267956187,
84.4954455722956));
#174880=CARTESIAN_POINT('Ctrl Pts',(-24.2405874762494,80.5269788055029,
84.8295547203288));
#174881=CARTESIAN_POINT('Ctrl Pts',(-24.2054384202444,79.0371977989294,
85.4245808899677));
#174882=CARTESIAN_POINT('Ctrl Pts',(-24.1869132397422,78.2079210009582,
85.6640247659888));
#174883=CARTESIAN_POINT('Ctrl Pts',(-24.159348477152,76.9706829437812,85.8919677005822));
#174884=CARTESIAN_POINT('Ctrl Pts',(-24.1506142201114,76.57716252112,85.9460441609189));
#174885=CARTESIAN_POINT('Ctrl Pts',(-24.122990590964,75.323465862265,86.0603600583802));
#174886=CARTESIAN_POINT('Ctrl Pts',(-24.1044674113239,74.4594960530369,
86.0533918699913));
#174887=CARTESIAN_POINT('Ctrl Pts',(-24.0764752968672,73.1853327358667,
85.9164537916965));
#174888=CARTESIAN_POINT('Ctrl Pts',(-24.0672638926978,72.7705275994402,
85.8515162077124));
#174889=CARTESIAN_POINT('Ctrl Pts',(-24.0391353816953,71.5153348118852,
85.5924780012352));
#174890=CARTESIAN_POINT('Ctrl Pts',(-24.0205803158517,70.6904341543003,
85.3350183743386));
#174891=CARTESIAN_POINT('Ctrl Pts',(-23.9853250595168,69.2015481645728,
84.7028176556543));
#174892=CARTESIAN_POINT('Ctrl Pts',(-23.9686655586623,68.5330870501817,
84.3476938805495));
#174893=CARTESIAN_POINT('Ctrl Pts',(-23.9431413809485,67.549959050079,83.7103959685794));
#174894=CARTESIAN_POINT('Ctrl Pts',(-23.9341463648957,67.2118231353462,
83.4674848765376));
#174895=CARTESIAN_POINT('Ctrl Pts',(-23.9084332537329,66.2843549821508,
82.7315139018156));
#174896=CARTESIAN_POINT('Ctrl Pts',(-23.8915970203927,65.7261456823091,
82.2020274357745));
#174897=CARTESIAN_POINT('Ctrl Pts',(-23.8558673745728,64.6471229765557,
80.9806261645898));
#174898=CARTESIAN_POINT('Ctrl Pts',(-23.8373498958916,64.1418959989384,
80.2797596515301));
#174899=CARTESIAN_POINT('Ctrl Pts',(-23.7998503057796,63.2811086834496,
78.7956795514478));
#174900=CARTESIAN_POINT('Ctrl Pts',(-23.7810378773673,62.9262616653751,
78.0168781016788));
#174901=CARTESIAN_POINT('Ctrl Pts',(-23.7441929747498,62.3776760125511,
76.412461113905));
#174902=CARTESIAN_POINT('Ctrl Pts',(-23.7258692836287,62.1830391019126,
75.5914155731213));
#174903=CARTESIAN_POINT('Ctrl Pts',(-23.6883757749156,61.9518865214893,
73.9030935608427));
#174904=CARTESIAN_POINT('Ctrl Pts',(-23.6696975256392,61.9198874434843,
73.0393246060036));
#174905=CARTESIAN_POINT('Ctrl Pts',(-23.6339180304091,62.0214110492959,
71.4041912157041));
#174906=CARTESIAN_POINT('Ctrl Pts',(-23.6167598849786,62.1385016709135,
70.6354831377901));
#174907=CARTESIAN_POINT('Ctrl Pts',(-23.5853517843891,62.4792638045982,
69.2448625450023));
#174908=CARTESIAN_POINT('Ctrl Pts',(-23.5711600566694,62.6831158930766,
68.6206416349461));
#174909=CARTESIAN_POINT('Ctrl Pts',(-23.5404775668991,63.2166128083746,
67.3264351919183));
#174910=CARTESIAN_POINT('Ctrl Pts',(-23.5239715408375,63.5585307626862,
66.6639952735067));
#174911=CARTESIAN_POINT('Ctrl Pts',(-23.4985238885039,64.17653413673,65.6825672886288));
#174912=CARTESIAN_POINT('Ctrl Pts',(-23.4894745094915,64.4147139712013,
65.3415995372487));
#174913=CARTESIAN_POINT('Ctrl Pts',(-23.4589239558264,65.2683875666543,
64.2360065988036));
#174914=CARTESIAN_POINT('Ctrl Pts',(-23.43713499007,65.9536909696,63.5295327002692));
#174915=CARTESIAN_POINT('Ctrl Pts',(-23.4003935425218,67.246631807523,62.4668871104082));
#174916=CARTESIAN_POINT('Ctrl Pts',(-23.3853234262154,67.815748405656,62.070489364388));
#174917=CARTESIAN_POINT('Ctrl Pts',(-23.3513960249935,69.1434681142476,
61.2946542503527));
#174918=CARTESIAN_POINT('Ctrl Pts',(-23.3326256794217,69.9130319325745,
60.9401066017162));
#174919=CARTESIAN_POINT('Ctrl Pts',(-23.2955716873773,71.5096272106183,
60.3849607232919));
#174920=CARTESIAN_POINT('Ctrl Pts',(-23.2769908251956,72.3328673269368,
60.1856238439957));
#174921=CARTESIAN_POINT('Ctrl Pts',(-23.2446586345435,73.7752227019225,
59.9816281184901));
#174922=CARTESIAN_POINT('Ctrl Pts',(-23.2312093739932,74.3858353153039,
59.9387052680259));
#174923=CARTESIAN_POINT('Ctrl Pts',(-23.2177969711981,74.9968912574536,
59.9387052680259));
#174924=CARTESIAN_POINT('Origin',(-23.90845228375,74.9968912574536,72.9873550812444));
#174925=CARTESIAN_POINT('',(-21.4178560137093,74.9968912615648,59.9387052680259));
#174926=CARTESIAN_POINT('',(-21.7173525905574,74.9968912574536,59.9387052680259));
#174927=CARTESIAN_POINT('',(-23.90845228375,74.9968912574536,59.9387052680259));
#174928=CARTESIAN_POINT('Ctrl Pts',(-21.7173525905574,74.9968912574536,
59.9387052680259));
#174929=CARTESIAN_POINT('Ctrl Pts',(-21.7302063156957,74.4099001677546,
59.9387052680259));
#174930=CARTESIAN_POINT('Ctrl Pts',(-21.7431527425349,73.8232749118547,
59.9783138155532));
#174931=CARTESIAN_POINT('Ctrl Pts',(-21.7708092415273,72.5655155837762,
60.1491152972995));
#174932=CARTESIAN_POINT('Ctrl Pts',(-21.7855248966112,71.8982337599918,
60.2936435535157));
#174933=CARTESIAN_POINT('Ctrl Pts',(-21.8191003663665,70.4283593294628,
60.7348728947392));
#174934=CARTESIAN_POINT('Ctrl Pts',(-21.8378973148665,69.6374204991757,
61.0596192085729));
#174935=CARTESIAN_POINT('Ctrl Pts',(-21.8747288597517,68.1409049880788,
61.8531785853791));
#174936=CARTESIAN_POINT('Ctrl Pts',(-21.8930604919257,67.4377836432537,
62.3180383883955));
#174937=CARTESIAN_POINT('Ctrl Pts',(-21.9305692928866,66.1141772728772,
63.3900487508716));
#174938=CARTESIAN_POINT('Ctrl Pts',(-21.9492545327781,65.4995031373312,
63.997887959706));
#174939=CARTESIAN_POINT('Ctrl Pts',(-21.9848582071682,64.4606572539026,
65.2516214026179));
#174940=CARTESIAN_POINT('Ctrl Pts',(-22.0018106593114,64.0248831296256,
65.883213286058));
#174941=CARTESIAN_POINT('Ctrl Pts',(-22.0330147115562,63.3236714450916,
67.119415143412));
#174942=CARTESIAN_POINT('Ctrl Pts',(-22.0472138050556,63.0437252157077,
67.713020593513));
#174943=CARTESIAN_POINT('Ctrl Pts',(-22.0779145829976,62.5438034372538,
69.0198477713323));
#174944=CARTESIAN_POINT('Ctrl Pts',(-22.0944308896737,62.3379321954157,
69.7360073497001));
#174945=CARTESIAN_POINT('Ctrl Pts',(-22.129335439035,62.030797955824,71.2954150665285));
#174946=CARTESIAN_POINT('Ctrl Pts',(-22.1476938852872,61.9484251444568,
72.1389601782033));
#174947=CARTESIAN_POINT('Ctrl Pts',(-22.1755511193479,61.9481517353011,
73.3995577115146));
#174948=CARTESIAN_POINT('Ctrl Pts',(-22.1847606537286,61.9678629056999,
73.8143580866054));
#174949=CARTESIAN_POINT('Ctrl Pts',(-22.2166947481541,62.1053025258008,
75.2539209439819));
#174950=CARTESIAN_POINT('Ctrl Pts',(-22.239043878839,62.3246091103632,76.2651053904178));
#174951=CARTESIAN_POINT('Ctrl Pts',(-22.2711436235005,62.7965937029218,
77.6342938685587));
#174952=CARTESIAN_POINT('Ctrl Pts',(-22.2804156024698,62.9513880347713,
78.0219507666679));
#174953=CARTESIAN_POINT('Ctrl Pts',(-22.3067245585184,63.4466509246774,
79.1079827179994));
#174954=CARTESIAN_POINT('Ctrl Pts',(-22.3236323917217,63.831229993946,79.784277032089));
#174955=CARTESIAN_POINT('Ctrl Pts',(-22.3598918509028,64.7648882940439,
81.1308600635285));
#174956=CARTESIAN_POINT('Ctrl Pts',(-22.3790270103378,65.3251442237077,
81.7889387092825));
#174957=CARTESIAN_POINT('Ctrl Pts',(-22.4072423632755,66.2508914561918,
82.6803250777755));
#174958=CARTESIAN_POINT('Ctrl Pts',(-22.4165352981841,66.5696746640338,
82.958724063532));
#174959=CARTESIAN_POINT('Ctrl Pts',(-22.4449458637187,67.5774712698267,
83.7559451056425));
#174960=CARTESIAN_POINT('Ctrl Pts',(-22.4641503387602,68.3048636704198,
84.2224384205132));
#174961=CARTESIAN_POINT('Ctrl Pts',(-22.501285303839,69.810995887443,84.9898517968133));
#174962=CARTESIAN_POINT('Ctrl Pts',(-22.5195102657382,70.5832021864251,
85.2947829556675));
#174963=CARTESIAN_POINT('Ctrl Pts',(-22.5473234879989,71.7857662883215,
85.6418050277371));
#174964=CARTESIAN_POINT('Ctrl Pts',(-22.5567166580511,72.1979223482805,
85.739304069248));
#174965=CARTESIAN_POINT('Ctrl Pts',(-22.5755244853457,73.0384172083656,
85.8954110279683));
#174966=CARTESIAN_POINT('Ctrl Pts',(-22.5849742453824,73.4663957365637,
85.9531220346386));
#174967=CARTESIAN_POINT('Ctrl Pts',(-22.6134362956185,74.7541220080876,
86.0621095313202));
#174968=CARTESIAN_POINT('Ctrl Pts',(-22.6326452386617,75.6168779584812,
86.0496578720941));
#174969=CARTESIAN_POINT('Ctrl Pts',(-22.6709677204125,77.3455119283745,
85.8529668449526));
#174970=CARTESIAN_POINT('Ctrl Pts',(-22.6901390972948,78.2066494312835,
85.6655821751704));
#174971=CARTESIAN_POINT('Ctrl Pts',(-22.7188784283504,79.4392868969434,
85.2636194263096));
#174972=CARTESIAN_POINT('Ctrl Pts',(-22.7281584536231,79.8297491229408,
85.1152168230004));
#174973=CARTESIAN_POINT('Ctrl Pts',(-22.7529088994009,80.8584175963002,
84.6666711263083));
#174974=CARTESIAN_POINT('Ctrl Pts',(-22.7682334187029,81.4805314596249,
84.3331176818899));
#174975=CARTESIAN_POINT('Ctrl Pts',(-22.8027983993634,82.798230900913,83.4826918577857));
#174976=CARTESIAN_POINT('Ctrl Pts',(-22.8219893591569,83.4755286998752,
82.9435445720348));
#174977=CARTESIAN_POINT('Ctrl Pts',(-22.8500422418408,84.3943652677719,
82.0498945200944));
#174978=CARTESIAN_POINT('Ctrl Pts',(-22.8591742850748,84.6799558464963,
81.7440895610898));
#174979=CARTESIAN_POINT('Ctrl Pts',(-22.8848888190843,85.4369641606758,
80.8510945590963));
#174980=CARTESIAN_POINT('Ctrl Pts',(-22.9016020345431,85.8729940299941,
80.2360725574547));
#174981=CARTESIAN_POINT('Ctrl Pts',(-22.9328203510394,86.592180103431,79.0093760664373));
#174982=CARTESIAN_POINT('Ctrl Pts',(-22.9473374998402,86.8858300687438,
78.4066353215133));
#174983=CARTESIAN_POINT('Ctrl Pts',(-22.9810286478547,87.4499899421313,
76.9793754199744));
#174984=CARTESIAN_POINT('Ctrl Pts',(-23.0001903855084,87.687230217045,76.1450754570486));
#174985=CARTESIAN_POINT('Ctrl Pts',(-23.0281619377263,87.9139481390874,
74.8824264543852));
#174986=CARTESIAN_POINT('Ctrl Pts',(-23.0372443937547,87.9679773265212,
74.4680913785842));
#174987=CARTESIAN_POINT('Ctrl Pts',(-23.0630282534535,88.0641325863715,
73.2933767558786));
#174988=CARTESIAN_POINT('Ctrl Pts',(-23.0798660430062,88.0597426142557,
72.5308961097817));
#174989=CARTESIAN_POINT('Ctrl Pts',(-23.110718626206,87.9284862467173,71.1264365952234));
#174990=CARTESIAN_POINT('Ctrl Pts',(-23.1247527535594,87.8198404230815,
70.4851270400342));
#174991=CARTESIAN_POINT('Ctrl Pts',(-23.1548832091132,87.488965590155,69.147273968047));
#174992=CARTESIAN_POINT('Ctrl Pts',(-23.1709822825055,87.2551013670816,
68.4558621510493));
#174993=CARTESIAN_POINT('Ctrl Pts',(-23.2030228570246,86.6699535964167,
67.1090751142984));
#174994=CARTESIAN_POINT('Ctrl Pts',(-23.2189810029665,86.3179822987398,
66.4568526780595));
#174995=CARTESIAN_POINT('Ctrl Pts',(-23.2540992817533,85.4388073950574,
65.1145176809523));
#174996=CARTESIAN_POINT('Ctrl Pts',(-23.273094347954,84.8942159179656,64.4399488194559));
#174997=CARTESIAN_POINT('Ctrl Pts',(-23.3010605059325,83.9890549409349,
63.5222526741222));
#174998=CARTESIAN_POINT('Ctrl Pts',(-23.3102640153634,83.6766534830802,
63.2349759785988));
#174999=CARTESIAN_POINT('Ctrl Pts',(-23.3349547795299,82.8080045551004,
62.511045374306));
#175000=CARTESIAN_POINT('Ctrl Pts',(-23.3505379759931,82.2293415547844,
62.1035037303804));
#175001=CARTESIAN_POINT('Ctrl Pts',(-23.3857950726989,80.8338711771206,
61.2813490305736));
#175002=CARTESIAN_POINT('Ctrl Pts',(-23.4054853657382,80.0007276929279,
60.9017215669824));
#175003=CARTESIAN_POINT('Ctrl Pts',(-23.4346634324885,78.7391752955122,
60.4798934857545));
#175004=CARTESIAN_POINT('Ctrl Pts',(-23.4438349553282,78.3374278451823,
60.3666537439739));
#175005=CARTESIAN_POINT('Ctrl Pts',(-23.4704941584884,77.1454165599863,
60.0915798224803));
#175006=CARTESIAN_POINT('Ctrl Pts',(-23.4878574344418,76.3447741654688,
59.9834942206835));
#175007=CARTESIAN_POINT('Ctrl Pts',(-23.5094742272526,75.3585248802206,
59.9424627256623));
#175008=CARTESIAN_POINT('Ctrl Pts',(-23.5134418416706,75.1776854349154,
59.9387052680259));
#175009=CARTESIAN_POINT('Ctrl Pts',(-23.5174110875174,74.9968912574536,
59.9387052680259));
#175010=CARTESIAN_POINT('Ctrl Pts',(-23.2177969711981,74.9968912574536,
59.9387052680259));
#175011=CARTESIAN_POINT('Ctrl Pts',(-23.2122766055301,75.2483937134876,
59.9387052680259));
#175012=CARTESIAN_POINT('Ctrl Pts',(-23.206749248666,75.4999709804517,59.9459765228389));
#175013=CARTESIAN_POINT('Ctrl Pts',(-23.1868382383162,76.4020104636423,
59.9982159163286));
#175014=CARTESIAN_POINT('Ctrl Pts',(-23.1723428150149,77.0489752417336,
60.084601801932));
#175015=CARTESIAN_POINT('Ctrl Pts',(-23.1387122513219,78.5330764331777,
60.3972523725853));
#175016=CARTESIAN_POINT('Ctrl Pts',(-23.1199095752067,79.3595669630887,
60.6592427751684));
#175017=CARTESIAN_POINT('Ctrl Pts',(-23.0821115498925,80.928707858494,61.3343719010139));
#175018=CARTESIAN_POINT('Ctrl Pts',(-23.0633339395976,81.6692455056542,
61.7419933123616));
#175019=CARTESIAN_POINT('Ctrl Pts',(-23.026231243293,83.0632383898893,62.6957779977219));
#175020=CARTESIAN_POINT('Ctrl Pts',(-23.0076119265723,83.7131413994759,
63.2400738492398));
#175021=CARTESIAN_POINT('Ctrl Pts',(-22.9696043379337,84.9119525223814,
64.4605110212791));
#175022=CARTESIAN_POINT('Ctrl Pts',(-22.9507158743888,85.4552559591635,
65.1363601419598));
#175023=CARTESIAN_POINT('Ctrl Pts',(-22.9155042556653,86.3281026320126,
66.4751749515315));
#175024=CARTESIAN_POINT('Ctrl Pts',(-22.8991783125384,86.6760500700446,
67.1220261592005));
#175025=CARTESIAN_POINT('Ctrl Pts',(-22.8668564914752,87.2581364432114,
68.4639344324216));
#175026=CARTESIAN_POINT('Ctrl Pts',(-22.8509925336531,87.4918125648176,
69.1563744887733));
#175027=CARTESIAN_POINT('Ctrl Pts',(-22.8206340138724,87.8212172413,70.4928648072465));
#175028=CARTESIAN_POINT('Ctrl Pts',(-22.806238240693,87.9291085757939,71.1316691579198));
#175029=CARTESIAN_POINT('Ctrl Pts',(-22.7750988398522,88.0602372016251,
72.5378822152587));
#175030=CARTESIAN_POINT('Ctrl Pts',(-22.7584828653642,88.0641145347429,
73.3047098546431));
#175031=CARTESIAN_POINT('Ctrl Pts',(-22.7324138496429,87.9662301188309,
74.4832024422141));
#175032=CARTESIAN_POINT('Ctrl Pts',(-22.7231744470205,87.9117785726254,
74.8970656786553));
#175033=CARTESIAN_POINT('Ctrl Pts',(-22.6948123438722,87.6837443283447,
76.1590496732804));
#175034=CARTESIAN_POINT('Ctrl Pts',(-22.6760669416386,87.4455877607315,
76.9930815762467));
#175035=CARTESIAN_POINT('Ctrl Pts',(-22.6424278831996,86.8811365666569,
78.4164937016521));
#175036=CARTESIAN_POINT('Ctrl Pts',(-22.6276612363186,86.5885910904656,
79.0158974838695));
#175037=CARTESIAN_POINT('Ctrl Pts',(-22.5964391064742,85.8693918341243,
80.241760875551));
#175038=CARTESIAN_POINT('Ctrl Pts',(-22.580104399766,85.4313757342021,80.8587724139661));
#175039=CARTESIAN_POINT('Ctrl Pts',(-22.5543476911904,84.6719346593615,
81.7529372499967));
#175040=CARTESIAN_POINT('Ctrl Pts',(-22.5451298498866,84.3862669712625,
82.0582711510441));
#175041=CARTESIAN_POINT('Ctrl Pts',(-22.5168945854871,83.4668746349344,
82.9509064102007));
#175042=CARTESIAN_POINT('Ctrl Pts',(-22.4982518930569,82.7891212725679,
83.4894561594511));
#175043=CARTESIAN_POINT('Ctrl Pts',(-22.4640609704995,81.4753840607504,
84.3357126021793));
#175044=CARTESIAN_POINT('Ctrl Pts',(-22.4486091828021,80.8581356614063,
84.6664773458807));
#175045=CARTESIAN_POINT('Ctrl Pts',(-22.4164653455312,79.5109525283242,
85.254573077216));
#175046=CARTESIAN_POINT('Ctrl Pts',(-22.3998470581778,78.7785961749314,
85.4997529814177));
#175047=CARTESIAN_POINT('Ctrl Pts',(-22.371927537044,77.5385094339891,85.7960100070408));
#175048=CARTESIAN_POINT('Ctrl Pts',(-22.3608216463112,77.0417476535548,
85.8846425891359));
#175049=CARTESIAN_POINT('Ctrl Pts',(-22.3309115730071,75.686064074394,86.0462136198581));
#175050=CARTESIAN_POINT('Ctrl Pts',(-22.3124113574507,74.8230307679019,
86.06323056571));
#175051=CARTESIAN_POINT('Ctrl Pts',(-22.2844976295114,73.5511422499418,
85.9622972377186));
#175052=CARTESIAN_POINT('Ctrl Pts',(-22.2753810369904,73.1394503764237,
85.9097862283033));
#175053=CARTESIAN_POINT('Ctrl Pts',(-22.2479090344006,71.9058450340341,
85.6922628264543));
#175054=CARTESIAN_POINT('Ctrl Pts',(-22.2299005836022,71.0966584396281,
85.4676368267309));
#175055=CARTESIAN_POINT('Ctrl Pts',(-22.1963292659058,69.6602856382711,
84.9154445903109));
#175056=CARTESIAN_POINT('Ctrl Pts',(-22.1808755930549,69.0272956180662,
84.6115799670374));
#175057=CARTESIAN_POINT('Ctrl Pts',(-22.1498527206671,67.7979802517079,
83.8944401723291));
#175058=CARTESIAN_POINT('Ctrl Pts',(-22.1343011644881,67.2054601110404,
83.4793725230097));
#175059=CARTESIAN_POINT('Ctrl Pts',(-22.099644458544,65.9862354625609,82.4647897794127));
#175060=CARTESIAN_POINT('Ctrl Pts',(-22.0806461069253,65.3786610366711,
81.8475661646679));
#175061=CARTESIAN_POINT('Ctrl Pts',(-22.0436459429237,64.3087605378871,
80.5198641077891));
#175062=CARTESIAN_POINT('Ctrl Pts',(-22.0253349894935,63.8455304541845,
79.815383715023));
#175063=CARTESIAN_POINT('Ctrl Pts',(-21.9883357764173,63.0602967221302,
78.3254831707363));
#175064=CARTESIAN_POINT('Ctrl Pts',(-21.9701218644042,62.740445122404,77.543387573231));
#175065=CARTESIAN_POINT('Ctrl Pts',(-21.9329171687018,62.2502690489961,
75.9090249825322));
#175066=CARTESIAN_POINT('Ctrl Pts',(-21.9138313883391,62.0849382226692,
75.0595520014559));
#175067=CARTESIAN_POINT('Ctrl Pts',(-21.8831639335681,61.9542807843014,
73.659696518979));
#175068=CARTESIAN_POINT('Ctrl Pts',(-21.8714103011927,61.9376040534942,
73.1167750496578));
#175069=CARTESIAN_POINT('Ctrl Pts',(-21.8447841194471,61.9761462799511,
71.899530429945));
#175070=CARTESIAN_POINT('Ctrl Pts',(-21.829870331753,62.0498643471665,71.2273407251253));
#175071=CARTESIAN_POINT('Ctrl Pts',(-21.7960876134562,62.3355164686168,
69.716065712891));
#175072=CARTESIAN_POINT('Ctrl Pts',(-21.7774683443526,62.5794646088965,
68.8862256271957));
#175073=CARTESIAN_POINT('Ctrl Pts',(-21.7395220919643,63.2273532065084,
67.2874750558743));
#175074=CARTESIAN_POINT('Ctrl Pts',(-21.7205019632403,63.6295849146174,
66.5224489724313));
#175075=CARTESIAN_POINT('Ctrl Pts',(-21.6924089429919,64.3379396258668,
65.4485197264231));
#175076=CARTESIAN_POINT('Ctrl Pts',(-21.6831340767359,64.5886944224072,
65.1059385879003));
#175077=CARTESIAN_POINT('Ctrl Pts',(-21.659278120494,65.270927375683,64.2633473401903));
#175078=CARTESIAN_POINT('Ctrl Pts',(-21.6446174555065,65.7244658960641,
63.7827468956438));
#175079=CARTESIAN_POINT('Ctrl Pts',(-21.6118775989816,66.8263515960952,
62.7795688081261));
#175080=CARTESIAN_POINT('Ctrl Pts',(-21.5938354133167,67.4922483153368,
62.280490089044));
#175081=CARTESIAN_POINT('Ctrl Pts',(-21.5663060261506,68.5552678323796,
61.631962757131));
#175082=CARTESIAN_POINT('Ctrl Pts',(-21.5570934981404,68.9196079363756,
61.4328722197951));
#175083=CARTESIAN_POINT('Ctrl Pts',(-21.5238327972696,70.2730997642258,
60.7750240509474));
#175084=CARTESIAN_POINT('Ctrl Pts',(-21.5001959074978,71.309231096036,60.4232634933932));
#175085=CARTESIAN_POINT('Ctrl Pts',(-21.4667040833065,72.7881122727344,
60.1201607677847));
#175086=CARTESIAN_POINT('Ctrl Pts',(-21.4573831533975,73.2030744272741,
60.0557806310605));
#175087=CARTESIAN_POINT('Ctrl Pts',(-21.4380251932069,74.0776710893075,
59.9630036391895));
#175088=CARTESIAN_POINT('Ctrl Pts',(-21.4279728616493,74.5371369704319,
59.9387052677362));
#175089=CARTESIAN_POINT('Ctrl Pts',(-21.4178560137093,74.996891265676,59.9387052680259));
#175090=CARTESIAN_POINT('Origin',(-23.90845228375,74.9968912574536,72.9873550812444));
#175091=CARTESIAN_POINT('',(-19.6178714446467,74.9968993681034,59.9387052680284));
#175092=CARTESIAN_POINT('',(-19.9173382169355,74.9968858117148,59.938705268027));
#175093=CARTESIAN_POINT('',(-23.90845228375,74.9968912574536,59.9387052680259));
#175094=CARTESIAN_POINT('',(-19.4177763141321,83.3874087122245,62.9938945755098));
#175095=CARTESIAN_POINT('Ctrl Pts',(-19.6178714446467,74.9968993681034,
59.9387052680284));
#175096=CARTESIAN_POINT('Ctrl Pts',(-19.6014685026439,75.7392562382868,
59.9387057294552));
#175097=CARTESIAN_POINT('Ctrl Pts',(-19.5849037811272,76.4802620090225,
60.0020567382725));
#175098=CARTESIAN_POINT('Ctrl Pts',(-19.5521553242652,77.9468225819595,
60.2546657056363));
#175099=CARTESIAN_POINT('Ctrl Pts',(-19.5358475432088,78.6695897925503,
60.4440397486719));
#175100=CARTESIAN_POINT('Ctrl Pts',(-19.5024014277747,80.0908261196311,
60.949875575312));
#175101=CARTESIAN_POINT('Ctrl Pts',(-19.4854578253639,80.7856360811503,
61.2681603085282));
#175102=CARTESIAN_POINT('Ctrl Pts',(-19.4513770173665,82.1343953610875,
62.0353827008737));
#175103=CARTESIAN_POINT('Ctrl Pts',(-19.4340082401173,82.7833490499622,
62.4868441028634));
#175104=CARTESIAN_POINT('Ctrl Pts',(-19.4164777809729,83.3875372457796,
62.9941412915471));
#175105=CARTESIAN_POINT('',(-19.7174312187882,83.3870026620653,62.9934580993663));
#175106=CARTESIAN_POINT('Ctrl Pts',(-19.4175483972726,83.3873255397984,
62.9939635397476));
#175107=CARTESIAN_POINT('Ctrl Pts',(-19.5175444259387,83.3883618596074,
62.9948336320698));
#175108=CARTESIAN_POINT('Ctrl Pts',(-19.6175404546048,83.3883617890154,
62.9948335017092));
#175109=CARTESIAN_POINT('Ctrl Pts',(-19.7175364832709,83.3869807545433,
62.993674068783));
#175110=CARTESIAN_POINT('Ctrl Pts',(-19.9173382169355,74.9968858117148,
59.9387052680271));
#175111=CARTESIAN_POINT('Ctrl Pts',(-19.9007967949276,75.7554436370929,
59.9387049514496));
#175112=CARTESIAN_POINT('Ctrl Pts',(-19.8844783676533,76.5125565364492,
60.0048502818403));
#175113=CARTESIAN_POINT('Ctrl Pts',(-19.8511771565402,78.0094031487965,
60.2684072581934));
#175114=CARTESIAN_POINT('Ctrl Pts',(-19.8344745302453,78.7461983267385,
60.4657909926964));
#175115=CARTESIAN_POINT('Ctrl Pts',(-19.8097614398516,79.8151448713332,
60.8550310149607));
#175116=CARTESIAN_POINT('Ctrl Pts',(-19.8016215987501,80.1629869715839,
60.9990145028378));
#175117=CARTESIAN_POINT('Ctrl Pts',(-19.7685609555398,81.5415893673538,
61.640821849789));
#175118=CARTESIAN_POINT('Ctrl Pts',(-19.7433909837073,82.5110269727701,
62.258205377191));
#175119=CARTESIAN_POINT('Ctrl Pts',(-19.7185673678502,83.3874552850052,
62.9940724750352));
#175120=CARTESIAN_POINT('Origin',(-30.2175364832709,75.,72.98888938658));
#175121=CARTESIAN_POINT('',(-21.9012048916249,75.,85.23888938658));
#175122=CARTESIAN_POINT('',(-21.2338306962369,75.0000000451294,85.23888938658));
#175123=CARTESIAN_POINT('',(-30.2175364832709,75.,85.23888938658));
#175124=CARTESIAN_POINT('',(-20.333830095635,74.9999987451807,60.7388893865801));
#175125=CARTESIAN_POINT('Ctrl Pts',(-21.2338306951809,75.0000000451541,
85.23888938658));
#175126=CARTESIAN_POINT('Ctrl Pts',(-21.2308191510264,74.871361328295,85.2388893870541));
#175127=CARTESIAN_POINT('Ctrl Pts',(-21.2278115085571,74.7427004254411,
85.2368631119487));
#175128=CARTESIAN_POINT('Ctrl Pts',(-21.2058934519332,73.8042229972792,
85.20728181132));
#175129=CARTESIAN_POINT('Ctrl Pts',(-21.1871523997013,72.9989089654438,
85.1014707422029));
#175130=CARTESIAN_POINT('Ctrl Pts',(-21.1495260451104,71.4409117896302,
84.7370461654598));
#175131=CARTESIAN_POINT('Ctrl Pts',(-21.1311094437916,70.6910556826918,
84.4832054784111));
#175132=CARTESIAN_POINT('Ctrl Pts',(-21.0942053201137,69.2442539047876,
83.831808053776));
#175133=CARTESIAN_POINT('Ctrl Pts',(-21.075441657003,68.5512901173082,83.4345407518324));
#175134=CARTESIAN_POINT('Ctrl Pts',(-21.0377929593798,67.2413083429758,
82.5031960890114));
#175135=CARTESIAN_POINT('Ctrl Pts',(-21.0191271760664,66.629013431728,81.9691962546522));
#175136=CARTESIAN_POINT('Ctrl Pts',(-20.9858849275086,65.6589217849771,
80.9370958377329));
#175137=CARTESIAN_POINT('Ctrl Pts',(-20.971616746096,65.2772244909203,80.4653436863645));
#175138=CARTESIAN_POINT('Ctrl Pts',(-20.9385451921586,64.4703503834183,
79.3012370082582));
#175139=CARTESIAN_POINT('Ctrl Pts',(-20.9198101437826,64.0759242141126,
78.5910156278606));
#175140=CARTESIAN_POINT('Ctrl Pts',(-20.8822214137268,63.4419820235771,
77.1235982340241));
#175141=CARTESIAN_POINT('Ctrl Pts',(-20.8638337880297,63.1999769384464,
76.3716486083549));
#175142=CARTESIAN_POINT('Ctrl Pts',(-20.8269888930974,62.8620798677787,
74.8238825473228));
#175143=CARTESIAN_POINT('Ctrl Pts',(-20.8082536887632,62.7685033600815,
74.031380699892));
#175144=CARTESIAN_POINT('Ctrl Pts',(-20.7706138558305,62.7361723723302,
72.4252421628072));
#175145=CARTESIAN_POINT('Ctrl Pts',(-20.751950591255,62.8002954436033,71.6154360354312));
#175146=CARTESIAN_POINT('Ctrl Pts',(-20.7199080581257,63.0423491357255,
70.2712374331459));
#175147=CARTESIAN_POINT('Ctrl Pts',(-20.7068214756622,63.1778605296797,
69.7318865262472));
#175148=CARTESIAN_POINT('Ctrl Pts',(-20.6748772346359,63.6000066794672,
68.4325907237052));
#175149=CARTESIAN_POINT('Ctrl Pts',(-20.6561810950743,63.9264273894639,
67.6883523095461));
#175150=CARTESIAN_POINT('Ctrl Pts',(-20.627897104647,64.5165457174671,66.639564847221));
#175151=CARTESIAN_POINT('Ctrl Pts',(-20.618657075158,64.7254772554321,66.3067550654007));
#175152=CARTESIAN_POINT('Ctrl Pts',(-20.5904775305639,65.4134561475278,
65.3196280949693));
#175153=CARTESIAN_POINT('Ctrl Pts',(-20.5718102858009,65.9417256516032,
64.7023305719617));
#175154=CARTESIAN_POINT('Ctrl Pts',(-20.5379444375143,66.9837287179269,
63.7044026020081));
#175155=CARTESIAN_POINT('Ctrl Pts',(-20.5230629812357,67.4735626595182,
63.3030726194347));
#175156=CARTESIAN_POINT('Ctrl Pts',(-20.494111971847,68.4912688554889,62.5932566893908));
#175157=CARTESIAN_POINT('Ctrl Pts',(-20.4800537774037,69.015598449212,62.2828304602826));
#175158=CARTESIAN_POINT('Ctrl Pts',(-20.4549535739366,69.974637421168,61.8075866858196));
#175159=CARTESIAN_POINT('Ctrl Pts',(-20.4440701016085,70.3997239685461,
61.6260877697878));
#175160=CARTESIAN_POINT('Ctrl Pts',(-20.4166548860844,71.4996832993576,
61.2283065868462));
#175161=CARTESIAN_POINT('Ctrl Pts',(-20.4002998196522,72.1849361025285,
61.0457350114487));
#175162=CARTESIAN_POINT('Ctrl Pts',(-20.3671858554372,73.5813927560392,
60.8006112868465));
#175163=CARTESIAN_POINT('Ctrl Pts',(-20.3504179150539,74.2900185738204,
60.7388894593063));
#175164=CARTESIAN_POINT('Ctrl Pts',(-20.333830095635,74.9999987451808,60.7388893865801));
#175165=CARTESIAN_POINT('',(-20.1338946865143,82.8747201161109,63.6053345409726));
#175166=CARTESIAN_POINT('Ctrl Pts',(-20.333830095635,74.9999987451808,60.7388893865801));
#175167=CARTESIAN_POINT('Ctrl Pts',(-20.3171609122067,75.7134614016029,
60.7388893134971));
#175168=CARTESIAN_POINT('Ctrl Pts',(-20.3006993175161,76.4255596663345,
60.8012190536067));
#175169=CARTESIAN_POINT('Ctrl Pts',(-20.2672143173303,77.8301246910242,
61.0489997289239));
#175170=CARTESIAN_POINT('Ctrl Pts',(-20.250461415262,78.5199352933805,61.2338634607188));
#175171=CARTESIAN_POINT('Ctrl Pts',(-20.2255958036809,79.5230727248523,
61.5989754564678));
#175172=CARTESIAN_POINT('Ctrl Pts',(-20.2173661387531,79.8509732204579,
61.7347175085119));
#175173=CARTESIAN_POINT('Ctrl Pts',(-20.1841011379601,81.1444854104172,
62.3372463704192));
#175174=CARTESIAN_POINT('Ctrl Pts',(-20.1588428593053,82.0528151074486,
62.9156573754959));
#175175=CARTESIAN_POINT('Ctrl Pts',(-20.1339068674138,82.8741969746378,
63.6048858697113));
#175176=CARTESIAN_POINT('',(-19.4263813260168,87.1238126841961,74.7426470661147));
#175177=CARTESIAN_POINT('Ctrl Pts',(-20.1339146423347,82.8747673376467,
63.605364495691));
#175178=CARTESIAN_POINT('Ctrl Pts',(-20.0750070626096,83.6655473294934,
64.2689966087262));
#175179=CARTESIAN_POINT('Ctrl Pts',(-20.0153558799609,84.3692856442602,
65.0299429613645));
#175180=CARTESIAN_POINT('Ctrl Pts',(-19.8973223675187,85.576628975846,66.7207259848247));
#175181=CARTESIAN_POINT('Ctrl Pts',(-19.8395215672343,86.0726477946759,
67.6455451969489));
#175182=CARTESIAN_POINT('Ctrl Pts',(-19.7215871660935,86.8132860967313,
69.5867095690446));
#175183=CARTESIAN_POINT('Ctrl Pts',(-19.6618458561677,87.0579171526477,
70.5940527189557));
#175184=CARTESIAN_POINT('Ctrl Pts',(-19.5435268983665,87.290081387854,72.6588170657527));
#175185=CARTESIAN_POINT('Ctrl Pts',(-19.485538173564,87.273451718315,73.7081850984936));
#175186=CARTESIAN_POINT('Ctrl Pts',(-19.4263813260168,87.1238126841961,
74.7426470661147));
#175187=CARTESIAN_POINT('',(-19.1263815299174,87.1238125173955,74.7426482192146));
#175188=CARTESIAN_POINT('',(-19.4263814899908,87.1238253799095,74.7426467836703));
#175189=CARTESIAN_POINT('',(-19.0011490535824,82.874758698514,63.6053538167644));
#175190=CARTESIAN_POINT('Ctrl Pts',(-19.1263815299174,87.1238125173955,
74.7426482192146));
#175191=CARTESIAN_POINT('Ctrl Pts',(-19.1161087162537,87.2734479483372,
73.7082118549104));
#175192=CARTESIAN_POINT('Ctrl Pts',(-19.1067682656167,87.2900817700419,
72.6588612733507));
#175193=CARTESIAN_POINT('Ctrl Pts',(-19.085604853827,87.0579293876326,70.5941212219599));
#175194=CARTESIAN_POINT('Ctrl Pts',(-19.0740038291453,86.8133083884435,
69.5867931485784));
#175195=CARTESIAN_POINT('Ctrl Pts',(-19.0533079901649,86.0726883888103,
67.645626130394));
#175196=CARTESIAN_POINT('Ctrl Pts',(-19.0441709589811,85.5766676037541,
66.720788062231));
#175197=CARTESIAN_POINT('Ctrl Pts',(-19.02327760971,84.3693228475831,65.0299871776317));
#175198=CARTESIAN_POINT('Ctrl Pts',(-19.0117355006677,83.66558539603,64.2690330647643));
#175199=CARTESIAN_POINT('Ctrl Pts',(-19.0011200059672,82.8747987388434,
63.6053908480439));
#175200=CARTESIAN_POINT('',(-19.2012431461282,75.0000012408645,60.7388893865801));
#175201=CARTESIAN_POINT('Ctrl Pts',(-19.0011647644417,82.8742002889142,
63.6048886507497));
#175202=CARTESIAN_POINT('Ctrl Pts',(-19.0263800941151,82.052819403866,62.9156604862996));
#175203=CARTESIAN_POINT('Ctrl Pts',(-19.0510542001329,81.1444903313531,
62.3372490326857));
#175204=CARTESIAN_POINT('Ctrl Pts',(-19.0845340441755,79.8509765741827,
61.7347189482849));
#175205=CARTESIAN_POINT('Ctrl Pts',(-19.0928876791463,79.5230760771588,
61.5989767903968));
#175206=CARTESIAN_POINT('Ctrl Pts',(-19.1179505022709,78.5199407196386,
61.2338652070603));
#175207=CARTESIAN_POINT('Ctrl Pts',(-19.1344708541158,77.8301319180988,
61.0490012011107));
#175208=CARTESIAN_POINT('Ctrl Pts',(-19.1676976678863,76.4255613881577,
60.8012191599193));
#175209=CARTESIAN_POINT('Ctrl Pts',(-19.1845437886602,75.7134618805566,
60.7388894588501));
#175210=CARTESIAN_POINT('Ctrl Pts',(-19.2012431461282,75.0000012408646,
60.7388893865801));
#175211=CARTESIAN_POINT('',(-20.1012419532334,74.9999999736999,85.23888938658));
#175212=CARTESIAN_POINT('Ctrl Pts',(-19.2012431461282,75.0000012408646,
60.7388893865801));
#175213=CARTESIAN_POINT('Ctrl Pts',(-19.2134414436994,74.4788431540949,
60.7388893337893));
#175214=CARTESIAN_POINT('Ctrl Pts',(-19.2255316436779,73.9582261001053,
60.7721462266043));
#175215=CARTESIAN_POINT('Ctrl Pts',(-19.2496023259986,72.9325536678046,
60.9037227977139));
#175216=CARTESIAN_POINT('Ctrl Pts',(-19.2616559602448,72.4284066056991,
61.000875007271));
#175217=CARTESIAN_POINT('Ctrl Pts',(-19.2971923316806,70.964770891133,61.3795292005648));
#175218=CARTESIAN_POINT('Ctrl Pts',(-19.3201799357145,70.0319253130648,
61.747067855105));
#175219=CARTESIAN_POINT('Ctrl Pts',(-19.3593847583475,68.5631416228094,
62.5446770846949));
#175220=CARTESIAN_POINT('Ctrl Pts',(-19.3752189169677,67.9996079481036,
62.9137102767736));
#175221=CARTESIAN_POINT('Ctrl Pts',(-19.4094187241687,66.8432021863185,
63.8150608881449));
#175222=CARTESIAN_POINT('Ctrl Pts',(-19.4278042339043,66.2660911726339,
64.3626902025144));
#175223=CARTESIAN_POINT('Ctrl Pts',(-19.4649076716685,65.2322706283307,
65.5545942849738));
#175224=CARTESIAN_POINT('Ctrl Pts',(-19.48317667112,64.7765667923802,66.1948699295475));
#175225=CARTESIAN_POINT('Ctrl Pts',(-19.5187769340716,64.0126196723153,
67.5210652427873));
#175226=CARTESIAN_POINT('Ctrl Pts',(-19.5363488515712,63.6999414443376,
68.200539244494));
#175227=CARTESIAN_POINT('Ctrl Pts',(-19.5728306395091,63.1810136242172,
69.667751902816));
#175228=CARTESIAN_POINT('Ctrl Pts',(-19.5914858748346,62.9873504500301,
70.4561749871619));
#175229=CARTESIAN_POINT('Ctrl Pts',(-19.6196435768446,62.817633464455,71.6452040910368));
#175230=CARTESIAN_POINT('Ctrl Pts',(-19.6288601738607,62.7809380375738,
72.0349137298658));
#175231=CARTESIAN_POINT('Ctrl Pts',(-19.6544834290468,62.7307562290817,
73.1252885164172));
#175232=CARTESIAN_POINT('Ctrl Pts',(-19.6707160276316,62.7586102506711,
73.8263408637774));
#175233=CARTESIAN_POINT('Ctrl Pts',(-19.7059100506015,62.9475964263193,
75.3253565069979));
#175234=CARTESIAN_POINT('Ctrl Pts',(-19.725057923176,63.1285523053371,76.1175051964773));
#175235=CARTESIAN_POINT('Ctrl Pts',(-19.7559496259563,63.5493004420543,
77.3713704283252));
#175236=CARTESIAN_POINT('Ctrl Pts',(-19.7678070748152,63.7424600523,77.8460957691832));
#175237=CARTESIAN_POINT('Ctrl Pts',(-19.7986461064567,64.3165236659883,
79.0372199075292));
#175238=CARTESIAN_POINT('Ctrl Pts',(-19.8177871208792,64.7398369689772,
79.7304043474254));
#175239=CARTESIAN_POINT('Ctrl Pts',(-19.8478203966771,65.516099512857,80.7571314685154));
#175240=CARTESIAN_POINT('Ctrl Pts',(-19.8588668534339,65.8256947439059,
81.1204375505771));
#175241=CARTESIAN_POINT('Ctrl Pts',(-19.8888962515482,66.7161925145208,
82.0496449273593));
#175242=CARTESIAN_POINT('Ctrl Pts',(-19.9080316552855,67.333342169459,82.5774824699059));
#175243=CARTESIAN_POINT('Ctrl Pts',(-19.9378463954545,68.3820843582458,
83.3080331022866));
#175244=CARTESIAN_POINT('Ctrl Pts',(-19.9486871406438,68.7811211268677,
83.5533145481652));
#175245=CARTESIAN_POINT('Ctrl Pts',(-19.9785111556418,69.9064760633333,
84.1591494050551));
#175246=CARTESIAN_POINT('Ctrl Pts',(-19.9976447410377,70.6560739141292,
84.4714415311945));
#175247=CARTESIAN_POINT('Ctrl Pts',(-20.0273999530786,71.8763787356722,
84.8430979285698));
#175248=CARTESIAN_POINT('Ctrl Pts',(-20.0381847070728,72.3291363992183,
84.9532429649795));
#175249=CARTESIAN_POINT('Ctrl Pts',(-20.0663734302189,73.5172146050537,
85.1714571165322));
#175250=CARTESIAN_POINT('Ctrl Pts',(-20.0839074383617,74.2579106759087,
85.2388893849859));
#175251=CARTESIAN_POINT('Ctrl Pts',(-20.1012419538474,74.9999999736855,
85.23888938658));
#175252=CARTESIAN_POINT('',(-18.5675364832709,75.,85.23888938658));
#175253=CARTESIAN_POINT('',(-30.2175364832709,75.,85.23888938658));
#175254=CARTESIAN_POINT('Origin',(-18.5675364832709,75.,72.98888938658));
#175255=CARTESIAN_POINT('Ctrl Pts',(-20.1012419538474,74.9999999736855,
85.23888938658));
#175256=CARTESIAN_POINT('Ctrl Pts',(-20.1028223166909,75.0676551875689,
85.2388893867253));
#175257=CARTESIAN_POINT('Ctrl Pts',(-20.1044017500603,75.1353219645402,
85.2383289101491));
#175258=CARTESIAN_POINT('Ctrl Pts',(-20.1153971737163,75.6066547974153,
85.2305174346676));
#175259=CARTESIAN_POINT('Ctrl Pts',(-20.1247609958429,76.009738492333,85.2038767090203));
#175260=CARTESIAN_POINT('Ctrl Pts',(-20.1530480306987,77.2159205135722,
85.0640365427909));
#175261=CARTESIAN_POINT('Ctrl Pts',(-20.1721961606555,78.0098209912336,
84.8910092458878));
#175262=CARTESIAN_POINT('Ctrl Pts',(-20.2097492344187,79.5392277376216,
84.3947517872493));
#175263=CARTESIAN_POINT('Ctrl Pts',(-20.2281692206887,80.2718241419228,
84.0751941446952));
#175264=CARTESIAN_POINT('Ctrl Pts',(-20.265532914787,81.6596032469581,83.300974092744));
#175265=CARTESIAN_POINT('Ctrl Pts',(-20.2840271704208,82.3120316605387,
82.8490926166641));
#175266=CARTESIAN_POINT('Ctrl Pts',(-20.3202501892902,83.50066929936,81.8425624201366));
#175267=CARTESIAN_POINT('Ctrl Pts',(-20.3382423866161,84.0373753924667,
81.2939928603718));
#175268=CARTESIAN_POINT('Ctrl Pts',(-20.3717530294913,84.9365885538429,
80.1837622258671));
#175269=CARTESIAN_POINT('Ctrl Pts',(-20.3871132904699,85.3113286396946,
79.635579466878));
#175270=CARTESIAN_POINT('Ctrl Pts',(-20.4117890395023,85.8362236370969,
78.7156457704034));
#175271=CARTESIAN_POINT('Ctrl Pts',(-20.421094180155,86.0157658109008,78.3621921294577));
#175272=CARTESIAN_POINT('Ctrl Pts',(-20.448804125734,86.4978596859949,77.2869681387593));
#175273=CARTESIAN_POINT('Ctrl Pts',(-20.467019065534,86.7487697008896,76.5442620191068));
#175274=CARTESIAN_POINT('Ctrl Pts',(-20.5040710007189,87.1120325898912,
74.9934560479705));
#175275=CARTESIAN_POINT('Ctrl Pts',(-20.5231799791372,87.2181120052346,
74.1877862472172));
#175276=CARTESIAN_POINT('Ctrl Pts',(-20.5557315826169,87.262242220435,72.7976337715917));
#175277=CARTESIAN_POINT('Ctrl Pts',(-20.5691687789934,87.2394256899517,
72.2171244313196));
#175278=CARTESIAN_POINT('Ctrl Pts',(-20.601583588832,87.0863470034626,70.8349469069845));
#175279=CARTESIAN_POINT('Ctrl Pts',(-20.6207303159624,86.9174291951864,
70.0403079980347));
#175280=CARTESIAN_POINT('Ctrl Pts',(-20.6582415576073,86.4293524196668,
68.5092825435072));
#175281=CARTESIAN_POINT('Ctrl Pts',(-20.6766611147279,86.1139751779511,
67.7757783466081));
#175282=CARTESIAN_POINT('Ctrl Pts',(-20.7139441602189,85.3489439344115,
66.3870454821064));
#175283=CARTESIAN_POINT('Ctrl Pts',(-20.7323540862565,84.9023774132677,
65.7343795777472));
#175284=CARTESIAN_POINT('Ctrl Pts',(-20.7684423465106,83.9067986201705,
64.544176703437));
#175285=CARTESIAN_POINT('Ctrl Pts',(-20.7863796880053,83.3638662589221,
64.0061298905882));
#175286=CARTESIAN_POINT('Ctrl Pts',(-20.819482597375,82.2728299293608,63.1101366643164));
#175287=CARTESIAN_POINT('Ctrl Pts',(-20.8345200996702,81.7392693547576,
62.7387157770536));
#175288=CARTESIAN_POINT('Ctrl Pts',(-20.8685278016309,80.4789467263994,
62.002508333814));
#175289=CARTESIAN_POINT('Ctrl Pts',(-20.8876760720512,79.7402454016475,
61.6641599491032));
#175290=CARTESIAN_POINT('Ctrl Pts',(-20.9252196337597,78.2194380305459,
61.1426538905575));
#175291=CARTESIAN_POINT('Ctrl Pts',(-20.9436417815588,77.4418691498786,
60.9582888637351));
#175292=CARTESIAN_POINT('Ctrl Pts',(-20.9809858540324,75.86814439489,60.7441145447466));
#175293=CARTESIAN_POINT('Ctrl Pts',(-20.9994564621255,75.0758712250009,
60.7136119037197));
#175294=CARTESIAN_POINT('Ctrl Pts',(-21.035655851417,73.5219913558667,60.8043087243461));
#175295=CARTESIAN_POINT('Ctrl Pts',(-21.0536474532168,72.7636378407663,
60.9204515119222));
#175296=CARTESIAN_POINT('Ctrl Pts',(-21.0870392604064,71.3825806657978,
61.2666833019794));
#175297=CARTESIAN_POINT('Ctrl Pts',(-21.1022910619968,70.7579984613976,
61.4779701746728));
#175298=CARTESIAN_POINT('Ctrl Pts',(-21.1365117190325,69.4090390905218,
62.059086120334));
#175299=CARTESIAN_POINT('Ctrl Pts',(-21.1556599928895,68.6983143827961,
62.4528465332682));
#175300=CARTESIAN_POINT('Ctrl Pts',(-21.1932065886658,67.3759844771906,
63.3674268622471));
#175301=CARTESIAN_POINT('Ctrl Pts',(-21.2116283123113,66.7661046410529,
63.8838842631046));
#175302=CARTESIAN_POINT('Ctrl Pts',(-21.248978490679,65.659598076138,65.0236246952985));
#175303=CARTESIAN_POINT('Ctrl Pts',(-21.267456116477,65.1647440817905,65.6433942431097));
#175304=CARTESIAN_POINT('Ctrl Pts',(-21.3036624201977,64.3154992015791,
66.9481885705126));
#175305=CARTESIAN_POINT('Ctrl Pts',(-21.3216541228067,63.9589435030155,
67.6275753624872));
#175306=CARTESIAN_POINT('Ctrl Pts',(-21.355080561869,63.417577167365,68.9459806329616));
#175307=CARTESIAN_POINT('Ctrl Pts',(-21.3703640420479,63.2167111228776,
69.5754258751196));
#175308=CARTESIAN_POINT('Ctrl Pts',(-21.4046161709535,62.8841636337735,
71.0074871142765));
#175309=CARTESIAN_POINT('Ctrl Pts',(-21.4237644421783,62.7796352669119,
71.8132496104919));
#175310=CARTESIAN_POINT('Ctrl Pts',(-21.4613114637403,62.7316661781799,
73.4203395033265));
#175311=CARTESIAN_POINT('Ctrl Pts',(-21.4797331112469,62.7857374480785,
74.2176902529325));
#175312=CARTESIAN_POINT('Ctrl Pts',(-21.5170841560245,63.0470665200251,
75.784597454807));
#175313=CARTESIAN_POINT('Ctrl Pts',(-21.5355627995451,63.2525521160856,
76.5506415933651));
#175314=CARTESIAN_POINT('Ctrl Pts',(-21.5728111592244,63.8150992117279,
78.050231102644));
#175315=CARTESIAN_POINT('Ctrl Pts',(-21.5918703440964,64.1743111610024,
78.7788496574188));
#175316=CARTESIAN_POINT('Ctrl Pts',(-21.6254652707981,64.9324581646813,
79.9957208106493));
#175317=CARTESIAN_POINT('Ctrl Pts',(-21.6399043307748,65.3019956610183,
80.4988691966758));
#175318=CARTESIAN_POINT('Ctrl Pts',(-21.6733168717337,66.2363698955215,
81.5864563713893));
#175319=CARTESIAN_POINT('Ctrl Pts',(-21.6924649125501,66.8242294875584,
82.1472814426361));
#175320=CARTESIAN_POINT('Ctrl Pts',(-21.7205547811873,67.7726337654651,
82.8874649023955));
#175321=CARTESIAN_POINT('Ctrl Pts',(-21.7296687303816,68.0935491655393,
83.1139847958481));
#175322=CARTESIAN_POINT('Ctrl Pts',(-21.7576697230568,69.1087909334589,
83.759839284864));
#175323=CARTESIAN_POINT('Ctrl Pts',(-21.7768004439335,69.8343025437369,
84.126001677358));
#175324=CARTESIAN_POINT('Ctrl Pts',(-21.8143017642663,71.3303827853448,
84.7032000564873));
#175325=CARTESIAN_POINT('Ctrl Pts',(-21.8325820446841,72.0960836069837,
84.9161033760842));
#175326=CARTESIAN_POINT('Ctrl Pts',(-21.860391207462,73.2618002069962,85.12123634458));
#175327=CARTESIAN_POINT('Ctrl Pts',(-21.8695882980235,73.6496522610376,
85.1705043446784));
#175328=CARTESIAN_POINT('Ctrl Pts',(-21.8862630534666,74.3590334071425,
85.2263152718581));
#175329=CARTESIAN_POINT('Ctrl Pts',(-21.8937447193925,74.6795488660732,
85.23888938658));
#175330=CARTESIAN_POINT('Ctrl Pts',(-21.9012048916249,75.,85.23888938658));
#175331=CARTESIAN_POINT('Origin',(-30.2175364832709,75.,72.98888938658));
#175332=CARTESIAN_POINT('',(-23.7011390782975,75.,85.23888938658));
#175333=CARTESIAN_POINT('',(-23.0338668482845,75.,85.23888938658));
#175334=CARTESIAN_POINT('',(-30.2175364832709,75.,85.23888938658));
#175335=CARTESIAN_POINT('Ctrl Pts',(-23.0338668482845,75.,85.23888938658));
#175336=CARTESIAN_POINT('Ctrl Pts',(-23.0263120013374,74.6783909709593,
85.23888938658));
#175337=CARTESIAN_POINT('Ctrl Pts',(-23.0187763345677,74.3567175223817,
85.2262242055521));
#175338=CARTESIAN_POINT('Ctrl Pts',(-23.0021463072687,73.646290598585,85.1701281976121));
#175339=CARTESIAN_POINT('Ctrl Pts',(-22.9930805082051,73.2585458076826,
85.1207666313114));
#175340=CARTESIAN_POINT('Ctrl Pts',(-22.9655328564508,72.0931519560926,
84.9153772668127));
#175341=CARTESIAN_POINT('Ctrl Pts',(-22.9468179854882,71.3276772120241,
84.702339729707));
#175342=CARTESIAN_POINT('Ctrl Pts',(-22.909325835243,69.8318905314435,84.1248828191962));
#175343=CARTESIAN_POINT('Ctrl Pts',(-22.8906302771522,69.1064587569298,
83.7585632583867));
#175344=CARTESIAN_POINT('Ctrl Pts',(-22.8623485231606,68.0913006755297,
83.1124533420822));
#175345=CARTESIAN_POINT('Ctrl Pts',(-22.8531101847616,67.7703796652923,
82.885821448698));
#175346=CARTESIAN_POINT('Ctrl Pts',(-22.8249319472578,66.8220873124818,
82.1453693358333));
#175347=CARTESIAN_POINT('Ctrl Pts',(-22.8062649784837,66.2343545239643,
81.5844021538354));
#175348=CARTESIAN_POINT('Ctrl Pts',(-22.772514657242,65.2975885592793,80.4935127700809));
#175349=CARTESIAN_POINT('Ctrl Pts',(-22.7577467471229,64.9260065200069,
79.986804823199));
#175350=CARTESIAN_POINT('Ctrl Pts',(-22.7241964292437,64.1672401178712,
78.7656014122186));
#175351=CARTESIAN_POINT('Ctrl Pts',(-22.705439963898,63.808944887396,78.0365987554647));
#175352=CARTESIAN_POINT('Ctrl Pts',(-22.6677622618039,63.2480161277709,
76.5357888114333));
#175353=CARTESIAN_POINT('Ctrl Pts',(-22.6493118745897,63.0433526965446,
75.7688555730252));
#175354=CARTESIAN_POINT('Ctrl Pts',(-22.6123430726462,62.784051079789,74.2008677874072));
#175355=CARTESIAN_POINT('Ctrl Pts',(-22.5935539315486,62.7310754699687,
73.4033577197027));
#175356=CARTESIAN_POINT('Ctrl Pts',(-22.5559060724289,62.781283068323,71.7962247618505));
#175357=CARTESIAN_POINT('Ctrl Pts',(-22.5372356107837,62.8869387764042,
70.990580215964));
#175358=CARTESIAN_POINT('Ctrl Pts',(-22.5087256307091,63.1632579992058,
69.8081608861876));
#175359=CARTESIAN_POINT('Ctrl Pts',(-22.4992183387842,63.2745084341583,
69.4198078208809));
#175360=CARTESIAN_POINT('Ctrl Pts',(-22.4707616900542,63.6660156724947,
68.2708918550354));
#175361=CARTESIAN_POINT('Ctrl Pts',(-22.4521007963699,64.0027134346281,
67.5319316564175));
#175362=CARTESIAN_POINT('Ctrl Pts',(-22.4221282699137,64.6454425721158,
66.4264747920951));
#175363=CARTESIAN_POINT('Ctrl Pts',(-22.4110817102931,64.9040650358912,
66.0351678654252));
#175364=CARTESIAN_POINT('Ctrl Pts',(-22.3811040731956,65.6691619197105,
65.0105288885819));
#175365=CARTESIAN_POINT('Ctrl Pts',(-22.3624431202076,66.2170498682182,
64.4110947555521));
#175366=CARTESIAN_POINT('Ctrl Pts',(-22.3322146846502,67.1769138921836,
63.5500541139756));
#175367=CARTESIAN_POINT('Ctrl Pts',(-22.3209160929939,67.5522257861086,
63.2511818551385));
#175368=CARTESIAN_POINT('Ctrl Pts',(-22.2906934185333,68.6064343357118,
62.508367425302));
#175369=CARTESIAN_POINT('Ctrl Pts',(-22.2720314700177,69.3134571007556,
62.1085285853074));
#175370=CARTESIAN_POINT('Ctrl Pts',(-22.2407773987685,70.532645300244,61.5705672310305));
#175371=CARTESIAN_POINT('Ctrl Pts',(-22.2284680414892,71.0235294802595,
61.3904833254764));
#175372=CARTESIAN_POINT('Ctrl Pts',(-22.197269485049,72.3017101128349,61.0122943939119));
#175373=CARTESIAN_POINT('Ctrl Pts',(-22.1785935328695,73.0999239393653,
60.8600268606802));
#175374=CARTESIAN_POINT('Ctrl Pts',(-22.1504170890603,74.2948041261042,
60.7530176446002));
#175375=CARTESIAN_POINT('Ctrl Pts',(-22.1412575001515,74.6837354561053,
60.7367942227941));
#175376=CARTESIAN_POINT('Ctrl Pts',(-22.1131454851736,75.8828449525262,
60.7439182963387));
#175377=CARTESIAN_POINT('Ctrl Pts',(-22.0944845789022,76.6904385687269,
60.8290724566312));
#175378=CARTESIAN_POINT('Ctrl Pts',(-22.0644079776263,77.9468822684201,
61.0892202410691));
#175379=CARTESIAN_POINT('Ctrl Pts',(-22.0532589317533,78.4041274143085,
61.2118711536342));
#175380=CARTESIAN_POINT('Ctrl Pts',(-22.0231815612751,79.6221848193041,
61.6154867007138));
#175381=CARTESIAN_POINT('Ctrl Pts',(-22.0045203442948,80.3640608371865,
61.945985284902));
#175382=CARTESIAN_POINT('Ctrl Pts',(-21.9738909404253,81.4988620635565,
62.5930511504154));
#175383=CARTESIAN_POINT('Ctrl Pts',(-21.9621972881698,81.9145368779402,
62.8647675968961));
#175384=CARTESIAN_POINT('Ctrl Pts',(-21.9315920193264,82.9627916328812,
63.6447323820389));
#175385=CARTESIAN_POINT('Ctrl Pts',(-21.9129263876182,83.5633824444697,
64.1918557313839));
#175386=CARTESIAN_POINT('Ctrl Pts',(-21.8797508772358,84.5090247055591,
65.2426144734212));
#175387=CARTESIAN_POINT('Ctrl Pts',(-21.8655483736077,84.8788580692846,
65.7201554167352));
#175388=CARTESIAN_POINT('Ctrl Pts',(-21.8325390794003,85.6596290684338,
66.898600115335));
#175389=CARTESIAN_POINT('Ctrl Pts',(-21.8138060932651,86.0391010609107,
67.6169660992002));
#175390=CARTESIAN_POINT('Ctrl Pts',(-21.7762304371996,86.6419396418536,
69.0968546758051));
#175391=CARTESIAN_POINT('Ctrl Pts',(-21.7578527532016,86.8680156369997,
69.8531430322923));
#175392=CARTESIAN_POINT('Ctrl Pts',(-21.7210286054322,87.1734415483734,
71.4067543125131));
#175393=CARTESIAN_POINT('Ctrl Pts',(-21.7023040011737,87.2504951157242,
72.2007313623139));
#175394=CARTESIAN_POINT('Ctrl Pts',(-21.6646685076583,87.2494910342737,
73.8068600343059));
#175395=CARTESIAN_POINT('Ctrl Pts',(-21.646005872562,87.1685851536727,74.6151245877216));
#175396=CARTESIAN_POINT('Ctrl Pts',(-21.6143142329042,86.9016250375725,
75.9395158528669));
#175397=CARTESIAN_POINT('Ctrl Pts',(-21.6015735042928,86.7598021247821,
76.4619185572941));
#175398=CARTESIAN_POINT('Ctrl Pts',(-21.5699607729825,86.3202589225274,
77.7398285391198));
#175399=CARTESIAN_POINT('Ctrl Pts',(-21.5512745108845,85.98114122429,78.4783539511488));
#175400=CARTESIAN_POINT('Ctrl Pts',(-21.5230340597457,85.3739164593992,
79.5155579927865));
#175401=CARTESIAN_POINT('Ctrl Pts',(-21.5138267781192,85.1602057794428,
79.8435057235982));
#175402=CARTESIAN_POINT('Ctrl Pts',(-21.4856735614721,84.4567546946394,
80.8176150508236));
#175403=CARTESIAN_POINT('Ctrl Pts',(-21.4670104272666,83.9183223689934,
81.4258722644299));
#175404=CARTESIAN_POINT('Ctrl Pts',(-21.4350379002795,82.9184112585684,
82.3519309510348));
#175405=CARTESIAN_POINT('Ctrl Pts',(-21.4220203126617,82.488095121459,82.6995133893867));
#175406=CARTESIAN_POINT('Ctrl Pts',(-21.3901421683619,81.3721585820072,
83.4824731299147));
#175407=CARTESIAN_POINT('Ctrl Pts',(-21.3714481011795,80.6639444453159,
83.8810625691443));
#175408=CARTESIAN_POINT('Ctrl Pts',(-21.3431722529523,79.5621920905754,
84.364429515229));
#175409=CARTESIAN_POINT('Ctrl Pts',(-21.3339383729774,79.1954466615754,
84.5047366456281));
#175410=CARTESIAN_POINT('Ctrl Pts',(-21.3057636184893,78.0526067978761,
84.8801022401905));
#175411=CARTESIAN_POINT('Ctrl Pts',(-21.2870973434153,77.2594137432834,
85.0559685801673));
#175412=CARTESIAN_POINT('Ctrl Pts',(-21.2566621730713,75.9718283819674,
85.2099586950105));
#175413=CARTESIAN_POINT('Ctrl Pts',(-21.2452100806794,75.4860727952401,
85.2388893847883));
#175414=CARTESIAN_POINT('Ctrl Pts',(-21.2338306951809,75.0000000451541,
85.23888938658));
#175415=CARTESIAN_POINT('Ctrl Pts',(-21.9012048916249,75.,85.23888938658));
#175416=CARTESIAN_POINT('Ctrl Pts',(-21.912586321363,75.4888884534696,85.23888938658));
#175417=CARTESIAN_POINT('Ctrl Pts',(-21.9239205229409,75.9776271232784,
85.2096225450995));
#175418=CARTESIAN_POINT('Ctrl Pts',(-21.9478961821272,76.9924718404084,
85.0874979530066));
#175419=CARTESIAN_POINT('Ctrl Pts',(-21.9604488578908,77.5166460610561,
84.9894213843955));
#175420=CARTESIAN_POINT('Ctrl Pts',(-21.9918811638311,78.8181833158265,
84.6568425582864));
#175421=CARTESIAN_POINT('Ctrl Pts',(-22.0105626377578,79.5817381472458,
84.3786799766011));
#175422=CARTESIAN_POINT('Ctrl Pts',(-22.0387765318448,80.6638973212022,
83.8578868167239));
#175423=CARTESIAN_POINT('Ctrl Pts',(-22.047963967763,81.007304699502,83.6719193403085));
#175424=CARTESIAN_POINT('Ctrl Pts',(-22.0761003861245,82.0344804774716,
83.0504535172506));
#175425=CARTESIAN_POINT('Ctrl Pts',(-22.0947621134101,82.6843931620147,
82.5632869565897));
#175426=CARTESIAN_POINT('Ctrl Pts',(-22.1258540645354,83.6613163762424,
81.6670157259261));
#175427=CARTESIAN_POINT('Ctrl Pts',(-22.1380036120981,84.0188201814993,
81.2948608886773));
#175428=CARTESIAN_POINT('Ctrl Pts',(-22.1690484562985,84.8753753289718,
80.2824828351675));
#175429=CARTESIAN_POINT('Ctrl Pts',(-22.187721216155,85.3362271984165,79.6132346325209));
#175430=CARTESIAN_POINT('Ctrl Pts',(-22.2237942094955,86.0779072546758,
78.2679920585282));
#175431=CARTESIAN_POINT('Ctrl Pts',(-22.2408382490607,86.3710832047136,
77.6027196336544));
#175432=CARTESIAN_POINT('Ctrl Pts',(-22.2668498050486,86.729151558269,76.544560108793));
#175433=CARTESIAN_POINT('Ctrl Pts',(-22.2759272013247,86.836795687971,76.1678919732641));
#175434=CARTESIAN_POINT('Ctrl Pts',(-22.3033834381558,87.105287081249,75.023402150957));
#175435=CARTESIAN_POINT('Ctrl Pts',(-22.3218965085367,87.2106624127075,
74.2446545384812));
#175436=CARTESIAN_POINT('Ctrl Pts',(-22.3577323383323,87.269894669926,72.7095136457393));
#175437=CARTESIAN_POINT('Ctrl Pts',(-22.3751417675776,87.2295980158523,
71.9567578392927));
#175438=CARTESIAN_POINT('Ctrl Pts',(-22.4113116058556,87.0065321938148,
70.4347788507262));
#175439=CARTESIAN_POINT('Ctrl Pts',(-22.429662439971,86.8179661250924,69.6698563217369));
#175440=CARTESIAN_POINT('Ctrl Pts',(-22.4664299287135,86.2939170618744,
68.1782892826909));
#175441=CARTESIAN_POINT('Ctrl Pts',(-22.4851244804542,85.9580308520165,
67.4557177032548));
#175442=CARTESIAN_POINT('Ctrl Pts',(-22.5227458722235,85.1432600648163,
66.0727335883611));
#175443=CARTESIAN_POINT('Ctrl Pts',(-22.5414073161341,84.6637588863931,
65.4171855764211));
#175444=CARTESIAN_POINT('Ctrl Pts',(-22.5722643028744,83.7855937627976,
64.4371902879453));
#175445=CARTESIAN_POINT('Ctrl Pts',(-22.5841822499176,83.4251278384314,
64.0818451042407));
#175446=CARTESIAN_POINT('Ctrl Pts',(-22.6150040070451,82.4324300019875,
63.2175829726687));
#175447=CARTESIAN_POINT('Ctrl Pts',(-22.6336727732604,81.7698128061756,
62.7473524548337));
#175448=CARTESIAN_POINT('Ctrl Pts',(-22.6681615035931,80.4934350204194,
62.0199139796853));
#175449=CARTESIAN_POINT('Ctrl Pts',(-22.683654689078,79.8958711362499,61.74048052583));
#175450=CARTESIAN_POINT('Ctrl Pts',(-22.7168617911713,78.5614370104438,
61.243051738332));
#175451=CARTESIAN_POINT('Ctrl Pts',(-22.7346003127391,77.8206366530425,
61.0434910778566));
#175452=CARTESIAN_POINT('Ctrl Pts',(-22.7712051161519,76.2863466356868,
60.7809578982311));
#175453=CARTESIAN_POINT('Ctrl Pts',(-22.7896421665589,75.4955214493371,
60.723379044344));
#175454=CARTESIAN_POINT('Ctrl Pts',(-22.8265862691434,73.9076783255466,
60.7616688154799));
#175455=CARTESIAN_POINT('Ctrl Pts',(-22.8453667500809,73.1144494904388,
60.8586469249961));
#175456=CARTESIAN_POINT('Ctrl Pts',(-22.883016901072,71.5451717287155,61.208244562513));
#175457=CARTESIAN_POINT('Ctrl Pts',(-22.9016852345603,70.7734956343306,
61.462567723342));
#175458=CARTESIAN_POINT('Ctrl Pts',(-22.9359987009992,69.4373570739347,
62.0552916966354));
#175459=CARTESIAN_POINT('Ctrl Pts',(-22.9513198607114,68.8641024388829,
62.3663980635183));
#175460=CARTESIAN_POINT('Ctrl Pts',(-22.9843524361103,67.6769570109697,
63.1389623386834));
#175461=CARTESIAN_POINT('Ctrl Pts',(-23.0020747944056,67.0761284594397,
63.6155080452088));
#175462=CARTESIAN_POINT('Ctrl Pts',(-23.0386402328967,65.9535390102774,
64.6914355274705));
#175463=CARTESIAN_POINT('Ctrl Pts',(-23.057055786477,65.4375575413906,65.2917536735474));
#175464=CARTESIAN_POINT('Ctrl Pts',(-23.0939578118267,64.5242824656047,
66.5891391158697));
#175465=CARTESIAN_POINT('Ctrl Pts',(-23.1127205262052,64.1302740978057,
67.2839342198859));
#175466=CARTESIAN_POINT('Ctrl Pts',(-23.150369023893,63.4772774808831,68.7525951946088));
#175467=CARTESIAN_POINT('Ctrl Pts',(-23.1690346957872,63.222317781978,69.5239905982264));
#175468=CARTESIAN_POINT('Ctrl Pts',(-23.202227942829,62.9135806669705,70.9042560445563));
#175469=CARTESIAN_POINT('Ctrl Pts',(-23.216447902048,62.8255154532279,71.5025654295138));
#175470=CARTESIAN_POINT('Ctrl Pts',(-23.2494737518504,62.7234541939232,
72.9132411431064));
#175471=CARTESIAN_POINT('Ctrl Pts',(-23.2682072921613,62.7453318376152,
73.7253705764239));
#175472=CARTESIAN_POINT('Ctrl Pts',(-23.3057864814918,62.9462990163618,
75.3107912865271));
#175473=CARTESIAN_POINT('Ctrl Pts',(-23.3241668488167,63.1204905522849,
76.0808464733005));
#175474=CARTESIAN_POINT('Ctrl Pts',(-23.3609966120288,63.616888236998,77.5846186867617));
#175475=CARTESIAN_POINT('Ctrl Pts',(-23.3797241105354,63.9394396058289,
78.3142962358958));
#175476=CARTESIAN_POINT('Ctrl Pts',(-23.4173608291487,64.7286015836965,
79.7132850820113));
#175477=CARTESIAN_POINT('Ctrl Pts',(-23.4360236235025,65.1957736412047,
80.3778180926077));
#175478=CARTESIAN_POINT('Ctrl Pts',(-23.4678074493266,66.0808862600834,
81.4036674680061));
#175479=CARTESIAN_POINT('Ctrl Pts',(-23.4806390461079,66.4637486534798,
81.7918147908507));
#175480=CARTESIAN_POINT('Ctrl Pts',(-23.5123389224929,67.4776347598111,
82.6911425165524));
#175481=CARTESIAN_POINT('Ctrl Pts',(-23.5310276517792,68.1360094350865,
83.167559580311));
#175482=CARTESIAN_POINT('Ctrl Pts',(-23.5592802040287,69.1750490493099,
83.7724796465241));
#175483=CARTESIAN_POINT('Ctrl Pts',(-23.5684965578351,69.5227521303402,
83.9531781953693));
#175484=CARTESIAN_POINT('Ctrl Pts',(-23.5966572561651,70.6146745287655,
84.4557174583123));
#175485=CARTESIAN_POINT('Ctrl Pts',(-23.6153212874812,71.3826421586133,
84.7206389130407));
#175486=CARTESIAN_POINT('Ctrl Pts',(-23.647754008211,72.7275538437635,85.0398455494248));
#175487=CARTESIAN_POINT('Ctrl Pts',(-23.6612250736101,73.2925523801279,
85.1327842323363));
#175488=CARTESIAN_POINT('Ctrl Pts',(-23.6834766321493,74.240518326684,85.2212331412086));
#175489=CARTESIAN_POINT('Ctrl Pts',(-23.6923070761891,74.6202726623436,
85.23888938658));
#175490=CARTESIAN_POINT('Ctrl Pts',(-23.7011390782975,75.,85.23888938658));
#175491=CARTESIAN_POINT('Origin',(-30.2175364832709,75.,72.98888938658));
#175492=CARTESIAN_POINT('',(-25.5022222452499,75.,85.23888938658));
#175493=CARTESIAN_POINT('',(-24.833932583624,74.9999999810258,85.23888938658));
#175494=CARTESIAN_POINT('',(-30.2175364832709,75.,85.23888938658));
#175495=CARTESIAN_POINT('Ctrl Pts',(-24.83393258407,74.9999999810153,85.23888938658));
#175496=CARTESIAN_POINT('Ctrl Pts',(-24.8330121802999,74.960857355121,85.2388893865193));
#175497=CARTESIAN_POINT('Ctrl Pts',(-24.8320915953716,74.9217106155544,
85.2387017768826));
#175498=CARTESIAN_POINT('Ctrl Pts',(-24.8127288074479,74.0983640523228,
85.2308081150725));
#175499=CARTESIAN_POINT('Ctrl Pts',(-24.7944554783897,73.3166959232225,
85.1480018195794));
#175500=CARTESIAN_POINT('Ctrl Pts',(-24.7588414083011,71.8165776073276,
84.8415734427302));
#175501=CARTESIAN_POINT('Ctrl Pts',(-24.7412594202536,71.1000320551724,
84.6254928687546));
#175502=CARTESIAN_POINT('Ctrl Pts',(-24.70501977218,69.6668392301149,84.0459427716953));
#175503=CARTESIAN_POINT('Ctrl Pts',(-24.6866087150995,68.9571207409134,
83.6746107660014));
#175504=CARTESIAN_POINT('Ctrl Pts',(-24.6587121174065,67.9612855727158,
83.0224389804367));
#175505=CARTESIAN_POINT('Ctrl Pts',(-24.6494928561014,67.6443946644282,
82.792495280465));
#175506=CARTESIAN_POINT('Ctrl Pts',(-24.6236449432613,66.7853464856481,
82.1040135503076));
#175507=CARTESIAN_POINT('Ctrl Pts',(-24.607195609566,66.2712438558182,81.6129741337991));
#175508=CARTESIAN_POINT('Ctrl Pts',(-24.5717868012854,65.2671534027392,
80.4716175012459));
#175509=CARTESIAN_POINT('Ctrl Pts',(-24.5526390934194,64.7934848457995,
79.8113939098884));
#175510=CARTESIAN_POINT('Ctrl Pts',(-24.5245074450009,64.1917606340085,
78.7681225330309));
#175511=CARTESIAN_POINT('Ctrl Pts',(-24.5153625937877,64.011575983453,78.4177117221588));
#175512=CARTESIAN_POINT('Ctrl Pts',(-24.4873393741456,63.5130408309317,
77.321262500087));
#175513=CARTESIAN_POINT('Ctrl Pts',(-24.4682185600995,63.2515827525554,
76.5518058783384));
#175514=CARTESIAN_POINT('Ctrl Pts',(-24.4359839844773,62.9396546659635,
75.2097537695167));
#175515=CARTESIAN_POINT('Ctrl Pts',(-24.4228498483481,62.8497751980916,
74.6490715313364));
#175516=CARTESIAN_POINT('Ctrl Pts',(-24.3907371325704,62.7266073101506,
73.2770561846433));
#175517=CARTESIAN_POINT('Ctrl Pts',(-24.3715910967796,62.7344196684428,
72.4647268153079));
#175518=CARTESIAN_POINT('Ctrl Pts',(-24.3412584919897,62.8754832630862,
71.1728903525902));
#175519=CARTESIAN_POINT('Ctrl Pts',(-24.3299297831827,62.9576560108063,
70.6902574351304));
#175520=CARTESIAN_POINT('Ctrl Pts',(-24.3093242695386,63.157743835355,69.8299664364236));
#175521=CARTESIAN_POINT('Ctrl Pts',(-24.3000501342154,63.2654969868885,
69.4506324720218));
#175522=CARTESIAN_POINT('Ctrl Pts',(-24.2697702028235,63.6767577691774,
68.2301547070909));
#175523=CARTESIAN_POINT('Ctrl Pts',(-24.2490918108296,64.0540125958005,
67.4169304399856));
#175524=CARTESIAN_POINT('Ctrl Pts',(-24.2093264662316,64.9353771546991,
65.9588136368118));
#175525=CARTESIAN_POINT('Ctrl Pts',(-24.1901958334356,65.4221086084808,
65.3088765046616));
#175526=CARTESIAN_POINT('Ctrl Pts',(-24.1605297197393,66.2815503642943,
64.3712018079504));
#175527=CARTESIAN_POINT('Ctrl Pts',(-24.1498287435204,66.6127000649262,
64.0485816731829));
#175528=CARTESIAN_POINT('Ctrl Pts',(-24.1201442699103,67.5724993407992,
63.2138761227789));
#175529=CARTESIAN_POINT('Ctrl Pts',(-24.1010120245648,68.2349415319324,
62.7442499488733));
#175530=CARTESIAN_POINT('Ctrl Pts',(-24.0727021089201,69.289701565734,62.1437073689938));
#175531=CARTESIAN_POINT('Ctrl Pts',(-24.0633386197286,69.6501906439882,
61.9614227308088));
#175532=CARTESIAN_POINT('Ctrl Pts',(-24.0350509998723,70.7595284257385,
61.467697073355));
#175533=CARTESIAN_POINT('Ctrl Pts',(-24.0159028058597,71.5309199688538,
61.2124318421222));
#175534=CARTESIAN_POINT('Ctrl Pts',(-23.9783515037176,73.0999023173503,
60.8609100051232));
#175535=CARTESIAN_POINT('Ctrl Pts',(-23.9599309020457,73.8931184972221,
60.7629715970578));
#175536=CARTESIAN_POINT('Ctrl Pts',(-23.9225709853616,75.4815689532512,
60.722787721409));
#175537=CARTESIAN_POINT('Ctrl Pts',(-23.904081555327,76.2730173676356,60.779524382697));
#175538=CARTESIAN_POINT('Ctrl Pts',(-23.8678634362634,77.8083196437933,
61.0405773617241));
#175539=CARTESIAN_POINT('Ctrl Pts',(-23.8498714208046,78.5495039887092,
61.2394283831196));
#175540=CARTESIAN_POINT('Ctrl Pts',(-23.8163855339271,79.8877636465009,
61.7367574745244));
#175541=CARTESIAN_POINT('Ctrl Pts',(-23.8010478112739,80.4885605653581,
62.0172710457133));
#175542=CARTESIAN_POINT('Ctrl Pts',(-23.7667417987372,81.7680023894197,
62.7461556850651));
#175543=CARTESIAN_POINT('Ctrl Pts',(-23.7475935338195,82.4307052325513,
63.2162711595252));
#175544=CARTESIAN_POINT('Ctrl Pts',(-23.7168433096365,83.4239619206798,
64.08071189901));
#175545=CARTESIAN_POINT('Ctrl Pts',(-23.7051198335117,83.7848512030601,
64.4363956576645));
#175546=CARTESIAN_POINT('Ctrl Pts',(-23.6744145331563,84.6634205510409,
65.4167535831173));
#175547=CARTESIAN_POINT('Ctrl Pts',(-23.6552742920802,85.1429519640128,
66.0722815645031));
#175548=CARTESIAN_POINT('Ctrl Pts',(-23.6272695660277,85.7522480813967,
67.1063898850051));
#175549=CARTESIAN_POINT('Ctrl Pts',(-23.6182185523546,85.9340885984846,
67.4517108876169));
#175550=CARTESIAN_POINT('Ctrl Pts',(-23.590263874454,86.4421807057408,68.539603470355));
#175551=CARTESIAN_POINT('Ctrl Pts',(-23.5711206896711,86.7114636581776,
69.3063279237869));
#175552=CARTESIAN_POINT('Ctrl Pts',(-23.5397769471509,87.0284096400574,
70.6095314041081));
#175553=CARTESIAN_POINT('Ctrl Pts',(-23.5274907470146,87.1201638457728,
71.1326538507386));
#175554=CARTESIAN_POINT('Ctrl Pts',(-23.4962238131374,87.2656105445745,
72.4655747094982));
#175555=CARTESIAN_POINT('Ctrl Pts',(-23.4770806724929,87.2733688763959,
73.277812894189));
#175556=CARTESIAN_POINT('Ctrl Pts',(-23.4490546123071,87.1659225412469,
74.4739710096168));
#175557=CARTESIAN_POINT('Ctrl Pts',(-23.4399878465529,87.1123736033312,
74.8611993165106));
#175558=CARTESIAN_POINT('Ctrl Pts',(-23.4145770368626,86.911318144442,75.9340947150916));
#175559=CARTESIAN_POINT('Ctrl Pts',(-23.3980458367828,86.7233398203084,
76.6106336928983));
#175560=CARTESIAN_POINT('Ctrl Pts',(-23.367041637428,86.2611951901439,77.8505006464516));
#175561=CARTESIAN_POINT('Ctrl Pts',(-23.3526269177924,85.9997219403267,
78.416218202404));
#175562=CARTESIAN_POINT('Ctrl Pts',(-23.3192385975873,85.3013701666968,
79.6672979462397));
#175563=CARTESIAN_POINT('Ctrl Pts',(-23.300090573773,84.8370828892794,80.3340351514571));
#175564=CARTESIAN_POINT('Ctrl Pts',(-23.2695021498846,83.9856822909245,
81.3297294986452));
#175565=CARTESIAN_POINT('Ctrl Pts',(-23.2579317490028,83.6380738197449,
81.6892215484255));
#175566=CARTESIAN_POINT('Ctrl Pts',(-23.2273792588619,82.6717641973288,
82.5734047131662));
#175567=CARTESIAN_POINT('Ctrl Pts',(-23.2082399709085,82.0212544609202,
83.0596831454881));
#175568=CARTESIAN_POINT('Ctrl Pts',(-23.1802414685338,80.9936912667864,
83.6795469027744));
#175569=CARTESIAN_POINT('Ctrl Pts',(-23.1711950484374,80.650441193471,83.8648724434101));
#175570=CARTESIAN_POINT('Ctrl Pts',(-23.1432437850686,79.5680658267244,
84.3841695874317));
#175571=CARTESIAN_POINT('Ctrl Pts',(-23.1241000139813,78.8041887715563,
84.6614118051235));
#175572=CARTESIAN_POINT('Ctrl Pts',(-23.092794553374,77.5058799785268,84.9915092788248));
#175573=CARTESIAN_POINT('Ctrl Pts',(-23.0805447012976,76.9853079426462,
85.0885121181525));
#175574=CARTESIAN_POINT('Ctrl Pts',(-23.0568225823766,75.9752893647638,
85.2097625158968));
#175575=CARTESIAN_POINT('Ctrl Pts',(-23.0453237417114,75.4877187316448,
85.23888938658));
#175576=CARTESIAN_POINT('Ctrl Pts',(-23.0338668482845,75.,85.23888938658));
#175577=CARTESIAN_POINT('',(-24.5014289287959,79.1898481021894,61.4773919099605));
#175578=CARTESIAN_POINT('Ctrl Pts',(-23.7011390782975,75.,85.23888938658));
#175579=CARTESIAN_POINT('Ctrl Pts',(-23.711138974241,75.4299403257455,85.23888938658));
#175580=CARTESIAN_POINT('Ctrl Pts',(-23.7211834578993,75.8598450501858,
85.2162549034665));
#175581=CARTESIAN_POINT('Ctrl Pts',(-23.7405701053338,76.67993557658,85.1295527181096));
#175582=CARTESIAN_POINT('Ctrl Pts',(-23.7498409659175,77.0697177426204,
85.069210539615));
#175583=CARTESIAN_POINT('Ctrl Pts',(-23.7780432552013,78.2500489799088,
84.8276708580129));
#175584=CARTESIAN_POINT('Ctrl Pts',(-23.7967172116631,79.0260974340909,
84.5867384923059));
#175585=CARTESIAN_POINT('Ctrl Pts',(-23.8246735716932,80.122456630624,84.1229455851328));
#175586=CARTESIAN_POINT('Ctrl Pts',(-23.8336166228644,80.4652004592394,
83.9587733355535));
#175587=CARTESIAN_POINT('Ctrl Pts',(-23.8609478396887,81.4917762273504,
83.4069786330634));
#175588=CARTESIAN_POINT('Ctrl Pts',(-23.8790634001258,82.1464024477594,
82.9693036849566));
#175589=CARTESIAN_POINT('Ctrl Pts',(-23.9138127481122,83.2956582429748,
82.0295234357861));
#175590=CARTESIAN_POINT('Ctrl Pts',(-23.9302990833014,83.7978674253144,
81.5415816859414));
#175591=CARTESIAN_POINT('Ctrl Pts',(-23.9655267975286,84.7864708438371,
80.4013076184334));
#175592=CARTESIAN_POINT('Ctrl Pts',(-23.9842685146157,85.2551783471532,
79.7379833250757));
#175593=CARTESIAN_POINT('Ctrl Pts',(-24.0218991260129,86.0447596067269,
78.3461182380094));
#175594=CARTESIAN_POINT('Ctrl Pts',(-24.0403190708493,86.3671820510835,
77.622871999162));
#175595=CARTESIAN_POINT('Ctrl Pts',(-24.0772298684548,86.8704400366199,
76.1178293978822));
#175596=CARTESIAN_POINT('Ctrl Pts',(-24.0959965207465,87.0488096300684,
75.339164270484));
#175597=CARTESIAN_POINT('Ctrl Pts',(-24.1336458027265,87.2534837979751,
73.7448529145002));
#175598=CARTESIAN_POINT('Ctrl Pts',(-24.1523119534404,87.2766522964618,
72.9327309876617));
#175599=CARTESIAN_POINT('Ctrl Pts',(-24.1857152921631,87.1762002643047,
71.513031033439));
#175600=CARTESIAN_POINT('Ctrl Pts',(-24.2001420143546,87.0871443185291,
70.9058728992067));
#175601=CARTESIAN_POINT('Ctrl Pts',(-24.2333633595733,86.7756987037478,
69.5172928243099));
#175602=CARTESIAN_POINT('Ctrl Pts',(-24.252103018098,86.5203555977892,68.7461937853734));
#175603=CARTESIAN_POINT('Ctrl Pts',(-24.2897205685122,85.8696587461812,
67.2848420936276));
#175604=CARTESIAN_POINT('Ctrl Pts',(-24.3081302371888,85.4796044106335,
66.59643013653));
#175605=CARTESIAN_POINT('Ctrl Pts',(-24.3555502304331,84.3081294375343,
64.9277245171954));
#175606=CARTESIAN_POINT('Ctrl Pts',(-24.3849309971721,83.4379723911377,
64.020931329993));
#175607=CARTESIAN_POINT('Ctrl Pts',(-24.4429386257001,81.4573944055484,
62.5049048593974));
#175608=CARTESIAN_POINT('Ctrl Pts',(-24.4722171551946,80.3594150263118,
61.9033791425484));
#175609=CARTESIAN_POINT('Ctrl Pts',(-24.5011646348533,79.1897461138953,
61.4776545483405));
#175610=CARTESIAN_POINT('Ctrl Pts',(-24.5020520203782,79.1897645405808,
61.477661255121));
#175611=CARTESIAN_POINT('Ctrl Pts',(-24.5125418046939,78.7623268423097,
61.322085908071));
#175612=CARTESIAN_POINT('Ctrl Pts',(-24.5228906675777,78.3265556311944,
61.1904388306657));
#175613=CARTESIAN_POINT('Ctrl Pts',(-24.5424644562946,77.4947744517867,
60.9889151848011));
#175614=CARTESIAN_POINT('Ctrl Pts',(-24.5516792289608,77.1006806111332,
60.9136907674308));
#175615=CARTESIAN_POINT('Ctrl Pts',(-24.5778835211609,76.0002940361128,
60.7591588247104));
#175616=CARTESIAN_POINT('Ctrl Pts',(-24.5951014639648,75.2897265319481,
60.7217394633869));
#175617=CARTESIAN_POINT('Ctrl Pts',(-24.6329131207955,73.6976368691199,
60.7763670271403));
#175618=CARTESIAN_POINT('Ctrl Pts',(-24.6531206325569,72.8212005650578,
60.9019251752237));
#175619=CARTESIAN_POINT('Ctrl Pts',(-24.6861647868287,71.4173086727461,
61.2608277090111));
#175620=CARTESIAN_POINT('Ctrl Pts',(-24.6991435803042,70.8791242303854,
61.4389330517108));
#175621=CARTESIAN_POINT('Ctrl Pts',(-24.7290959930944,69.7115537195404,
61.9173650258494));
#175622=CARTESIAN_POINT('Ctrl Pts',(-24.7459006918793,69.0915542528856,
62.2354434946132));
#175623=CARTESIAN_POINT('Ctrl Pts',(-24.7807577979218,67.8410241662928,
63.0179642747568));
#175624=CARTESIAN_POINT('Ctrl Pts',(-24.7986082540868,67.2211292125195,
63.4936555520269));
#175625=CARTESIAN_POINT('Ctrl Pts',(-24.8299852249833,66.2150337533001,
64.4307781454737));
#175626=CARTESIAN_POINT('Ctrl Pts',(-24.8436259496644,65.8095810325872,
64.8677380032304));
#175627=CARTESIAN_POINT('Ctrl Pts',(-24.8655811323225,65.2321081959332,
65.5889718544895));
#175628=CARTESIAN_POINT('Ctrl Pts',(-24.8734682389785,65.0371225598899,
65.8536555248908));
#175629=CARTESIAN_POINT('Ctrl Pts',(-24.8988885544839,64.4425285237137,
66.7327620601062));
#175630=CARTESIAN_POINT('Ctrl Pts',(-24.916225865812,64.0873129039124,67.3752791692422));
#175631=CARTESIAN_POINT('Ctrl Pts',(-24.9445693940492,63.5922400120015,
68.4978200978249));
#175632=CARTESIAN_POINT('Ctrl Pts',(-24.9557990219495,63.4203753776834,
68.9616091579511));
#175633=CARTESIAN_POINT('Ctrl Pts',(-24.991191551118,62.9707920372626,70.4444184105539));
#175634=CARTESIAN_POINT('Ctrl Pts',(-25.0165149476227,62.7963775809172,
71.4896608629926));
#175635=CARTESIAN_POINT('Ctrl Pts',(-25.0605993053149,62.7291359905145,
73.3408964512946));
#175636=CARTESIAN_POINT('Ctrl Pts',(-25.0790518804435,62.7780339324203,
74.1384901465993));
#175637=CARTESIAN_POINT('Ctrl Pts',(-25.1145026886564,63.0234223963534,
75.6710346121499));
#175638=CARTESIAN_POINT('Ctrl Pts',(-25.1316616917218,63.2114049355636,
76.4037603153742));
#175639=CARTESIAN_POINT('Ctrl Pts',(-25.1656894913147,63.6926489417875,
77.7492126837831));
#175640=CARTESIAN_POINT('Ctrl Pts',(-25.1819489843272,63.9716683124179,
78.3640898425759));
#175641=CARTESIAN_POINT('Ctrl Pts',(-25.216118304735,64.6766406413764,79.6288984702076));
#175642=CARTESIAN_POINT('Ctrl Pts',(-25.2338084321378,65.1166502414938,
80.2676859027829));
#175643=CARTESIAN_POINT('Ctrl Pts',(-25.2642361424389,65.9735515230226,
81.2894217431666));
#175644=CARTESIAN_POINT('Ctrl Pts',(-25.2770595146836,66.3620685198686,
81.6930119904588));
#175645=CARTESIAN_POINT('Ctrl Pts',(-25.3068814134131,67.2935598837059,
82.5366283717952));
#175646=CARTESIAN_POINT('Ctrl Pts',(-25.323733229335,67.8493112143265,82.9596567953659));
#175647=CARTESIAN_POINT('Ctrl Pts',(-25.3586951911263,69.0981345086375,
83.7518620114951));
#175648=CARTESIAN_POINT('Ctrl Pts',(-25.376601320342,69.7968141874185,84.1064641152546));
#175649=CARTESIAN_POINT('Ctrl Pts',(-25.4075151318772,71.0581039950824,
84.6014918961754));
#175650=CARTESIAN_POINT('Ctrl Pts',(-25.4206199201852,71.6057279659652,
84.7732010160532));
#175651=CARTESIAN_POINT('Ctrl Pts',(-25.4508552603207,72.8462113482914,
85.0684748773236));
#175652=CARTESIAN_POINT('Ctrl Pts',(-25.4678284623517,73.5417624027446,
85.1720231422624));
#175653=CARTESIAN_POINT('Ctrl Pts',(-25.4904073576037,74.49471956676,85.2310757780062));
#175654=CARTESIAN_POINT('Ctrl Pts',(-25.4963391614053,74.7473913001414,
85.23888938658));
#175655=CARTESIAN_POINT('Ctrl Pts',(-25.5022222452499,75.,85.23888938658));
#175656=CARTESIAN_POINT('Origin',(-30.2175364832709,75.,72.98888938658));
#175657=CARTESIAN_POINT('',(-27.3010916068384,75.,85.23888938658));
#175658=CARTESIAN_POINT('',(-26.6339799854461,75.,85.23888938658));
#175659=CARTESIAN_POINT('',(-30.2175364832709,75.,85.23888938658));
#175660=CARTESIAN_POINT('',(-25.633313136734,79.1896865699813,61.4777794235982));
#175661=CARTESIAN_POINT('Ctrl Pts',(-26.6339799854461,75.,85.23888938658));
#175662=CARTESIAN_POINT('Ctrl Pts',(-26.6191344607835,74.3618886790399,
85.23888938658));
#175663=CARTESIAN_POINT('Ctrl Pts',(-26.6038014873088,73.7246076393242,
85.1890298360207));
#175664=CARTESIAN_POINT('Ctrl Pts',(-26.5510773887447,71.5348844170923,
84.8441233871728));
#175665=CARTESIAN_POINT('Ctrl Pts',(-26.5162064908492,70.037852256756,84.2995345304749));
#175666=CARTESIAN_POINT('Ctrl Pts',(-26.4650951800277,68.1955326183883,
83.1912671047002));
#175667=CARTESIAN_POINT('Ctrl Pts',(-26.4514103901535,67.7269049983729,
82.8626618812816));
#175668=CARTESIAN_POINT('Ctrl Pts',(-26.4174837867177,66.6092017933043,
81.9560294094145));
#175669=CARTESIAN_POINT('Ctrl Pts',(-26.397717102787,65.9954229202779,81.3394994261153));
#175670=CARTESIAN_POINT('Ctrl Pts',(-26.3402521640497,64.4294838156008,
79.3912524211144));
#175671=CARTESIAN_POINT('Ctrl Pts',(-26.3007334648626,63.6714882588937,
77.927602021171));
#175672=CARTESIAN_POINT('Ctrl Pts',(-26.2463389568543,63.0199241914413,
75.6502720141751));
#175673=CARTESIAN_POINT('Ctrl Pts',(-26.2295436540705,62.8815895363798,
74.9252011742734));
#175674=CARTESIAN_POINT('Ctrl Pts',(-26.192645675109,62.7288491446227,73.3776538367586));
#175675=CARTESIAN_POINT('Ctrl Pts',(-26.1730357227808,62.7302834796635,
72.5571854721671));
#175676=CARTESIAN_POINT('Ctrl Pts',(-26.1356161377997,62.893448701657,70.9611979077159));
#175677=CARTESIAN_POINT('Ctrl Pts',(-26.1178365708504,63.0484246652574,
70.1888978503789));
#175678=CARTESIAN_POINT('Ctrl Pts',(-26.0845253655014,63.465989093539,68.8107300743042));
#175679=CARTESIAN_POINT('Ctrl Pts',(-26.0688767706139,63.705513665866,68.2008865543368));
#175680=CARTESIAN_POINT('Ctrl Pts',(-26.0144120069597,64.7089497653021,
66.146257029447));
#175681=CARTESIAN_POINT('Ctrl Pts',(-25.978333870295,65.7113512534435,64.8373035441054));
#175682=CARTESIAN_POINT('Ctrl Pts',(-25.9261162324526,67.3661157897606,
63.3917373803513));
#175683=CARTESIAN_POINT('Ctrl Pts',(-25.9125953614106,67.816675035508,63.0500079896439));
#175684=CARTESIAN_POINT('Ctrl Pts',(-25.8784056904707,69.0294522571061,
62.2558563967337));
#175685=CARTESIAN_POINT('Ctrl Pts',(-25.8582495341768,69.8200434030659,
61.8527550487459));
#175686=CARTESIAN_POINT('Ctrl Pts',(-25.8097366834901,71.7916545355979,
61.1032577446227));
#175687=CARTESIAN_POINT('Ctrl Pts',(-25.7800416015991,72.9949463612515,
60.8422260893582));
#175688=CARTESIAN_POINT('Ctrl Pts',(-25.7334192166397,74.9862994855731,
60.7146562681797));
#175689=CARTESIAN_POINT('Ctrl Pts',(-25.7159396589751,75.7586830737479,
60.738118782859));
#175690=CARTESIAN_POINT('Ctrl Pts',(-25.6770209075191,77.4336945508136,
60.9480964001632));
#175691=CARTESIAN_POINT('Ctrl Pts',(-25.654923438463,78.3279707607524,61.1639952156199));
#175692=CARTESIAN_POINT('Ctrl Pts',(-25.6332414813969,79.189732077303,61.4776494394493));
#175693=CARTESIAN_POINT('Ctrl Pts',(-25.6339066113238,79.1897464476885,
61.4776546698313));
#175694=CARTESIAN_POINT('Ctrl Pts',(-25.6244228599011,79.5687070061174,
61.6155850215755));
#175695=CARTESIAN_POINT('Ctrl Pts',(-25.6149598570696,79.9406262882323,
61.7721452284987));
#175696=CARTESIAN_POINT('Ctrl Pts',(-25.5961845640087,80.6653410871441,
62.1202659299911));
#175697=CARTESIAN_POINT('Ctrl Pts',(-25.5868826993398,81.0178063006061,
62.3113862569872));
#175698=CARTESIAN_POINT('Ctrl Pts',(-25.5592839406543,82.0314738714595,
62.9271967218725));
#175699=CARTESIAN_POINT('Ctrl Pts',(-25.5407561921154,82.6619102834156,
63.3985604625245));
#175700=CARTESIAN_POINT('Ctrl Pts',(-25.5102264420635,83.6270429003146,
64.2764651963806));
#175701=CARTESIAN_POINT('Ctrl Pts',(-25.4981809809063,83.9886043293266,
64.6499927535362));
#175702=CARTESIAN_POINT('Ctrl Pts',(-25.470364243981,84.7633543361056,65.5595136167616));
#175703=CARTESIAN_POINT('Ctrl Pts',(-25.4544354609332,85.158065708514,66.1090341992136));
#175704=CARTESIAN_POINT('Ctrl Pts',(-25.4196190296736,85.9220036523635,
67.3828026001748));
#175705=CARTESIAN_POINT('Ctrl Pts',(-25.4009646689382,86.2686440486874,
68.1169254575523));
#175706=CARTESIAN_POINT('Ctrl Pts',(-25.3728060380299,86.6715156917527,
69.2484003154342));
#175707=CARTESIAN_POINT('Ctrl Pts',(-25.3635897704838,86.7850070930907,
69.623009846663));
#175708=CARTESIAN_POINT('Ctrl Pts',(-25.3380015362742,87.0507602419729,
70.6801890597495));
#175709=CARTESIAN_POINT('Ctrl Pts',(-25.321802762279,87.1628268943266,71.3713103111357));
#175710=CARTESIAN_POINT('Ctrl Pts',(-25.2866422182078,87.2762726975011,
72.8764725514986));
#175711=CARTESIAN_POINT('Ctrl Pts',(-25.2674943079216,87.2568201649851,
73.6887930209408));
#175712=CARTESIAN_POINT('Ctrl Pts',(-25.2393672130477,87.1089389726804,
74.8839006810161));
#175713=CARTESIAN_POINT('Ctrl Pts',(-25.2302257318265,87.041791937479,75.2720271696218));
#175714=CARTESIAN_POINT('Ctrl Pts',(-25.2022049284722,86.7795554791705,
76.4474677567833));
#175715=CARTESIAN_POINT('Ctrl Pts',(-25.1830828927367,86.5249307987711,
77.2192151133254));
#175716=CARTESIAN_POINT('Ctrl Pts',(-25.1508847843385,85.9663959330241,
78.477115675564));
#175717=CARTESIAN_POINT('Ctrl Pts',(-25.137785447126,85.7013110055866,78.9775795287955));
#175718=CARTESIAN_POINT('Ctrl Pts',(-25.1057074235496,84.974651219608,80.1460910728034));
#175719=CARTESIAN_POINT('Ctrl Pts',(-25.0865614772975,84.4794755639195,
80.7900908997777));
#175720=CARTESIAN_POINT('Ctrl Pts',(-25.0562364262827,83.5894869590496,
81.7365845430329));
#175721=CARTESIAN_POINT('Ctrl Pts',(-25.044914848025,83.2336084026925,82.072344040375));
#175722=CARTESIAN_POINT('Ctrl Pts',(-25.0146107691436,82.2371558735807,
82.9056635592529));
#175723=CARTESIAN_POINT('Ctrl Pts',(-24.995473199644,81.5656622672234,83.3624575174222));
#175724=CARTESIAN_POINT('Ctrl Pts',(-24.9655815292263,80.4401412988308,
83.9747594835686));
#175725=CARTESIAN_POINT('Ctrl Pts',(-24.9546683989537,80.0136298427335,
84.1758458051449));
#175726=CARTESIAN_POINT('Ctrl Pts',(-24.9247721148819,78.8251849668783,
84.6545088452004));
#175727=CARTESIAN_POINT('Ctrl Pts',(-24.9056378692957,78.0456005704614,
84.8818720659351));
#175728=CARTESIAN_POINT('Ctrl Pts',(-24.8691385022778,76.5074657479838,
85.1691835366419));
#175729=CARTESIAN_POINT('Ctrl Pts',(-24.8516738491272,75.7544946100201,
85.2388893877493));
#175730=CARTESIAN_POINT('Ctrl Pts',(-24.83393258407,74.9999999810153,85.23888938658));
#175731=CARTESIAN_POINT('Ctrl Pts',(-25.5022222452499,75.,85.23888938658));
#175732=CARTESIAN_POINT('Ctrl Pts',(-25.5145582143817,75.5296836159723,
85.23888938658));
#175733=CARTESIAN_POINT('Ctrl Pts',(-25.5266607095738,76.0590905354262,
85.204536325136));
#175734=CARTESIAN_POINT('Ctrl Pts',(-25.5528563869749,77.1976076353555,
85.0559901518693));
#175735=CARTESIAN_POINT('Ctrl Pts',(-25.5670074610243,77.8034077134567,
84.9297935650865));
#175736=CARTESIAN_POINT('Ctrl Pts',(-25.5979716716373,79.0545874499822,
84.5686637966591));
#175737=CARTESIAN_POINT('Ctrl Pts',(-25.6144957909623,79.6950543068848,
84.3241147354621));
#175738=CARTESIAN_POINT('Ctrl Pts',(-25.6428038802106,80.7750953811887,
83.8043959163946));
#175739=CARTESIAN_POINT('Ctrl Pts',(-25.6547341790472,81.2239504874583,
83.5524757249011));
#175740=CARTESIAN_POINT('Ctrl Pts',(-25.6788361783004,82.1061277943838,
82.9815554703247));
#175741=CARTESIAN_POINT('Ctrl Pts',(-25.6909699054758,82.5369640183544,
82.6607349247864));
#175742=CARTESIAN_POINT('Ctrl Pts',(-25.7112200888136,83.2054426742654,
82.0910848494002));
#175743=CARTESIAN_POINT('Ctrl Pts',(-25.7192361417016,83.4561204881654,
81.8586849080742));
#175744=CARTESIAN_POINT('Ctrl Pts',(-25.743511910138,84.1745022555095,81.1345132843351));
#175745=CARTESIAN_POINT('Ctrl Pts',(-25.7598819243811,84.6114232063115,
80.6140607396345));
#175746=CARTESIAN_POINT('Ctrl Pts',(-25.7874700754102,85.2860334182378,
79.6597521881797));
#175747=CARTESIAN_POINT('Ctrl Pts',(-25.7988506171131,85.5447652769501,
79.2427542847843));
#175748=CARTESIAN_POINT('Ctrl Pts',(-25.8226608907992,86.0378577557304,
78.3300066105182));
#175749=CARTESIAN_POINT('Ctrl Pts',(-25.8350291901725,86.2653630445236,
77.831763274363));
#175750=CARTESIAN_POINT('Ctrl Pts',(-25.8614698333218,86.6709539871991,
76.7586901004144));
#175751=CARTESIAN_POINT('Ctrl Pts',(-25.8757928860907,86.8415752119532,
76.1825750362739));
#175752=CARTESIAN_POINT('Ctrl Pts',(-25.9088926368427,87.135626729741,74.8327338465253));
#175753=CARTESIAN_POINT('Ctrl Pts',(-25.9274277270387,87.2285181775744,
74.0549915971521));
#175754=CARTESIAN_POINT('Ctrl Pts',(-25.956943262443,87.2582207561284,72.7778440792218));
#175755=CARTESIAN_POINT('Ctrl Pts',(-25.9682148471961,87.2396262566493,
72.2817356219742));
#175756=CARTESIAN_POINT('Ctrl Pts',(-25.9890232955504,87.1503377314522,
71.375217119128));
#175757=CARTESIAN_POINT('Ctrl Pts',(-25.9985499355979,87.0887182070633,
70.9646517574472));
#175758=CARTESIAN_POINT('Ctrl Pts',(-26.0248858082225,86.8671575003706,
69.8703439722172));
#175759=CARTESIAN_POINT('Ctrl Pts',(-26.0418770296343,86.6691107154739,
69.1959198412059));
#175760=CARTESIAN_POINT('Ctrl Pts',(-26.076389872062,86.1410827207986,67.8405101810176));
#175761=CARTESIAN_POINT('Ctrl Pts',(-26.0937667670734,85.803624014196,67.1655518865847));
#175762=CARTESIAN_POINT('Ctrl Pts',(-26.1276076056421,85.0216574270792,
65.9064830067026));
#175763=CARTESIAN_POINT('Ctrl Pts',(-26.1442010004447,84.5824647065737,
65.3226992987825));
#175764=CARTESIAN_POINT('Ctrl Pts',(-26.1776635838977,83.6406458278622,
64.2791520242437));
#175765=CARTESIAN_POINT('Ctrl Pts',(-26.1939882784656,83.1464861244611,
63.8152825186859));
#175766=CARTESIAN_POINT('Ctrl Pts',(-26.2282475967468,82.0096615039802,
62.9127989002998));
#175767=CARTESIAN_POINT('Ctrl Pts',(-26.2459640520519,81.3584153361494,
62.4896741456299));
#175768=CARTESIAN_POINT('Ctrl Pts',(-26.2763555392959,80.1778305594957,
61.8730059192247));
#175769=CARTESIAN_POINT('Ctrl Pts',(-26.2891146528552,79.6670833495305,
61.6490865264613));
#175770=CARTESIAN_POINT('Ctrl Pts',(-26.3189224438612,78.4845004647766,
61.2241039602073));
#175771=CARTESIAN_POINT('Ctrl Pts',(-26.3358360679419,77.8070767349799,
61.0443402680199));
#175772=CARTESIAN_POINT('Ctrl Pts',(-26.3693694917381,76.4101983602222,
60.7991277925184));
#175773=CARTESIAN_POINT('Ctrl Pts',(-26.3858965208382,75.6928151195828,
60.7374009453157));
#175774=CARTESIAN_POINT('Ctrl Pts',(-26.4177107095338,74.2988393329807,
60.7403409390513));
#175775=CARTESIAN_POINT('Ctrl Pts',(-26.433098685999,73.6248026975056,60.7976055921089));
#175776=CARTESIAN_POINT('Ctrl Pts',(-26.4739869598978,71.928762114844,61.084204811009));
#175777=CARTESIAN_POINT('Ctrl Pts',(-26.4991577052325,70.9250630761789,
61.3893637125483));
#175778=CARTESIAN_POINT('Ctrl Pts',(-26.5394496017554,69.3356561106817,
62.1047196212309));
#175779=CARTESIAN_POINT('Ctrl Pts',(-26.5551668293537,68.7246641508355,
62.4451664658636));
#175780=CARTESIAN_POINT('Ctrl Pts',(-26.5845868601615,67.6673044851022,
63.1589522258663));
#175781=CARTESIAN_POINT('Ctrl Pts',(-26.5983651700094,67.212064180179,63.5155523955322));
#175782=CARTESIAN_POINT('Ctrl Pts',(-26.6309031984934,66.2047929183061,
64.4264131486841));
#175783=CARTESIAN_POINT('Ctrl Pts',(-26.6494385005048,65.677238477793,65.0040401879711));
#175784=CARTESIAN_POINT('Ctrl Pts',(-26.6835152225745,64.7917739601575,
66.1819107053303));
#175785=CARTESIAN_POINT('Ctrl Pts',(-26.699124989789,64.4230831402206,66.7702353200393));
#175786=CARTESIAN_POINT('Ctrl Pts',(-26.7282222628511,63.8455535873771,
67.8932581754709));
#175787=CARTESIAN_POINT('Ctrl Pts',(-26.7417877914915,63.6206550203681,
68.417498873445));
#175788=CARTESIAN_POINT('Ctrl Pts',(-26.7739871746114,63.1781401653773,
69.6865315707564));
#175789=CARTESIAN_POINT('Ctrl Pts',(-26.7924057247524,62.9930944229818,
70.4401275384381));
#175790=CARTESIAN_POINT('Ctrl Pts',(-26.8259662057046,62.7822023604105,
71.873823859587));
#175791=CARTESIAN_POINT('Ctrl Pts',(-26.841194940152,62.7393317975643,72.5484801014744));
#175792=CARTESIAN_POINT('Ctrl Pts',(-26.8738752755997,62.7665423153993,
73.9706719580667));
#175793=CARTESIAN_POINT('Ctrl Pts',(-26.891785792233,62.849235171412,74.7152278980948));
#175794=CARTESIAN_POINT('Ctrl Pts',(-26.9271500513814,63.1458292715302,
76.1628947758508));
#175795=CARTESIAN_POINT('Ctrl Pts',(-26.9443595783814,63.3560502168863,
76.8636968340701));
#175796=CARTESIAN_POINT('Ctrl Pts',(-26.977276902664,63.8869178748331,78.1897925355681));
#175797=CARTESIAN_POINT('Ctrl Pts',(-26.9929723131151,64.2013438969176,
78.8146081545245));
#175798=CARTESIAN_POINT('Ctrl Pts',(-27.0222081515521,64.8625384705814,
79.8890166205348));
#175799=CARTESIAN_POINT('Ctrl Pts',(-27.035719320342,65.190544498994,80.3478593849382));
#175800=CARTESIAN_POINT('Ctrl Pts',(-27.0673457801649,66.0304724343931,
81.3664133494237));
#175801=CARTESIAN_POINT('Ctrl Pts',(-27.0852704564228,66.5650812259686,
81.904466025504));
#175802=CARTESIAN_POINT('Ctrl Pts',(-27.1191463267901,67.6905232501511,
82.8447335551604));
#175803=CARTESIAN_POINT('Ctrl Pts',(-27.1351057959906,68.2736290477985,
83.2515418518609));
#175804=CARTESIAN_POINT('Ctrl Pts',(-27.1628269622865,69.3133414011717,
83.8500371397582));
#175805=CARTESIAN_POINT('Ctrl Pts',(-27.1744849767242,69.7523000306373,
84.0687919840298));
#175806=CARTESIAN_POINT('Ctrl Pts',(-27.1971313539743,70.6224088729331,
84.439076728993));
#175807=CARTESIAN_POINT('Ctrl Pts',(-27.2080552166184,71.0512797416377,
84.5939618347456));
#175808=CARTESIAN_POINT('Ctrl Pts',(-27.2374137065437,72.2396282620299,
84.949606447519));
#175809=CARTESIAN_POINT('Ctrl Pts',(-27.2554184518982,73.0113618164258,
85.1018468685512));
#175810=CARTESIAN_POINT('Ctrl Pts',(-27.2825281172747,74.1937952563766,
85.2189866014275));
#175811=CARTESIAN_POINT('Ctrl Pts',(-27.2917126768954,74.5968360592202,
85.23888938658));
#175812=CARTESIAN_POINT('Ctrl Pts',(-27.3010916068384,75.,85.23888938658));
#175813=CARTESIAN_POINT('Origin',(-30.2175364832709,75.,72.98888938658));
#175814=CARTESIAN_POINT('',(-28.5675339373409,75.,85.23888938658));
#175815=CARTESIAN_POINT('',(-28.4332364523223,75.,85.23888938658));
#175816=CARTESIAN_POINT('',(-30.2175364832709,75.,85.23888938658));
#175817=CARTESIAN_POINT('',(-28.5670923992066,80.5057115855401,83.931352177925));
#175818=CARTESIAN_POINT('Origin',(-28.5675339373409,75.,72.98888938658));
#175819=CARTESIAN_POINT('Ctrl Pts',(-28.566799738496,80.5059347416729,83.9317949705846));
#175820=CARTESIAN_POINT('Ctrl Pts',(-28.5535796072272,79.9942929045818,
84.1892281124963));
#175821=CARTESIAN_POINT('Ctrl Pts',(-28.5405678264509,79.4652288872978,
84.4104600130184));
#175822=CARTESIAN_POINT('Ctrl Pts',(-28.5147317043305,78.4072126454951,
84.7680835514775));
#175823=CARTESIAN_POINT('Ctrl Pts',(-28.501791026997,77.880764281267,84.9077689340001));
#175824=CARTESIAN_POINT('Ctrl Pts',(-28.4700174024026,76.5730609737536,
85.1630194521663));
#175825=CARTESIAN_POINT('Ctrl Pts',(-28.4514197202864,75.7871460836583,
85.23888938658));
#175826=CARTESIAN_POINT('Ctrl Pts',(-28.4332364523223,75.,85.23888938658));
#175827=CARTESIAN_POINT('Origin',(-30.2175364832709,75.,72.98888938658));
#175828=CARTESIAN_POINT('',(-18.5675364832709,75.,83.48888938658));
#175829=CARTESIAN_POINT('Origin',(-18.5675364832709,75.,72.98888938658));
#175830=CARTESIAN_POINT('',(-16.5675364832709,75.,83.48888938658));
#175831=CARTESIAN_POINT('',(-30.2175364832709,75.,83.48888938658));
#175832=CARTESIAN_POINT('Origin',(-16.5675364832709,75.,72.98888938658));
#175833=CARTESIAN_POINT('Origin',(-30.2175364832709,75.,72.98888938658));
#175834=CARTESIAN_POINT('Ctrl Pts',(-28.4332364523223,75.,85.23888938658));
#175835=CARTESIAN_POINT('Ctrl Pts',(-28.4272749498642,74.7419290458744,
85.23888938658));
#175836=CARTESIAN_POINT('Ctrl Pts',(-28.4213453076129,74.4837260430028,
85.2307342343628));
#175837=CARTESIAN_POINT('Ctrl Pts',(-28.4026862400576,73.6716846387427,
85.1793089434919));
#175838=CARTESIAN_POINT('Ctrl Pts',(-28.3900005580085,73.120626176869,85.1065915600061));
#175839=CARTESIAN_POINT('Ctrl Pts',(-28.3491296798301,71.4220415560737,
84.7637580573169));
#175840=CARTESIAN_POINT('Ctrl Pts',(-28.3208970451119,70.3072774227404,
84.3655230158273));
#175841=CARTESIAN_POINT('Ctrl Pts',(-28.2744393311864,68.5252546847671,
83.4217141014942));
#175842=CARTESIAN_POINT('Ctrl Pts',(-28.2554501173914,67.8262563139882,
82.9540067640435));
#175843=CARTESIAN_POINT('Ctrl Pts',(-28.2169592060924,66.5772317562602,
81.9182646195507));
#175844=CARTESIAN_POINT('Ctrl Pts',(-28.1981684500683,66.0233171933883,
81.3612222826943));
#175845=CARTESIAN_POINT('Ctrl Pts',(-28.1616294382387,65.0322733817012,
80.1523014088068));
#175846=CARTESIAN_POINT('Ctrl Pts',(-28.1439543433449,64.596781755144,79.5037254941978));
#175847=CARTESIAN_POINT('Ctrl Pts',(-28.0882170818909,63.4469586964431,
77.3785390349933));
#175848=CARTESIAN_POINT('Ctrl Pts',(-28.048685544448,62.9644379248214,75.7972773555105));
#175849=CARTESIAN_POINT('Ctrl Pts',(-27.9981982467316,62.7525313524604,
73.6060037079195));
#175850=CARTESIAN_POINT('Ctrl Pts',(-27.9852995728824,62.7371041860924,
73.040908888065));
#175851=CARTESIAN_POINT('Ctrl Pts',(-27.9587146833293,62.784210732244,71.9151150510992));
#175852=CARTESIAN_POINT('Ctrl Pts',(-27.9452213158272,62.846343595883,71.3557522001653));
#175853=CARTESIAN_POINT('Ctrl Pts',(-27.9050939417333,63.1482049915785,
69.6915179279531));
#175854=CARTESIAN_POINT('Ctrl Pts',(-27.8795411038892,63.5024125963837,
68.6135998065467));
#175855=CARTESIAN_POINT('Ctrl Pts',(-27.8157427363851,64.7162759867173,
66.1358619334095));
#175856=CARTESIAN_POINT('Ctrl Pts',(-27.7764672099206,65.7182862431928,
64.8299194672785));
#175857=CARTESIAN_POINT('Ctrl Pts',(-27.7276820821298,67.3215909710765,
63.4310423100382));
#175858=CARTESIAN_POINT('Ctrl Pts',(-27.7162937230547,67.7163678791779,
63.1268860850115));
#175859=CARTESIAN_POINT('Ctrl Pts',(-27.6857189745135,68.7920210069889,
62.3980554773914));
#175860=CARTESIAN_POINT('Ctrl Pts',(-27.6664002681072,69.4979985547185,
62.0147029178625));
#175861=CARTESIAN_POINT('Ctrl Pts',(-27.6273286350037,71.0296360170234,
61.3682125275706));
#175862=CARTESIAN_POINT('Ctrl Pts',(-27.6077835078715,71.8560126351464,
61.117947601639));
#175863=CARTESIAN_POINT('Ctrl Pts',(-27.5502213685077,74.3098029942126,
60.6492701197802));
#175864=CARTESIAN_POINT('Ctrl Pts',(-27.5106451187069,75.9631888004553,
60.6675726774185));
#175865=CARTESIAN_POINT('Ctrl Pts',(-27.4593017697344,78.1518737205639,
61.1360586865382));
#175866=CARTESIAN_POINT('Ctrl Pts',(-27.4455805910085,78.7296572604109,
61.3049875462863));
#175867=CARTESIAN_POINT('Ctrl Pts',(-27.4042205380485,80.3696740473794,
61.9185992689906));
#175868=CARTESIAN_POINT('Ctrl Pts',(-27.3766829939307,81.3845739332598,
62.471187798176));
#175869=CARTESIAN_POINT('Ctrl Pts',(-27.3306180247843,82.9888676637545,
63.6635883551543));
#175870=CARTESIAN_POINT('Ctrl Pts',(-27.3114076338512,83.6157423471456,
64.2394760263181));
#175871=CARTESIAN_POINT('Ctrl Pts',(-27.266683614692,84.8642990763544,65.6518763485752));
#175872=CARTESIAN_POINT('Ctrl Pts',(-27.2419529267703,85.4493246742462,
66.5121738831067));
#175873=CARTESIAN_POINT('Ctrl Pts',(-27.1972850869743,86.326590303122,68.2371433892149));
#175874=CARTESIAN_POINT('Ctrl Pts',(-27.1769847565351,86.644672984736,69.0809060502006));
#175875=CARTESIAN_POINT('Ctrl Pts',(-27.1369967096554,87.0623364724272,
70.7129777021961));
#175876=CARTESIAN_POINT('Ctrl Pts',(-27.1181738246318,87.1834450510193,
71.4910816820856));
#175877=CARTESIAN_POINT('Ctrl Pts',(-27.0815337674519,87.2748157577772,
73.0571920400213));
#175878=CARTESIAN_POINT('Ctrl Pts',(-27.0637927592734,87.2453557865096,
73.8415443202955));
#175879=CARTESIAN_POINT('Ctrl Pts',(-27.0285245469332,87.042273413979,75.3553303872363));
#175880=CARTESIAN_POINT('Ctrl Pts',(-27.0106861812576,86.8763023485678,
76.0823979323705));
#175881=CARTESIAN_POINT('Ctrl Pts',(-26.9560904443585,86.1639986647825,
78.2647375315542));
#175882=CARTESIAN_POINT('Ctrl Pts',(-26.9218022723246,85.406793785591,79.6347969653061));
#175883=CARTESIAN_POINT('Ctrl Pts',(-26.8715478842244,84.0529225937617,
81.2608741454549));
#175884=CARTESIAN_POINT('Ctrl Pts',(-26.8580254905575,83.6621824953892,
81.6691969570759));
#175885=CARTESIAN_POINT('Ctrl Pts',(-26.8233349394846,82.5753679147139,
82.6581833308507));
#175886=CARTESIAN_POINT('Ctrl Pts',(-26.8027190063652,81.8406239914801,
83.1912081901866));
#175887=CARTESIAN_POINT('Ctrl Pts',(-26.7536317685662,79.9848987459978,
84.2461241957079));
#175888=CARTESIAN_POINT('Ctrl Pts',(-26.7238224526101,78.8304820323874,
84.6893982949392));
#175889=CARTESIAN_POINT('Ctrl Pts',(-26.6768151453692,76.8645997039973,
85.1214536856491));
#175890=CARTESIAN_POINT('Ctrl Pts',(-26.6590742008417,76.0853352897924,
85.2158222530688));
#175891=CARTESIAN_POINT('Ctrl Pts',(-26.6386599167246,75.2016038738315,
85.237645433459));
#175892=CARTESIAN_POINT('Ctrl Pts',(-26.636324880805,75.100791606156,85.23888938658));
#175893=CARTESIAN_POINT('Ctrl Pts',(-26.6339799854461,75.,85.23888938658));
#175894=CARTESIAN_POINT('',(-28.2015531594526,75.00001897909,60.7388893865947));
#175895=CARTESIAN_POINT('Ctrl Pts',(-27.3010916068384,75.,85.23888938658));
#175896=CARTESIAN_POINT('Ctrl Pts',(-27.3058229610351,75.2033826262405,
85.23888938658));
#175897=CARTESIAN_POINT('Ctrl Pts',(-27.3106144561045,75.4067963411875,
85.2338243834481));
#175898=CARTESIAN_POINT('Ctrl Pts',(-27.3284325344786,76.1564688718875,
85.196444072552));
#175899=CARTESIAN_POINT('Ctrl Pts',(-27.3416267514371,76.700445405241,85.1326243949349));
#175900=CARTESIAN_POINT('Ctrl Pts',(-27.3663300689989,77.7204171731748,
84.9430629030699));
#175901=CARTESIAN_POINT('Ctrl Pts',(-27.3778533444614,78.196691782318,84.8246024386126));
#175902=CARTESIAN_POINT('Ctrl Pts',(-27.4049117962594,79.311901247527,84.4749770165384));
#175903=CARTESIAN_POINT('Ctrl Pts',(-27.4202137963442,79.9412372568343,
84.2186209013142));
#175904=CARTESIAN_POINT('Ctrl Pts',(-27.443661321696,80.8507374759572,83.7568092182322));
#175905=CARTESIAN_POINT('Ctrl Pts',(-27.4516255212873,81.1487583792507,
83.589455131192));
#175906=CARTESIAN_POINT('Ctrl Pts',(-27.4724655619897,81.895838660614,83.1278143911429));
#175907=CARTESIAN_POINT('Ctrl Pts',(-27.4854035766097,82.3332578802525,
82.8160823844634));
#175908=CARTESIAN_POINT('Ctrl Pts',(-27.5104419511676,83.1471463816151,
82.1513667409141));
#175909=CARTESIAN_POINT('Ctrl Pts',(-27.522530685445,83.5245858552855,81.8012914623614));
#175910=CARTESIAN_POINT('Ctrl Pts',(-27.5502688602431,84.3504208840545,
80.9324734068029));
#175911=CARTESIAN_POINT('Ctrl Pts',(-27.5656966933563,84.779532225077,80.3977786503999));
#175912=CARTESIAN_POINT('Ctrl Pts',(-27.5957947175092,85.5100585257217,
79.3126688038495));
#175913=CARTESIAN_POINT('Ctrl Pts',(-27.6106600120252,85.8183477470029,
78.7694458291332));
#175914=CARTESIAN_POINT('Ctrl Pts',(-27.6444082217492,86.4181348212994,
77.4949663337692));
#175915=CARTESIAN_POINT('Ctrl Pts',(-27.6630233100806,86.6833278989251,
76.7543128852062));
#175916=CARTESIAN_POINT('Ctrl Pts',(-27.6975205814915,87.0495871238234,
75.3066059726427));
#175917=CARTESIAN_POINT('Ctrl Pts',(-27.7134539259211,87.1634343043775,
74.6060515393013));
#175918=CARTESIAN_POINT('Ctrl Pts',(-27.7412590167738,87.2529116368176,
73.4058194687855));
#175919=CARTESIAN_POINT('Ctrl Pts',(-27.7530393663587,87.2597501207847,
72.9102718279261));
#175920=CARTESIAN_POINT('Ctrl Pts',(-27.7757995881677,87.2152814417707,
71.9609702666392));
#175921=CARTESIAN_POINT('Ctrl Pts',(-27.7867125648806,87.1686515422412,
71.5077945096812));
#175922=CARTESIAN_POINT('Ctrl Pts',(-27.8156815443413,86.9757301515703,
70.2989864261983));
#175923=CARTESIAN_POINT('Ctrl Pts',(-27.8333353719806,86.7833350659435,
69.5527983956408));
#175924=CARTESIAN_POINT('Ctrl Pts',(-27.8651210764537,86.3103238864562,
68.2424471102556));
#175925=CARTESIAN_POINT('Ctrl Pts',(-27.8793700232485,86.053820750885,67.6723877258993));
#175926=CARTESIAN_POINT('Ctrl Pts',(-27.9073692610972,85.4892886817221,
66.6370909515588));
#175927=CARTESIAN_POINT('Ctrl Pts',(-27.9207554178926,85.1907845063452,
66.168446960112));
#175928=CARTESIAN_POINT('Ctrl Pts',(-27.9452553340675,84.5800992988148,
65.3397551300243));
#175929=CARTESIAN_POINT('Ctrl Pts',(-27.9564014000352,84.2767144470895,
64.9745189473525));
#175930=CARTESIAN_POINT('Ctrl Pts',(-27.9830279008244,83.4919537648032,
64.134210935316));
#175931=CARTESIAN_POINT('Ctrl Pts',(-27.9982668164661,82.9909700275654,
63.6795928526122));
#175932=CARTESIAN_POINT('Ctrl Pts',(-28.0308464320267,81.8658252908171,
62.8166522069551));
#175933=CARTESIAN_POINT('Ctrl Pts',(-28.0486347182099,81.2367073262537,
62.4192443947449));
#175934=CARTESIAN_POINT('Ctrl Pts',(-28.0843777710471,79.9069104355396,
61.7395093727613));
#175935=CARTESIAN_POINT('Ctrl Pts',(-28.1020658386639,79.2082978167326,
61.4599441731932));
#175936=CARTESIAN_POINT('Ctrl Pts',(-28.1325884212831,77.9375545894379,
61.0824377087962));
#175937=CARTESIAN_POINT('Ctrl Pts',(-28.1455798759461,77.3757856424469,
60.9577440834114));
#175938=CARTESIAN_POINT('Ctrl Pts',(-28.1643434019884,76.5683511157738,
60.8372983827645));
#175939=CARTESIAN_POINT('Ctrl Pts',(-28.1699401585733,76.3283548966331,
60.8087267273936));
#175940=CARTESIAN_POINT('Ctrl Pts',(-28.1841624485064,75.7260116475704,
60.7550329302604));
#175941=CARTESIAN_POINT('Ctrl Pts',(-28.1928541804325,75.3631092856355,
60.7388899491354));
#175942=CARTESIAN_POINT('Ctrl Pts',(-28.2015531594526,75.0000189790899,
60.7388893865947));
#175943=CARTESIAN_POINT('',(-28.5675342178229,63.2672737070204,69.46672519));
#175944=CARTESIAN_POINT('Ctrl Pts',(-28.2015531594526,75.0000189790899,
60.7388893865947));
#175945=CARTESIAN_POINT('Ctrl Pts',(-28.2115085777166,74.5844856319101,
60.7388887428033));
#175946=CARTESIAN_POINT('Ctrl Pts',(-28.2214581486582,74.1692192048778,
60.7600311204056));
#175947=CARTESIAN_POINT('Ctrl Pts',(-28.2563764973938,72.7014270353383,
60.9098820884185));
#175948=CARTESIAN_POINT('Ctrl Pts',(-28.2802056089586,71.6654569059614,
61.153913573752));
#175949=CARTESIAN_POINT('Ctrl Pts',(-28.3161178277994,70.2052579637771,
61.7051026614066));
#175950=CARTESIAN_POINT('Ctrl Pts',(-28.3279543485361,69.7479402986497,
61.9105662236379));
#175951=CARTESIAN_POINT('Ctrl Pts',(-28.3551888069236,68.7402228127518,
62.439770798747));
#175952=CARTESIAN_POINT('Ctrl Pts',(-28.3704805414799,68.1999305771706,
62.7796884624181));
#175953=CARTESIAN_POINT('Ctrl Pts',(-28.4005460677347,67.172577142645,63.5439176697712));
#175954=CARTESIAN_POINT('Ctrl Pts',(-28.4152665757593,66.6876325732374,
63.9677699594751));
#175955=CARTESIAN_POINT('Ctrl Pts',(-28.4443880543649,65.7956167561956,
64.880690622336));
#175956=CARTESIAN_POINT('Ctrl Pts',(-28.458867085717,65.3888279971904,65.3672798388102));
#175957=CARTESIAN_POINT('Ctrl Pts',(-28.498775366339,64.4150539396884,66.7347398350393));
#175958=CARTESIAN_POINT('Ctrl Pts',(-28.5239637024401,63.9201129993077,
67.6605065258106));
#175959=CARTESIAN_POINT('Ctrl Pts',(-28.5548780727218,63.445093108566,68.9106765416759));
#175960=CARTESIAN_POINT('Ctrl Pts',(-28.5615651320877,63.351205608257,69.1871419701496));
#175961=CARTESIAN_POINT('Ctrl Pts',(-28.568231723297,63.2672824189022,69.4666971484707));
#175962=CARTESIAN_POINT('Origin',(-28.5675339373409,75.,72.98888938658));
#175963=CARTESIAN_POINT('Origin',(-23.90845228375,74.9968912574536,72.9873550812444));
#175964=CARTESIAN_POINT('Ctrl Pts',(-19.9173382169355,74.9968858117149,
59.938705268027));
#175965=CARTESIAN_POINT('Ctrl Pts',(-19.9330420568071,74.2767378935156,
59.9387055685744));
#175966=CARTESIAN_POINT('Ctrl Pts',(-19.9489225765158,73.5578381134046,
59.9983214666742));
#175967=CARTESIAN_POINT('Ctrl Pts',(-19.9801875397725,72.1459011840029,
60.2341150131016));
#175968=CARTESIAN_POINT('Ctrl Pts',(-19.9955184081017,71.4550251746423,
60.4084653748063));
#175969=CARTESIAN_POINT('Ctrl Pts',(-20.0214018597075,70.33484625965,60.7908125262915));
#175970=CARTESIAN_POINT('Ctrl Pts',(-20.0317932982671,69.8964947186888,
60.9675269909449));
#175971=CARTESIAN_POINT('Ctrl Pts',(-20.0556893445538,68.9115536151873,
61.428192831652));
#175972=CARTESIAN_POINT('Ctrl Pts',(-20.0690233674465,68.373536871566,61.7278371577208));
#175973=CARTESIAN_POINT('Ctrl Pts',(-20.1014548923896,67.1267436688524,
62.5426181791745));
#175974=CARTESIAN_POINT('Ctrl Pts',(-20.1207321421361,66.4447485068989,
63.0932866102794));
#175975=CARTESIAN_POINT('Ctrl Pts',(-20.1544590052907,65.3517709601478,
64.1738449216507));
#175976=CARTESIAN_POINT('Ctrl Pts',(-20.1687858392181,64.9167365633608,
64.6749072142671));
#175977=CARTESIAN_POINT('Ctrl Pts',(-20.2000827148801,64.0643659267137,
65.8224904223784));
#175978=CARTESIAN_POINT('Ctrl Pts',(-20.2170830906625,63.6622529469042,
66.4772578952479));
#175979=CARTESIAN_POINT('Ctrl Pts',(-20.2482227120542,63.0283175309696,
67.7483152702444));
#175980=CARTESIAN_POINT('Ctrl Pts',(-20.2623973174422,62.7810003086865,
68.3541805370158));
#175981=CARTESIAN_POINT('Ctrl Pts',(-20.2918856392969,62.3683715854022,
69.631439903851));
#175982=CARTESIAN_POINT('Ctrl Pts',(-20.3071798697992,62.208859614119,70.3025983686922));
#175983=CARTESIAN_POINT('Ctrl Pts',(-20.3367714609488,62.0020807315052,
71.6329195219529));
#175984=CARTESIAN_POINT('Ctrl Pts',(-20.3510559154005,61.9503445633049,
72.2893442443117));
#175985=CARTESIAN_POINT('Ctrl Pts',(-20.3785808855754,61.9464631009909,
73.5402113093633));
#175986=CARTESIAN_POINT('Ctrl Pts',(-20.3917485995825,61.9850951817803,
74.1329921751189));
#175987=CARTESIAN_POINT('Ctrl Pts',(-20.4239469084602,62.1786459992294,
75.5768132285351));
#175988=CARTESIAN_POINT('Ctrl Pts',(-20.442671274263,62.3780103413679,76.4190528982472));
#175989=CARTESIAN_POINT('Ctrl Pts',(-20.4731627485336,62.8273500526258,
77.724088988084));
#175990=CARTESIAN_POINT('Ctrl Pts',(-20.484656147901,63.0244933321518,78.2023399842857));
#175991=CARTESIAN_POINT('Ctrl Pts',(-20.5152005459052,63.6255454851649,
79.4453787026285));
#175992=CARTESIAN_POINT('Ctrl Pts',(-20.533963916611,64.0779194525373,80.1838562999077));
#175993=CARTESIAN_POINT('Ctrl Pts',(-20.5641170501726,64.9012866303631,
81.2695486505498));
#175994=CARTESIAN_POINT('Ctrl Pts',(-20.5752195748772,65.2251642673089,
81.6493013698919));
#175995=CARTESIAN_POINT('Ctrl Pts',(-20.5955234230254,65.8592165383069,
82.3117935273445));
#175996=CARTESIAN_POINT('Ctrl Pts',(-20.6046911779992,66.1628183603434,
82.5999201880847));
#175997=CARTESIAN_POINT('Ctrl Pts',(-20.6346185984662,67.1951964060269,
83.48938727183));
#175998=CARTESIAN_POINT('Ctrl Pts',(-20.655580595683,67.9754682664369,84.0263189844671));
#175999=CARTESIAN_POINT('Ctrl Pts',(-20.6920836689512,69.4263633798384,
84.808174845495));
#176000=CARTESIAN_POINT('Ctrl Pts',(-20.7074175988213,70.0719036021621,
85.0913650963437));
#176001=CARTESIAN_POINT('Ctrl Pts',(-20.7364113500887,71.3135071457599,
85.5201836585844));
#176002=CARTESIAN_POINT('Ctrl Pts',(-20.7499833159838,71.9031382356305,
85.6786039963794));
#176003=CARTESIAN_POINT('Ctrl Pts',(-20.7827001188224,73.3514320986593,
85.9607593187245));
#176004=CARTESIAN_POINT('Ctrl Pts',(-20.8015164287551,74.2155559906024,
86.0413303144843));
#176005=CARTESIAN_POINT('Ctrl Pts',(-20.8393343037172,75.9252661660537,
86.0302742768058));
#176006=CARTESIAN_POINT('Ctrl Pts',(-20.8581058582092,76.7667479860193,
85.9429421494968));
#176007=CARTESIAN_POINT('Ctrl Pts',(-20.8951238339364,78.4201817940811,
85.6071520765293));
#176008=CARTESIAN_POINT('Ctrl Pts',(-20.9136668209986,79.228273233321,85.3596464630248));
#176009=CARTESIAN_POINT('Ctrl Pts',(-20.9503565042217,80.7556820110671,
84.7245334042394));
#176010=CARTESIAN_POINT('Ctrl Pts',(-20.9680553081979,81.4738907755999,
84.3440054328353));
#176011=CARTESIAN_POINT('Ctrl Pts',(-21.0027004007613,82.7930115983596,
83.4790247872099));
#176012=CARTESIAN_POINT('Ctrl Pts',(-21.019713441587,83.3956378002191,83.0031263137548));
#176013=CARTESIAN_POINT('Ctrl Pts',(-21.0528120499888,84.4871179982778,
81.9730233894142));
#176014=CARTESIAN_POINT('Ctrl Pts',(-21.0687362238809,84.9777240174162,
81.4247491183197));
#176015=CARTESIAN_POINT('Ctrl Pts',(-21.0993279547773,85.814806856134,80.313435524131));
#176016=CARTESIAN_POINT('Ctrl Pts',(-21.1139020257325,86.1698360147959,
79.7596555846068));
#176017=CARTESIAN_POINT('Ctrl Pts',(-21.145109445782,86.8437470022363,78.5101369405165));
#176018=CARTESIAN_POINT('Ctrl Pts',(-21.1616176529458,87.1462750542629,
77.8083081998923));
#176019=CARTESIAN_POINT('Ctrl Pts',(-21.187548413683,87.5167704632658,76.6878974934662));
#176020=CARTESIAN_POINT('Ctrl Pts',(-21.1967602241767,87.6287006191586,
76.2856547671196));
#176021=CARTESIAN_POINT('Ctrl Pts',(-21.2250037279068,87.9125711093249,
75.03641198948));
#176022=CARTESIAN_POINT('Ctrl Pts',(-21.2436593958821,88.0198633178678,
74.1771537817256));
#176023=CARTESIAN_POINT('Ctrl Pts',(-21.2776117572916,88.0586334289964,
72.6270566305324));
#176024=CARTESIAN_POINT('Ctrl Pts',(-21.2927971039351,88.0215759479958,
71.9402125395721));
#176025=CARTESIAN_POINT('Ctrl Pts',(-21.3169667097406,87.875329475273,70.8455022641578));
#176026=CARTESIAN_POINT('Ctrl Pts',(-21.3260206594937,87.8001790700835,
70.4344102966169));
#176027=CARTESIAN_POINT('Ctrl Pts',(-21.3543309053144,87.5050793294366,
69.1673020077081));
#176028=CARTESIAN_POINT('Ctrl Pts',(-21.3737642612831,87.2178691754204,
68.329538119423));
#176029=CARTESIAN_POINT('Ctrl Pts',(-21.4119659520071,86.4879995764537,
66.7453317928356));
#176030=CARTESIAN_POINT('Ctrl Pts',(-21.4304732288375,86.0512599347866,
66.0009854150646));
#176031=CARTESIAN_POINT('Ctrl Pts',(-21.45877073841,85.2903319415476,64.9562540583632));
#176032=CARTESIAN_POINT('Ctrl Pts',(-21.4682633490694,85.0191071670509,
64.6202353673414));
#176033=CARTESIAN_POINT('Ctrl Pts',(-21.4870039107528,84.449790917879,63.982399851356));
#176034=CARTESIAN_POINT('Ctrl Pts',(-21.4961934348158,84.1526419610169,
63.6804350576366));
#176035=CARTESIAN_POINT('Ctrl Pts',(-21.5233547247884,83.2321115197238,
62.8318145792477));
#176036=CARTESIAN_POINT('Ctrl Pts',(-21.5414238145453,82.5707706179085,
62.329484825224));
#176037=CARTESIAN_POINT('Ctrl Pts',(-21.5785210670392,81.1333979409496,
61.4394720739356));
#176038=CARTESIAN_POINT('Ctrl Pts',(-21.597076175883,80.3573456562022,61.0594111100691));
#176039=CARTESIAN_POINT('Ctrl Pts',(-21.6250796896882,79.1531224230812,
60.6110914879113));
#176040=CARTESIAN_POINT('Ctrl Pts',(-21.6343447696767,78.7497996221477,
60.4828824650073));
#176041=CARTESIAN_POINT('Ctrl Pts',(-21.6625492020202,77.5076450230888,
60.153547569202));
#176042=CARTESIAN_POINT('Ctrl Pts',(-21.6811736407976,76.6544741846669,
60.0157351749384));
#176043=CARTESIAN_POINT('Ctrl Pts',(-21.7057297020164,75.528449936209,59.9468231966896));
#176044=CARTESIAN_POINT('Ctrl Pts',(-21.7115334678031,75.2626331470515,
59.9387052680259));
#176045=CARTESIAN_POINT('Ctrl Pts',(-21.7173525905574,74.9968912574536,
59.9387052680259));
#176046=CARTESIAN_POINT('Ctrl Pts',(-21.4178560137093,74.996891265676,59.9387052680259));
#176047=CARTESIAN_POINT('Ctrl Pts',(-21.41681366863,75.0442600341101,59.9387052680558));
#176048=CARTESIAN_POINT('Ctrl Pts',(-21.4157707615431,75.0916318668529,
59.9389632028205));
#176049=CARTESIAN_POINT('Ctrl Pts',(-21.3957577137173,76.0001586580206,
59.9488585939689));
#176050=CARTESIAN_POINT('Ctrl Pts',(-21.3765309548117,76.858270577439,60.0434684027457));
#176051=CARTESIAN_POINT('Ctrl Pts',(-21.3458801869731,78.2198977052432,
60.3318795149761));
#176052=CARTESIAN_POINT('Ctrl Pts',(-21.3342766158643,78.7318223000384,
60.4733979380445));
#176053=CARTESIAN_POINT('Ctrl Pts',(-21.3069126076966,79.905205400192,60.8762128117258));
#176054=CARTESIAN_POINT('Ctrl Pts',(-21.291086993832,80.5567698007339,61.1611528710284));
#176055=CARTESIAN_POINT('Ctrl Pts',(-21.2587222061821,81.844710534345,61.854465152685));
#176056=CARTESIAN_POINT('Ctrl Pts',(-21.2423307058054,82.4753959811991,
62.2679410595901));
#176057=CARTESIAN_POINT('Ctrl Pts',(-21.2066278909854,83.7443724506534,
63.266651874344));
#176058=CARTESIAN_POINT('Ctrl Pts',(-21.1874199767991,84.3673335228922,
63.8656602232681));
#176059=CARTESIAN_POINT('Ctrl Pts',(-21.1592772520458,85.1987432622261,
64.8408609746335));
#176060=CARTESIAN_POINT('Ctrl Pts',(-21.1500818761777,85.4552887949796,
65.1729407676574));
#176061=CARTESIAN_POINT('Ctrl Pts',(-21.1218145432478,86.1889436702785,
66.2235998285199));
#176062=CARTESIAN_POINT('Ctrl Pts',(-21.1025835347235,86.6112356261139,
66.9775770080341));
#176063=CARTESIAN_POINT('Ctrl Pts',(-21.0670621257983,87.2581623840701,
68.4597967379077));
#176064=CARTESIAN_POINT('Ctrl Pts',(-21.0505482640139,87.4995922590061,
69.176840533366));
#176065=CARTESIAN_POINT('Ctrl Pts',(-21.0245961035509,87.7758976962381,
70.3156719535861));
#176066=CARTESIAN_POINT('Ctrl Pts',(-21.0153375906866,87.8546928580724,
70.7250919862511));
#176067=CARTESIAN_POINT('Ctrl Pts',(-20.9879143247382,88.0307955637858,
71.9548059008335));
#176068=CARTESIAN_POINT('Ctrl Pts',(-20.9700045145971,88.0700073241251,
72.7812983205284));
#176069=CARTESIAN_POINT('Ctrl Pts',(-20.9327282218023,87.9899244881527,
74.4687021843473));
#176070=CARTESIAN_POINT('Ctrl Pts',(-20.9136153739934,87.8634149024849,
75.3252771702288));
#176071=CARTESIAN_POINT('Ctrl Pts',(-20.88548594242,87.5502408558111,76.5733917951643));
#176072=CARTESIAN_POINT('Ctrl Pts',(-20.8762371854095,87.4273830566958,
76.9784850315698));
#176073=CARTESIAN_POINT('Ctrl Pts',(-20.8507301847959,87.0372377676382,
78.0706669550707));
#176074=CARTESIAN_POINT('Ctrl Pts',(-20.8343758561155,86.7311001454912,
78.7422095494678));
#176075=CARTESIAN_POINT('Ctrl Pts',(-20.8065255442574,86.1070840304626,
79.8516360577577));
#176076=CARTESIAN_POINT('Ctrl Pts',(-20.7948767455376,85.8156806869038,
80.3023077829987));
#176077=CARTESIAN_POINT('Ctrl Pts',(-20.7666792793523,85.0516918165158,
81.337916593493));
#176078=CARTESIAN_POINT('Ctrl Pts',(-20.7500468352409,84.5546952456442,
81.9024698525982));
#176079=CARTESIAN_POINT('Ctrl Pts',(-20.7186048796733,83.5163516485031,
82.8947221405498));
#176080=CARTESIAN_POINT('Ctrl Pts',(-20.7037805924562,82.9842316261899,
83.3285119549456));
#176081=CARTESIAN_POINT('Ctrl Pts',(-20.6727459699732,81.8191585735813,
84.1344894493512));
#176082=CARTESIAN_POINT('Ctrl Pts',(-20.6565728896771,81.1839074716829,
84.4992085356232));
#176083=CARTESIAN_POINT('Ctrl Pts',(-20.6294708145913,80.0579524538981,
85.0254065546555));
#176084=CARTESIAN_POINT('Ctrl Pts',(-20.6183950189988,79.5821048388523,
85.2145723093971));
#176085=CARTESIAN_POINT('Ctrl Pts',(-20.5883413164331,78.2743649906955,
85.6473368864876));
#176086=CARTESIAN_POINT('Ctrl Pts',(-20.569210958263,77.4273096571947,85.8368703335035));
#176087=CARTESIAN_POINT('Ctrl Pts',(-20.5377080645285,75.9903290890004,
86.0111278513581));
#176088=CARTESIAN_POINT('Ctrl Pts',(-20.5251349688791,75.4088756721479,
86.0424631067098));
#176089=CARTESIAN_POINT('Ctrl Pts',(-20.4968563732491,74.1138237924929,
86.0256277651038));
#176090=CARTESIAN_POINT('Ctrl Pts',(-20.4811152915302,73.4023336282443,
85.9578503823963));
#176091=CARTESIAN_POINT('Ctrl Pts',(-20.4474752967114,71.8825012624425,
85.6860734269489));
#176092=CARTESIAN_POINT('Ctrl Pts',(-20.4295842421063,71.0808580967995,
85.4621922381434));
#176093=CARTESIAN_POINT('Ctrl Pts',(-20.4022763370671,69.9175317344837,
85.0140181389652));
#176094=CARTESIAN_POINT('Ctrl Pts',(-20.3931231801359,69.5365017488138,
84.8458821231825));
#176095=CARTESIAN_POINT('Ctrl Pts',(-20.3651767119189,68.3937867628417,
84.2748676877471));
#176096=CARTESIAN_POINT('Ctrl Pts',(-20.3466886326991,67.6634124563664,
83.8145901929087));
#176097=CARTESIAN_POINT('Ctrl Pts',(-20.3089705059557,66.3023363505552,
82.755536642036));
#176098=CARTESIAN_POINT('Ctrl Pts',(-20.2900276098555,65.675242593848,82.1590250083103));
#176099=CARTESIAN_POINT('Ctrl Pts',(-20.2620774778898,64.8342974085004,
81.1830559580949));
#176100=CARTESIAN_POINT('Ctrl Pts',(-20.252852986785,64.5728121536784,80.8477876691409));
#176101=CARTESIAN_POINT('Ctrl Pts',(-20.2287246937958,63.9370110683983,
79.9449272410045));
#176102=CARTESIAN_POINT('Ctrl Pts',(-20.2137340927338,63.589842662658,79.3597959535171));
#176103=CARTESIAN_POINT('Ctrl Pts',(-20.180104674203,62.908689691543,77.9760753281143));
#176104=CARTESIAN_POINT('Ctrl Pts',(-20.1614842839252,62.6053081244397,
77.1659456196048));
#176105=CARTESIAN_POINT('Ctrl Pts',(-20.1334055932045,62.2775686771867,
75.9299624077936));
#176106=CARTESIAN_POINT('Ctrl Pts',(-20.1242425797183,62.1902767982458,
75.5232436360709));
#176107=CARTESIAN_POINT('Ctrl Pts',(-20.0981978934479,61.9965793065736,
74.3501104304278));
#176108=CARTESIAN_POINT('Ctrl Pts',(-20.0815282551429,61.9386765950035,
73.5774782424547));
#176109=CARTESIAN_POINT('Ctrl Pts',(-20.050001059248,61.9588586865063,72.139145920468));
#176110=CARTESIAN_POINT('Ctrl Pts',(-20.0352810139129,62.0190389983518,
71.4756993029304));
#176111=CARTESIAN_POINT('Ctrl Pts',(-20.0016074559056,62.2747903613662,
69.9575120421242));
#176112=CARTESIAN_POINT('Ctrl Pts',(-19.9826750811475,62.5063387440246,
69.1120612509894));
#176113=CARTESIAN_POINT('Ctrl Pts',(-19.9542428259785,62.9701294617421,
67.9082770841441));
#176114=CARTESIAN_POINT('Ctrl Pts',(-19.9450489658567,63.1380126501298,
67.5277735283805));
#176115=CARTESIAN_POINT('Ctrl Pts',(-19.9193164912298,63.6613477631329,
66.4801808585826));
#176116=CARTESIAN_POINT('Ctrl Pts',(-19.9029642840316,64.0569679482172,
65.8350167335816));
#176117=CARTESIAN_POINT('Ctrl Pts',(-19.8718434284005,64.8982605894784,
64.6976236507171));
#176118=CARTESIAN_POINT('Ctrl Pts',(-19.8571985066566,65.32996246771,64.1980163306893));
#176119=CARTESIAN_POINT('Ctrl Pts',(-19.8245579560657,66.3838078226897,
63.1504171632873));
#176120=CARTESIAN_POINT('Ctrl Pts',(-19.8066007523067,67.0240990345888,
62.6246747936668));
#176121=CARTESIAN_POINT('Ctrl Pts',(-19.7744569492311,68.2306011504375,
61.8124398093872));
#176122=CARTESIAN_POINT('Ctrl Pts',(-19.7605100521488,68.7760217270058,
61.4998749157207));
#176123=CARTESIAN_POINT('Ctrl Pts',(-19.7361577734367,69.7761724614817,
61.0189111200789));
#176124=CARTESIAN_POINT('Ctrl Pts',(-19.7256297548061,70.2217660199513,
60.8342593997852));
#176125=CARTESIAN_POINT('Ctrl Pts',(-19.6989346662376,71.3661028564162,
60.4327279679045));
#176126=CARTESIAN_POINT('Ctrl Pts',(-19.6826650619117,72.0747597355435,
60.2491281214674));
#176127=CARTESIAN_POINT('Ctrl Pts',(-19.6502356237299,73.5223875407533,
60.0012997842663));
#176128=CARTESIAN_POINT('Ctrl Pts',(-19.634176490088,74.2589730558603,59.9387048093555));
#176129=CARTESIAN_POINT('Ctrl Pts',(-19.6178714446467,74.9968993681035,
59.9387052680284));
#176130=CARTESIAN_POINT('Origin',(-29.0675369414309,75.,72.98888938658));
#176131=CARTESIAN_POINT('',(-29.3659074908669,61.9518604038339,72.9107242579373));
#176132=CARTESIAN_POINT('',(-29.0715747727696,75.,60.2348484464093));
#176133=CARTESIAN_POINT('Ctrl Pts',(-29.3659074908668,61.951860403834,72.9107242579373));
#176134=CARTESIAN_POINT('Ctrl Pts',(-29.3546070927146,61.9679108610104,
72.1178290340207));
#176135=CARTESIAN_POINT('Ctrl Pts',(-29.3435513987406,62.0560537850465,
71.3272167571516));
#176136=CARTESIAN_POINT('Ctrl Pts',(-29.3198744527501,62.3845025016822,
69.7320276469564));
#176137=CARTESIAN_POINT('Ctrl Pts',(-29.3073471940742,62.631814685764,68.9317585168648));
#176138=CARTESIAN_POINT('Ctrl Pts',(-29.271600961411,63.5738929101862,66.6770808866654));
#176139=CARTESIAN_POINT('Ctrl Pts',(-29.2493251735019,64.4653657292663,
65.3168568073909));
#176140=CARTESIAN_POINT('Ctrl Pts',(-29.2008834203262,66.7259955316958,
62.9788091341843));
#176141=CARTESIAN_POINT('Ctrl Pts',(-29.1779340274077,68.0820978808835,
62.0244452185557));
#176142=CARTESIAN_POINT('Ctrl Pts',(-29.1412176792257,70.3529225888009,
61.0067126405035));
#176143=CARTESIAN_POINT('Ctrl Pts',(-29.1283139882168,71.161267589059,60.7373079796422));
#176144=CARTESIAN_POINT('Ctrl Pts',(-29.1035475953523,72.7936407465736,
60.3677278885743));
#176145=CARTESIAN_POINT('Ctrl Pts',(-29.0916996520816,73.614095259019,60.2633970793433));
#176146=CARTESIAN_POINT('Ctrl Pts',(-29.077037613407,74.6255543768367,60.2335039391159));
#176147=CARTESIAN_POINT('Ctrl Pts',(-29.0743156629422,74.8128642429899,
60.2321075556721));
#176148=CARTESIAN_POINT('Ctrl Pts',(-29.0715747727696,75.,60.2348484464093));
#176149=CARTESIAN_POINT('',(-29.5675339851921,75.,59.7388891318012));
#176150=CARTESIAN_POINT('',(-29.0675369414309,75.,60.23888627858));
#176151=CARTESIAN_POINT('Origin',(-29.5675339847409,75.,72.98888938658));
#176152=CARTESIAN_POINT('Ctrl Pts',(-29.0715747727696,75.,60.2348484464093));
#176153=CARTESIAN_POINT('Ctrl Pts',(-29.0624830013438,75.6207456049797,
60.2439402197083));
#176154=CARTESIAN_POINT('Ctrl Pts',(-29.0530879239043,76.2395732334621,
60.2986134781171));
#176155=CARTESIAN_POINT('Ctrl Pts',(-29.0196088358868,78.4291737250614,
60.654585606508));
#176156=CARTESIAN_POINT('Ctrl Pts',(-28.997054407396,79.9505617589687,61.2063873465342));
#176157=CARTESIAN_POINT('Ctrl Pts',(-28.9605640939282,82.031973030273,62.4497133388104));
#176158=CARTESIAN_POINT('Ctrl Pts',(-28.9479315721182,82.6958287686398,
62.9401165234336));
#176159=CARTESIAN_POINT('Ctrl Pts',(-28.9236753448959,83.9002169768209,
64.0256989171434));
#176160=CARTESIAN_POINT('Ctrl Pts',(-28.9120635621438,84.4420480810486,
64.6158534954276));
#176161=CARTESIAN_POINT('Ctrl Pts',(-28.8757570605852,85.9290861966703,
66.5825031306264));
#176162=CARTESIAN_POINT('Ctrl Pts',(-28.849912430552,86.6557590389786,68.0941753323764));
#176163=CARTESIAN_POINT('Ctrl Pts',(-28.8133913070783,87.2699061763046,
70.4880258729443));
#176164=CARTESIAN_POINT('Ctrl Pts',(-28.8014073382066,87.3946594029363,
71.2917639572309));
#176165=CARTESIAN_POINT('Ctrl Pts',(-28.7766246431267,87.4843571247555,
72.9010220159898));
#176166=CARTESIAN_POINT('Ctrl Pts',(-28.7642803679124,87.4519621690978,
73.7016986292209));
#176167=CARTESIAN_POINT('Ctrl Pts',(-28.7402659878291,87.2354224393507,
75.2800816266037));
#176168=CARTESIAN_POINT('Ctrl Pts',(-28.7286237203282,87.052444662765,76.0555728901073));
#176169=CARTESIAN_POINT('Ctrl Pts',(-28.6920185593489,86.2697007508172,
78.3547530241982));
#176170=CARTESIAN_POINT('Ctrl Pts',(-28.6664353682694,85.4407395791364,
79.7818999882862));
#176171=CARTESIAN_POINT('Ctrl Pts',(-28.6175016536567,83.2796947023339,
82.2305946258017));
#176172=CARTESIAN_POINT('Ctrl Pts',(-28.5917552851528,81.9706263726822,
83.2219482748408));
#176173=CARTESIAN_POINT('Ctrl Pts',(-28.5670511147326,80.5057179591556,
83.9313635516325));
#176174=CARTESIAN_POINT('',(-29.3655838523951,68.398637325302,84.2438270474906));
#176175=CARTESIAN_POINT('Ctrl Pts',(-29.3655838526627,68.3986373254374,
84.2438270472598));
#176176=CARTESIAN_POINT('Ctrl Pts',(-29.3515369276677,68.1394510957219,
84.0755215996163));
#176177=CARTESIAN_POINT('Ctrl Pts',(-29.3375494753959,67.8866810149154,
83.8983413632411));
#176178=CARTESIAN_POINT('Ctrl Pts',(-29.3235615282545,67.6409397655344,
83.7127408512439));
#176179=CARTESIAN_POINT('Ctrl Pts',(-29.3096896422788,67.3972374869589,
83.5286803087323));
#176180=CARTESIAN_POINT('Ctrl Pts',(-29.2958172696114,67.1604481100554,
83.3363387224561));
#176181=CARTESIAN_POINT('Ctrl Pts',(-29.2818859230026,66.9311451205241,
83.136204656219));
#176182=CARTESIAN_POINT('Ctrl Pts',(-29.2769072652868,66.8491989074151,
83.0646825671448));
#176183=CARTESIAN_POINT('Ctrl Pts',(-29.2719210757759,66.7682085691129,
82.9921656866276));
#176184=CARTESIAN_POINT('Ctrl Pts',(-29.2669246850387,66.6881994399432,
82.9186776996054));
#176185=CARTESIAN_POINT('Ctrl Pts',(-29.253192592924,66.4683021601713,82.7167031423293));
#176186=CARTESIAN_POINT('Ctrl Pts',(-29.2393423955425,66.2558213412074,
82.5073393284892));
#176187=CARTESIAN_POINT('Ctrl Pts',(-29.2254372276085,66.0511772646013,
82.2911763378466));
#176188=CARTESIAN_POINT('Ctrl Pts',(-29.2113899558857,65.8444418289547,
82.0728042706834));
#176189=CARTESIAN_POINT('Ctrl Pts',(-29.1972865843269,65.6457041683321,
81.8474936242022));
#176190=CARTESIAN_POINT('Ctrl Pts',(-29.1831922031098,65.4553465105166,
81.6158677489117));
#176191=CARTESIAN_POINT('Ctrl Pts',(-29.1776338924618,65.3802763829204,
81.5245229392928));
#176192=CARTESIAN_POINT('Ctrl Pts',(-29.1720769800155,65.3065089777228,
81.4321961088971));
#176193=CARTESIAN_POINT('Ctrl Pts',(-29.1665254579116,65.2340655732272,
81.3389259770428));
#176194=CARTESIAN_POINT('Ctrl Pts',(-29.1526002959194,65.0523521396864,
81.1049718162177));
#176195=CARTESIAN_POINT('Ctrl Pts',(-29.1387540387589,64.8789555202937,
80.8651301507343));
#176196=CARTESIAN_POINT('Ctrl Pts',(-29.1249636357171,64.7142624726138,
80.620000836512));
#176197=CARTESIAN_POINT('Ctrl Pts',(-29.1112138923694,64.550055006748,80.3755942627985));
#176198=CARTESIAN_POINT('Ctrl Pts',(-29.0975196742648,64.3945000183605,
80.1259313935898));
#176199=CARTESIAN_POINT('Ctrl Pts',(-29.0838581339783,64.2479378038455,
79.8716355509124));
#176200=CARTESIAN_POINT('Ctrl Pts',(-29.0702192763373,64.1016189307598,
79.6177619228831));
#176201=CARTESIAN_POINT('Ctrl Pts',(-29.0566129880926,63.9642631393004,
79.3592709194713));
#176202=CARTESIAN_POINT('Ctrl Pts',(-29.0430165354331,63.8361638164801,
79.0968081432358));
#176203=CARTESIAN_POINT('Ctrl Pts',(-29.0294524529147,63.7083694697629,
78.8349702327134));
#176204=CARTESIAN_POINT('Ctrl Pts',(-29.0158981592045,63.5897876890377,
78.5691796794683));
#176205=CARTESIAN_POINT('Ctrl Pts',(-29.0023310824776,63.4806627565782,
78.3000992657792));
#176206=CARTESIAN_POINT('Ctrl Pts',(-28.9909220184838,63.3888955054007,
78.0738194472864));
#176207=CARTESIAN_POINT('Ctrl Pts',(-28.9795039146484,63.3038151339953,
77.8452135701696));
#176208=CARTESIAN_POINT('Ctrl Pts',(-28.968063347715,63.2255401942507,77.6146858321683));
#176209=CARTESIAN_POINT('Ctrl Pts',(-28.9545124222423,63.1328264431715,
77.3416343116226));
#176210=CARTESIAN_POINT('Ctrl Pts',(-28.9408729669519,63.0496843738629,
77.0657889256946));
#176211=CARTESIAN_POINT('Ctrl Pts',(-28.927181688329,62.9762246025752,76.7878423327904));
#176212=CARTESIAN_POINT('Ctrl Pts',(-28.9133962221623,62.9022594734155,
76.5079836389326));
#176213=CARTESIAN_POINT('Ctrl Pts',(-28.8995582171853,62.8381102929787,
76.2259950093747));
#176214=CARTESIAN_POINT('Ctrl Pts',(-28.8857051426603,62.7838370734446,
75.9425807157959));
#176215=CARTESIAN_POINT('Ctrl Pts',(-28.8717987806007,62.7293550853761,
75.6580762346949));
#176216=CARTESIAN_POINT('Ctrl Pts',(-28.8578772328365,62.6848251069248,
75.3721353741));
#176217=CARTESIAN_POINT('Ctrl Pts',(-28.8439784026856,62.6502555083076,
75.0854635881187));
#176218=CARTESIAN_POINT('Ctrl Pts',(-28.8299871301315,62.6154559840967,
74.7968851216078));
#176219=CARTESIAN_POINT('Ctrl Pts',(-28.8160188783894,62.5907496985111,
74.507566246316));
#176220=CARTESIAN_POINT('Ctrl Pts',(-28.8021123121141,62.5760933692594,
74.2182154033664));
#176221=CARTESIAN_POINT('Ctrl Pts',(-28.7906519385058,62.5640151174734,
73.9797619491884));
#176222=CARTESIAN_POINT('Ctrl Pts',(-28.779233457813,62.5587611821413,73.7412866412681));
#176223=CARTESIAN_POINT('Ctrl Pts',(-28.7678785097109,62.5602818434642,
73.5031784169355));
#176224=CARTESIAN_POINT('Ctrl Pts',(-28.7538051587481,62.5621665548957,
73.2080664905723));
#176225=CARTESIAN_POINT('Ctrl Pts',(-28.7397945616724,62.574495885705,72.9135590415678));
#176226=CARTESIAN_POINT('Ctrl Pts',(-28.7257924240596,62.5972144711822,
72.6203915837616));
#176227=CARTESIAN_POINT('Ctrl Pts',(-28.7118903162118,62.6197707575284,
72.3293184827403));
#176228=CARTESIAN_POINT('Ctrl Pts',(-28.6979965473916,62.6525684315748,
72.039566545924));
#176229=CARTESIAN_POINT('Ctrl Pts',(-28.6840579785024,62.6955019826906,
71.7518582558115));
#176230=CARTESIAN_POINT('Ctrl Pts',(-28.6791171162738,62.7107208163266,
71.6498731069214));
#176231=CARTESIAN_POINT('Ctrl Pts',(-28.6741706248306,62.7272127669116,
71.5481447522842));
#176232=CARTESIAN_POINT('Ctrl Pts',(-28.6692161373386,62.744971557244,71.446705358476));
#176233=CARTESIAN_POINT('Ctrl Pts',(-28.6547265382075,62.7969078581004,
71.1500417469971));
#176234=CARTESIAN_POINT('Ctrl Pts',(-28.6401112616264,62.8597417243038,
70.8558425314139));
#176235=CARTESIAN_POINT('Ctrl Pts',(-28.6253112490716,62.9332865719164,
70.5648824322531));
#176236=CARTESIAN_POINT('Ctrl Pts',(-28.6106590834907,63.0060967321,70.2768289232089));
#176237=CARTESIAN_POINT('Ctrl Pts',(-28.5958258543968,63.0894049728235,
69.9919503385894));
#176238=CARTESIAN_POINT('Ctrl Pts',(-28.5807542555663,63.1829792308997,
69.7109948177064));
#176239=CARTESIAN_POINT('Ctrl Pts',(-28.5763682341958,63.2102104954961,
69.6292332917668));
#176240=CARTESIAN_POINT('Ctrl Pts',(-28.5719620257246,63.2383108366438,
69.5478039687374));
#176241=CARTESIAN_POINT('Ctrl Pts',(-28.5675342178229,63.2672737070204,
69.46672519));
#176242=CARTESIAN_POINT('',(-29.3666998404582,61.9513562005121,72.9886184577035));
#176243=CARTESIAN_POINT('Ctrl Pts',(-29.3655838529308,68.398637325302,84.2438270474913));
#176244=CARTESIAN_POINT('Ctrl Pts',(-29.3663355387957,67.4434486808997,
83.6844513479272));
#176245=CARTESIAN_POINT('Ctrl Pts',(-29.3681108351944,66.5594392044141,
83.0049447002618));
#176246=CARTESIAN_POINT('Ctrl Pts',(-29.3658391655718,64.9568327293927,
81.398488742438));
#176247=CARTESIAN_POINT('Ctrl Pts',(-29.3646108212369,64.2514758328537,
80.473804649592));
#176248=CARTESIAN_POINT('Ctrl Pts',(-29.3665216258898,63.1238041156622,
78.508904879264));
#176249=CARTESIAN_POINT('Ctrl Pts',(-29.3680011405059,62.6942531079225,
77.4766733383823));
#176250=CARTESIAN_POINT('Ctrl Pts',(-29.3656365873995,62.1043691345675,
75.2854002296065));
#176251=CARTESIAN_POINT('Ctrl Pts',(-29.3647732455976,61.9527377954335,
74.1368535505302));
#176252=CARTESIAN_POINT('Ctrl Pts',(-29.3658340844142,61.9516996901141,
72.9886310426174));
#176253=CARTESIAN_POINT('Ctrl Pts',(-29.3673261860752,61.9511076972435,
72.988609352938));
#176254=CARTESIAN_POINT('Ctrl Pts',(-29.3668532876725,61.9512817219048,
72.9626462799096));
#176255=CARTESIAN_POINT('Ctrl Pts',(-29.3663803892696,61.9515326191958,
72.9366844270784));
#176256=CARTESIAN_POINT('Ctrl Pts',(-29.3659074908668,61.951860403834,72.9107242579373));
#176257=CARTESIAN_POINT('Origin',(-28.5675364832709,75.,72.98888938658));
#176258=CARTESIAN_POINT('',(-27.5675364826718,89.5000000000001,66.2250147575798));
#176259=CARTESIAN_POINT('',(-27.56753648264,89.5,79.7527640156553));
#176260=CARTESIAN_POINT('Ctrl Pts',(-27.5675364817657,89.5,66.2250147580311));
#176261=CARTESIAN_POINT('Ctrl Pts',(-30.4269114864224,89.5,72.9888893867033));
#176262=CARTESIAN_POINT('Ctrl Pts',(-27.5675364816388,89.5,79.7527640154292));
#176263=CARTESIAN_POINT('',(-27.5675364826398,88.1076872567925,63.8134583462434));
#176264=CARTESIAN_POINT('Origin',(-27.5675364832709,75.,72.98888938658));
#176265=CARTESIAN_POINT('',(-27.5675364826717,76.3923127432732,57.0495837172059));
#176266=CARTESIAN_POINT('Ctrl Pts',(-27.5675364817724,76.3923127436787,
57.0495837174391));
#176267=CARTESIAN_POINT('Ctrl Pts',(-30.4269114864031,82.2500000000807,
60.4315210317516));
#176268=CARTESIAN_POINT('Ctrl Pts',(-27.567536481677,88.1076872565176,63.8134583460843));
#176269=CARTESIAN_POINT('',(-27.5675364826717,73.6076872567269,57.0495837172059));
#176270=CARTESIAN_POINT('Origin',(-27.5675364832709,75.,72.98888938658));
#176271=CARTESIAN_POINT('',(-27.5675364826398,61.8923127432075,63.8134583462433));
#176272=CARTESIAN_POINT('Ctrl Pts',(-27.567536481677,61.8923127434824,63.8134583460842));
#176273=CARTESIAN_POINT('Ctrl Pts',(-30.426911486403,67.7499999999193,60.4315210317516));
#176274=CARTESIAN_POINT('Ctrl Pts',(-27.5675364817723,73.6076872563213,
57.0495837174391));
#176275=CARTESIAN_POINT('',(-27.5675364826718,60.5,66.2250147575798));
#176276=CARTESIAN_POINT('Origin',(-27.5675364832709,75.,72.98888938658));
#176277=CARTESIAN_POINT('',(-27.5675364826718,60.5,79.7527640155803));
#176278=CARTESIAN_POINT('Ctrl Pts',(-27.5675364817658,60.5,66.2250147580311));
#176279=CARTESIAN_POINT('Ctrl Pts',(-30.4269114864094,60.5,72.9888893866725));
#176280=CARTESIAN_POINT('Ctrl Pts',(-27.5675364816705,60.5,79.7527640153542));
#176281=CARTESIAN_POINT('',(-27.5675364826398,61.8923127432075,82.1643204269167));
#176282=CARTESIAN_POINT('Origin',(-27.5675364832709,75.,72.98888938658));
#176283=CARTESIAN_POINT('',(-27.5675364826717,73.6076872567269,88.9281950559541));
#176284=CARTESIAN_POINT('Ctrl Pts',(-27.5675364817723,73.6076872563214,
88.9281950557209));
#176285=CARTESIAN_POINT('Ctrl Pts',(-30.4269114864031,67.7499999999193,
85.5462577414084));
#176286=CARTESIAN_POINT('Ctrl Pts',(-27.567536481677,61.8923127434824,82.1643204270758));
#176287=CARTESIAN_POINT('',(-27.5675364816388,75.,88.9888893864172));
#176288=CARTESIAN_POINT('Origin',(-27.5675364832709,75.,72.98888938658));
#176289=CARTESIAN_POINT('',(-29.5675364841684,75.,86.9888893874774));
#176290=CARTESIAN_POINT('',(-28.5675364832709,75.,87.98888938658));
#176291=CARTESIAN_POINT('Origin',(-29.5675364832709,75.,72.98888938658));
#176292=CARTESIAN_POINT('',(-27.5675364826399,76.3923127432082,88.9281950559916));
#176293=CARTESIAN_POINT('Origin',(-27.5675364832709,75.,72.98888938658));
#176294=CARTESIAN_POINT('',(-27.5675364826716,88.1076872567275,82.1643204269542));
#176295=CARTESIAN_POINT('Ctrl Pts',(-27.5675364817722,88.1076872563225,
82.1643204271884));
#176296=CARTESIAN_POINT('Ctrl Pts',(-30.426911486403,82.2499999999205,85.5462577415009));
#176297=CARTESIAN_POINT('Ctrl Pts',(-27.5675364816771,76.3923127434836,
88.9281950558335));
#176298=CARTESIAN_POINT('Origin',(-27.5675364832709,75.,72.98888938658));
#176299=CARTESIAN_POINT('Origin',(-17.5675364832709,75.,72.98888938658));
#176300=CARTESIAN_POINT('',(-18.5675364839018,89.5,66.2250147575047));
#176301=CARTESIAN_POINT('',(-18.56753648387,89.5,79.7527640155803));
#176302=CARTESIAN_POINT('Ctrl Pts',(-18.5675364848006,89.5,79.7527640151869));
#176303=CARTESIAN_POINT('Ctrl Pts',(-15.7081614801611,89.5,72.9888893866029));
#176304=CARTESIAN_POINT('Ctrl Pts',(-18.567536484777,89.5,66.2250147580289));
#176305=CARTESIAN_POINT('',(-18.5675364838598,88.1076872567062,82.1643204269666));
#176306=CARTESIAN_POINT('Origin',(-18.5675364832709,75.,72.98888938658));
#176307=CARTESIAN_POINT('',(-18.567536483878,76.3923127432567,88.9281950559637));
#176308=CARTESIAN_POINT('Ctrl Pts',(-18.5675364847385,88.1076872562589,
82.1643204272251));
#176309=CARTESIAN_POINT('Ctrl Pts',(-15.7081614801807,82.2499999999541,
85.5462577414815));
#176310=CARTESIAN_POINT('Ctrl Pts',(-18.5675364847937,76.3923127436291,
88.9281950557496));
#176311=CARTESIAN_POINT('',(-18.567536483878,73.6076872567433,88.9281950559637));
#176312=CARTESIAN_POINT('Origin',(-18.5675364832709,75.,72.98888938658));
#176313=CARTESIAN_POINT('',(-18.5675364838598,61.8923127432938,82.1643204269665));
#176314=CARTESIAN_POINT('Ctrl Pts',(-18.5675364847937,73.607687256371,88.9281950557496));
#176315=CARTESIAN_POINT('Ctrl Pts',(-15.7081614801806,67.750000000046,85.5462577414815));
#176316=CARTESIAN_POINT('Ctrl Pts',(-18.5675364847385,61.8923127437411,
82.1643204272251));
#176317=CARTESIAN_POINT('',(-18.56753648387,60.5,79.7527640155802));
#176318=CARTESIAN_POINT('Origin',(-18.5675364832709,75.,72.98888938658));
#176319=CARTESIAN_POINT('',(-18.5675364839017,60.5,66.2250147575048));
#176320=CARTESIAN_POINT('Ctrl Pts',(-18.5675364848005,60.5,79.7527640151869));
#176321=CARTESIAN_POINT('Ctrl Pts',(-15.7081614801611,60.5,72.9888893866029));
#176322=CARTESIAN_POINT('Ctrl Pts',(-18.5675364847769,60.5,66.225014758029));
#176323=CARTESIAN_POINT('',(-18.5675364838598,61.8923127432938,63.8134583461934));
#176324=CARTESIAN_POINT('Origin',(-18.5675364832709,75.,72.98888938658));
#176325=CARTESIAN_POINT('',(-18.5675364838782,73.6076872567434,57.0495837171963));
#176326=CARTESIAN_POINT('Ctrl Pts',(-18.5675364847385,61.8923127437411,
63.8134583459349));
#176327=CARTESIAN_POINT('Ctrl Pts',(-15.7081614801806,67.750000000046,60.4315210316784));
#176328=CARTESIAN_POINT('Ctrl Pts',(-18.5675364847938,73.6076872563712,
57.0495837174103));
#176329=CARTESIAN_POINT('',(-18.5675364848006,75.,56.9888893868452));
#176330=CARTESIAN_POINT('Origin',(-18.5675364832709,75.,72.98888938658));
#176331=CARTESIAN_POINT('',(-16.5675364823734,75.,58.9888893856825));
#176332=CARTESIAN_POINT('',(-17.5675364832709,75.,57.98888938658));
#176333=CARTESIAN_POINT('Origin',(-16.5675364832709,75.,72.98888938658));
#176334=CARTESIAN_POINT('',(-18.5675364838598,76.3923127432944,57.0495837172181));
#176335=CARTESIAN_POINT('Origin',(-18.5675364832709,75.,72.98888938658));
#176336=CARTESIAN_POINT('',(-18.5675364838783,88.107687256744,63.8134583462153));
#176337=CARTESIAN_POINT('Ctrl Pts',(-18.5675364847385,76.3923127437421,
57.0495837174757));
#176338=CARTESIAN_POINT('Ctrl Pts',(-15.7081614801806,82.2500000000471,
60.4315210317322));
#176339=CARTESIAN_POINT('Ctrl Pts',(-18.5675364847939,88.1076872563724,
63.8134583460004));
#176340=CARTESIAN_POINT('Origin',(-18.5675364832709,75.,72.98888938658));
#176341=CARTESIAN_POINT('Origin',(-31.5405364832709,75.,72.98888938658));
#176342=CARTESIAN_POINT('',(-27.5675364832709,76.39231274307,57.04958371709));
#176343=CARTESIAN_POINT('',(-27.5675364832709,73.60768725693,57.04958371709));
#176344=CARTESIAN_POINT('Origin',(-16.5675364832709,75.,89.73204719308));
#176345=CARTESIAN_POINT('',(-27.5675364832709,76.39231274307,88.92819505607));
#176346=CARTESIAN_POINT('',(-27.5675364832709,88.10768725693,82.164320426837));
#176347=CARTESIAN_POINT('Origin',(-16.5675364832709,75.,56.24573158008));
#176348=CARTESIAN_POINT('',(-27.5675364832709,61.89231274307,63.813458346323));
#176349=CARTESIAN_POINT('Origin',(-16.5675364832709,89.5,64.61731048333));
#176350=CARTESIAN_POINT('',(-27.5675364832709,88.10768725693,63.813458346323));
#176351=CARTESIAN_POINT('Origin',(-31.5405364832709,75.,72.98888938658));
#176352=CARTESIAN_POINT('',(-27.5675364832709,60.5,66.225014757346));
#176353=CARTESIAN_POINT('Origin',(-31.5405364832709,75.,72.98888938658));
#176354=CARTESIAN_POINT('',(-27.5675364832709,89.5,66.225014757346));
#176355=CARTESIAN_POINT('Origin',(-16.5675364832709,89.5,81.36046828983));
#176356=CARTESIAN_POINT('',(-27.5675364832709,89.5,79.752764015814));
#176357=CARTESIAN_POINT('Origin',(-16.5675364832709,60.5,81.36046828983));
#176358=CARTESIAN_POINT('',(-27.5675364832709,61.89231274307,82.164320426837));
#176359=CARTESIAN_POINT('',(-27.5675364832709,73.60768725693,88.92819505607));
#176360=CARTESIAN_POINT('Origin',(-31.5405364832709,75.,72.98888938658));
#176361=CARTESIAN_POINT('Origin',(-31.5405364832709,75.,72.98888938658));
#176362=CARTESIAN_POINT('',(-27.5675364832709,60.5,79.752764015814));
#176363=CARTESIAN_POINT('Origin',(-31.5405364832709,75.,72.98888938658));
#176364=CARTESIAN_POINT('Origin',(-16.5675364832709,60.5,64.61731048333));
#176365=CARTESIAN_POINT('Origin',(-29.5675364832709,75.,72.98888938658));
#176366=CARTESIAN_POINT('Ctrl Pts',(-29.4235335827009,62.44414915689,76.731819067654));
#176367=CARTESIAN_POINT('Ctrl Pts',(-29.3785752787509,61.85675590838,74.761378091484));
#176368=CARTESIAN_POINT('Ctrl Pts',(-29.2886586708509,61.6274868926,70.540717962258));
#176369=CARTESIAN_POINT('Ctrl Pts',(-29.1537837590009,64.19287556944,64.740945094149));
#176370=CARTESIAN_POINT('Ctrl Pts',(-29.0189088471409,69.10991196088,60.73624495104));
#176371=CARTESIAN_POINT('Ctrl Pts',(-28.8840339352909,75.308544783193,59.3974994093));
#176372=CARTESIAN_POINT('Ctrl Pts',(-28.7491590234309,81.440049640839,61.01614190121));
#176373=CARTESIAN_POINT('Ctrl Pts',(-28.6142841115809,86.17025756511,65.239934789744));
#176374=CARTESIAN_POINT('Ctrl Pts',(-28.4794091997309,88.46992237593,71.14982987547));
#176375=CARTESIAN_POINT('Ctrl Pts',(-28.3445342878709,87.8386577141,77.459886586808));
#176376=CARTESIAN_POINT('Ctrl Pts',(-28.2096593760209,84.413821081764,82.797096210383));
#176377=CARTESIAN_POINT('Ctrl Pts',(-28.0747844641709,78.940624888933,86.00013159165));
#176378=CARTESIAN_POINT('Ctrl Pts',(-27.9399095523109,72.609985526153,86.37204219574));
#176379=CARTESIAN_POINT('Ctrl Pts',(-27.8050346404609,66.799390990941,83.83190373521));
#176380=CARTESIAN_POINT('Ctrl Pts',(-27.6701597286009,62.77317238826,78.932426619492));
#176381=CARTESIAN_POINT('Ctrl Pts',(-27.5352848167509,61.40739728363,72.7396913102611));
#176382=CARTESIAN_POINT('Ctrl Pts',(-27.4004099049009,62.99924558451,66.601179175152));
#176383=CARTESIAN_POINT('Ctrl Pts',(-27.2655349930409,67.202345967366,61.8525731252));
#176384=CARTESIAN_POINT('Ctrl Pts',(-27.1306600811909,73.102143042981,59.52712548816));
#176385=CARTESIAN_POINT('Ctrl Pts',(-26.9957851693409,79.414896067747,60.13083195176));
#176386=CARTESIAN_POINT('Ctrl Pts',(-26.8609102574809,84.767008940321,63.532331627755));
#176387=CARTESIAN_POINT('Ctrl Pts',(-26.7260353456309,87.99391188448,68.991489954176));
#176388=CARTESIAN_POINT('Ctrl Pts',(-26.5911604337809,88.39346095746,75.320445064586));
#176389=CARTESIAN_POINT('Ctrl Pts',(-26.4562855219229,85.87871800947,81.142075432836));
#176390=CARTESIAN_POINT('Ctrl Pts',(-26.3214106100699,80.996867631233,85.18964866916));
#176391=CARTESIAN_POINT('Ctrl Pts',(-26.1865356982159,74.8101548300925,
86.58245060783));
#176392=CARTESIAN_POINT('Ctrl Pts',(-26.0516607863629,68.66475068801,85.01742067074));
#176393=CARTESIAN_POINT('Ctrl Pts',(-25.9167858745089,63.89783716987,80.835094323236));
#176394=CARTESIAN_POINT('Ctrl Pts',(-25.7819109626559,61.54665231168,74.945508333151));
#176395=CARTESIAN_POINT('Ctrl Pts',(-25.6470360508029,62.12278386605,68.630175581195));
#176396=CARTESIAN_POINT('Ctrl Pts',(-25.5121611389499,65.500901269506,63.263275982751));
#176397=CARTESIAN_POINT('Ctrl Pts',(-25.3772862270959,70.945844710137,60.01251283554));
#176398=CARTESIAN_POINT('Ctrl Pts',(-25.2424113152429,77.273267122096,59.58553507798));
#176399=CARTESIAN_POINT('Ctrl Pts',(-25.1524947073409,81.160959972294,61.24456506882));
#176400=CARTESIAN_POINT('Ctrl Pts',(-25.1075364033899,82.811656888157,62.4704803028));
#176401=CARTESIAN_POINT('Ctrl Pts',(-29.5803515522709,62.73283940876,76.645759801271));
#176402=CARTESIAN_POINT('Ctrl Pts',(-29.5353932483209,62.15895179256,74.720624165918));
#176403=CARTESIAN_POINT('Ctrl Pts',(-29.4454766404109,61.93495424192,70.597007514748));
#176404=CARTESIAN_POINT('Ctrl Pts',(-29.3106017285609,64.44135824997,64.930585855648));
#176405=CARTESIAN_POINT('Ctrl Pts',(-29.1757268167109,69.245339740392,61.01796373317));
#176406=CARTESIAN_POINT('Ctrl Pts',(-29.0408519048509,75.301450570921,59.70999928245));
#176407=CARTESIAN_POINT('Ctrl Pts',(-28.9059769930009,81.291976875715,61.29142515603));
#176408=CARTESIAN_POINT('Ctrl Pts',(-28.7711020811409,85.91342555028,65.418102536579));
#176409=CARTESIAN_POINT('Ctrl Pts',(-28.6362271692909,88.16021534517,71.192114429511));
#176410=CARTESIAN_POINT('Ctrl Pts',(-28.5013522574409,87.5434650286,77.357087236615));
#176411=CARTESIAN_POINT('Ctrl Pts',(-28.3664773455809,84.197373911983,82.571581131104));
#176412=CARTESIAN_POINT('Ctrl Pts',(-28.2316024337309,78.850020117821,85.70097075929));
#176413=CARTESIAN_POINT('Ctrl Pts',(-28.0967275218809,72.664937905644,86.06433021321));
#176414=CARTESIAN_POINT('Ctrl Pts',(-27.9618526100209,66.987943396495,83.58259585616));
#176415=CARTESIAN_POINT('Ctrl Pts',(-27.8269776981709,63.05429757737,78.795769910022));
#176416=CARTESIAN_POINT('Ctrl Pts',(-27.6921027863109,61.71992504067,72.7454209940753));
#176417=CARTESIAN_POINT('Ctrl Pts',(-27.5572278744609,63.27517278834,66.748048526563));
#176418=CARTESIAN_POINT('Ctrl Pts',(-27.4223529626109,67.381633435404,62.108624745));
#176419=CARTESIAN_POINT('Ctrl Pts',(-27.2874780507509,73.145779496604,59.83664493523));
#176420=CARTESIAN_POINT('Ctrl Pts',(-27.1526031389009,79.31338662218,60.42647068511));
#176421=CARTESIAN_POINT('Ctrl Pts',(-27.0177282270509,84.542441102891,63.749761420078));
#176422=CARTESIAN_POINT('Ctrl Pts',(-26.8828533151909,87.69514951931,69.083400113308));
#176423=CARTESIAN_POINT('Ctrl Pts',(-26.7479784033409,88.08551196495,75.266836798267));
#176424=CARTESIAN_POINT('Ctrl Pts',(-26.6131034914909,85.62858921442,80.954613399192));
#176425=CARTESIAN_POINT('Ctrl Pts',(-26.4782285796339,80.858984723211,84.90912285579));
#176426=CARTESIAN_POINT('Ctrl Pts',(-26.3433536677799,74.8145198429094,
86.26990081237));
#176427=CARTESIAN_POINT('Ctrl Pts',(-26.2084787559269,68.810413832813,84.74085480758));
#176428=CARTESIAN_POINT('Ctrl Pts',(-26.0736038440729,64.15310351731,80.654690549114));
#176429=CARTESIAN_POINT('Ctrl Pts',(-25.9387289322199,61.85597824913,74.900520795182));
#176430=CARTESIAN_POINT('Ctrl Pts',(-25.8038540203669,62.41886310557,68.730393256763));
#176431=CARTESIAN_POINT('Ctrl Pts',(-25.6689791085129,65.719309184614,63.486892033801));
#176432=CARTESIAN_POINT('Ctrl Pts',(-25.5341041966599,71.039059827646,60.31087201977));
#176433=CARTESIAN_POINT('Ctrl Pts',(-25.3992292848069,77.220999054703,59.89371154324));
#176434=CARTESIAN_POINT('Ctrl Pts',(-25.3093126769049,81.019304173067,61.51459630666));
#176435=CARTESIAN_POINT('Ctrl Pts',(-25.2643543729539,82.632047459634,62.71232469914));
#176436=CARTESIAN_POINT('Ctrl Pts',(-29.7371695218309,63.02152966063,76.559700534901));
#176437=CARTESIAN_POINT('Ctrl Pts',(-29.6922112178809,62.46114767674,74.679870240367));
#176438=CARTESIAN_POINT('Ctrl Pts',(-29.6022946099809,62.24242159123,70.653297067253));
#176439=CARTESIAN_POINT('Ctrl Pts',(-29.4674196981209,64.68984093049,65.120226617163));
#176440=CARTESIAN_POINT('Ctrl Pts',(-29.3325447862709,69.380767519885,61.29968251531));
#176441=CARTESIAN_POINT('Ctrl Pts',(-29.1976698744209,75.2943563586239,
60.02249915561));
#176442=CARTESIAN_POINT('Ctrl Pts',(-29.0627949625609,81.143904110566,61.56670841083));
#176443=CARTESIAN_POINT('Ctrl Pts',(-28.9279200507109,85.65659353544,65.596270283389));
#176444=CARTESIAN_POINT('Ctrl Pts',(-28.7930451388509,87.8505083144,71.23439898352));
#176445=CARTESIAN_POINT('Ctrl Pts',(-28.6581702270009,87.24827234311,77.254287886388));
#176446=CARTESIAN_POINT('Ctrl Pts',(-28.5232953151509,83.98092674223,82.346066051798));
#176447=CARTESIAN_POINT('Ctrl Pts',(-28.3884204032909,78.759415346747,85.40180992691));
#176448=CARTESIAN_POINT('Ctrl Pts',(-28.2535454914409,72.719890285177,85.75661823069));
#176449=CARTESIAN_POINT('Ctrl Pts',(-28.1186705795909,67.176495802086,83.33328797713));
#176450=CARTESIAN_POINT('Ctrl Pts',(-27.9837956677309,63.33542276651,78.659113200594));
#176451=CARTESIAN_POINT('Ctrl Pts',(-27.8489207558809,62.03245279771,72.7511506779378));
#176452=CARTESIAN_POINT('Ctrl Pts',(-27.7140458440209,63.55109999215,66.894917878018));
#176453=CARTESIAN_POINT('Ctrl Pts',(-27.5791709321709,67.560920903401,62.36467636483));
#176454=CARTESIAN_POINT('Ctrl Pts',(-27.4442960203209,73.189415950175,60.1461643823));
#176455=CARTESIAN_POINT('Ctrl Pts',(-27.3094211084609,79.211877176565,60.72210941845));
#176456=CARTESIAN_POINT('Ctrl Pts',(-27.1745461966109,84.317873265426,63.967191212364));
#176457=CARTESIAN_POINT('Ctrl Pts',(-27.0396712847609,87.39638715412,69.175310272392));
#176458=CARTESIAN_POINT('Ctrl Pts',(-26.9047963729009,87.77756297245,75.213228531899));
#176459=CARTESIAN_POINT('Ctrl Pts',(-26.7699214610509,85.3784604194,80.767151365512));
#176460=CARTESIAN_POINT('Ctrl Pts',(-26.6350465492009,80.72110181523,84.62859704241));
#176461=CARTESIAN_POINT('Ctrl Pts',(-26.5001716373439,74.8188848557683,
85.95735101692));
#176462=CARTESIAN_POINT('Ctrl Pts',(-26.3652967254909,68.956076977649,84.46428894445));
#176463=CARTESIAN_POINT('Ctrl Pts',(-26.2304218136369,64.40836986477,80.47428677502));
#176464=CARTESIAN_POINT('Ctrl Pts',(-26.0955469017839,62.16530418659,74.855533257242));
#176465=CARTESIAN_POINT('Ctrl Pts',(-25.9606719899309,62.71494234507,68.830610932353));
#176466=CARTESIAN_POINT('Ctrl Pts',(-25.8257970780769,65.937717099708,63.710508084863));
#176467=CARTESIAN_POINT('Ctrl Pts',(-25.6909221662239,71.132274945143,60.609231204));
#176468=CARTESIAN_POINT('Ctrl Pts',(-25.5560472543709,77.168730987308,60.20188800851));
#176469=CARTESIAN_POINT('Ctrl Pts',(-25.4661306464689,80.877648373842,61.7846275445));
#176470=CARTESIAN_POINT('Ctrl Pts',(-25.4211723425179,82.452438031115,62.95416909548));
#176471=CARTESIAN_POINT('Ctrl Pts',(-29.8939874914009,63.3102199125,76.473641268518));
#176472=CARTESIAN_POINT('Ctrl Pts',(-29.8490291874409,62.76334356092,74.639116314802));
#176473=CARTESIAN_POINT('Ctrl Pts',(-29.7591125795409,62.54988894054,70.709586619743));
#176474=CARTESIAN_POINT('Ctrl Pts',(-29.6242376676909,64.93832361102,65.309867378662));
#176475=CARTESIAN_POINT('Ctrl Pts',(-29.4893627558309,69.516195299397,61.58140129744));
#176476=CARTESIAN_POINT('Ctrl Pts',(-29.3544878439809,75.2872621463521,
60.33499902876));
#176477=CARTESIAN_POINT('Ctrl Pts',(-29.2196129321309,80.995831345442,61.84199166565));
#176478=CARTESIAN_POINT('Ctrl Pts',(-29.0847380202709,85.39976152061,65.774438030224));
#176479=CARTESIAN_POINT('Ctrl Pts',(-28.9498631084209,87.54080128363,71.276683537561));
#176480=CARTESIAN_POINT('Ctrl Pts',(-28.8149881965709,86.95307965761,77.151488536196));
#176481=CARTESIAN_POINT('Ctrl Pts',(-28.6801132847109,83.764479572449,82.120550972519));
#176482=CARTESIAN_POINT('Ctrl Pts',(-28.5452383728609,78.668810575635,85.10264909454));
#176483=CARTESIAN_POINT('Ctrl Pts',(-28.4103634610009,72.774842664668,85.44890624816));
#176484=CARTESIAN_POINT('Ctrl Pts',(-28.2754885491509,67.365048207639,83.08398009808));
#176485=CARTESIAN_POINT('Ctrl Pts',(-28.1406136373009,63.61654795562,78.522456491124));
#176486=CARTESIAN_POINT('Ctrl Pts',(-28.0057387254409,62.34498055475,72.7568803617516));
#176487=CARTESIAN_POINT('Ctrl Pts',(-27.8708638135909,63.82702719598,67.041787229428));
#176488=CARTESIAN_POINT('Ctrl Pts',(-27.7359889017409,67.740208371439,62.62072798463));
#176489=CARTESIAN_POINT('Ctrl Pts',(-27.6011139898809,73.233052403798,60.45568382937));
#176490=CARTESIAN_POINT('Ctrl Pts',(-27.4662390780309,79.110367730999,61.0177481518));
#176491=CARTESIAN_POINT('Ctrl Pts',(-27.3313641661709,84.093305427996,64.184621004688));
#176492=CARTESIAN_POINT('Ctrl Pts',(-27.1964892543209,87.09762478895,69.267220431524));
#176493=CARTESIAN_POINT('Ctrl Pts',(-27.0616143424709,87.46961397994,75.159620265581));
#176494=CARTESIAN_POINT('Ctrl Pts',(-26.9267394306109,85.12833162435,80.579689331869));
#176495=CARTESIAN_POINT('Ctrl Pts',(-26.7918645187609,80.583218907207,84.34807122905));
#176496=CARTESIAN_POINT('Ctrl Pts',(-26.6569896069109,74.8232498685848,
85.64480122147));
#176497=CARTESIAN_POINT('Ctrl Pts',(-26.5221146950539,69.101740122451,84.18772308129));
#176498=CARTESIAN_POINT('Ctrl Pts',(-26.3872397832009,64.6636362122,80.293883000897));
#176499=CARTESIAN_POINT('Ctrl Pts',(-26.2523648713479,62.47463012405,74.810545719273));
#176500=CARTESIAN_POINT('Ctrl Pts',(-26.1174899594939,63.01102158459,68.93082860792));
#176501=CARTESIAN_POINT('Ctrl Pts',(-25.9826150476409,66.156125014816,63.934124135913));
#176502=CARTESIAN_POINT('Ctrl Pts',(-25.8477401357879,71.225490062652,60.90759038823));
#176503=CARTESIAN_POINT('Ctrl Pts',(-25.7128652239349,77.116462919915,60.51006447377));
#176504=CARTESIAN_POINT('Ctrl Pts',(-25.6229486160329,80.735992574615,62.05465878235));
#176505=CARTESIAN_POINT('Ctrl Pts',(-25.5779903120819,82.272828602591,63.196013491817));
#176506=CARTESIAN_POINT('Ctrl Pts',(-29.3659074908668,61.9518604038339,
72.9107242579373));
#176507=CARTESIAN_POINT('Ctrl Pts',(-29.3564982338579,61.9539954571989,
72.4863077052749));
#176508=CARTESIAN_POINT('Ctrl Pts',(-29.3471083830932,61.9767196234027,
72.0619896297967));
#176509=CARTESIAN_POINT('Ctrl Pts',(-29.3281064148669,62.0654264883602,
71.201562242445));
#176510=CARTESIAN_POINT('Ctrl Pts',(-29.3185886994199,62.1328230949399,
70.7675430471975));
#176511=CARTESIAN_POINT('Ctrl Pts',(-29.289671755828,62.4039391099025,69.4669196437128));
#176512=CARTESIAN_POINT('Ctrl Pts',(-29.2702173421716,62.6747728688316,
68.6164798036698));
#176513=CARTESIAN_POINT('Ctrl Pts',(-29.2253010143749,63.4868923496922,
66.7420249311327));
#176514=CARTESIAN_POINT('Ctrl Pts',(-29.1996910938571,64.0862024991567,
65.740124142594));
#176515=CARTESIAN_POINT('Ctrl Pts',(-29.1554746275351,65.3421021879449,
64.1717374147651));
#176516=CARTESIAN_POINT('Ctrl Pts',(-29.1369985242667,65.9388441111051,
63.5616726039035));
#176517=CARTESIAN_POINT('Ctrl Pts',(-29.0982964755062,67.2973649983439,
62.4171369941487));
#176518=CARTESIAN_POINT('Ctrl Pts',(-29.0780486891563,68.0695483513939,
61.8944315984558));
#176519=CARTESIAN_POINT('Ctrl Pts',(-29.0439062068915,69.4272642755156,
61.1728740841599));
#176520=CARTESIAN_POINT('Ctrl Pts',(-29.030205421648,69.9843041918136,60.9255555918941));
#176521=CARTESIAN_POINT('Ctrl Pts',(-29.005076972165,71.0608373329505,60.5371020287685));
#176522=CARTESIAN_POINT('Ctrl Pts',(-28.9935432859152,71.5729114864887,
60.3872947629798));
#176523=CARTESIAN_POINT('Ctrl Pts',(-28.9678778363645,72.7305854823305,
60.1235672511679));
#176524=CARTESIAN_POINT('Ctrl Pts',(-28.9537518307,73.3799877554864,60.0257510402805));
#176525=CARTESIAN_POINT('Ctrl Pts',(-28.9272333959977,74.5867108664625,
59.935094182849));
#176526=CARTESIAN_POINT('Ctrl Pts',(-28.9148514570428,75.1431274515827,
59.9285573507583));
#176527=CARTESIAN_POINT('Ctrl Pts',(-28.894245021341,76.0531290116093,59.9765702061662));
#176528=CARTESIAN_POINT('Ctrl Pts',(-28.8862433423036,76.4068465772595,
60.009980381597));
#176529=CARTESIAN_POINT('Ctrl Pts',(-28.8628405996903,77.4569079514817,
60.1535672105847));
#176530=CARTESIAN_POINT('Ctrl Pts',(-28.847775368609,78.1460495216983,60.3060100929327));
#176531=CARTESIAN_POINT('Ctrl Pts',(-28.8184409165635,79.45395328342,60.7071765218225));
#176532=CARTESIAN_POINT('Ctrl Pts',(-28.8041641772532,80.0746521341312,
60.9501490391669));
#176533=CARTESIAN_POINT('Ctrl Pts',(-28.7788127382842,81.1069822190985,
61.4473862647356));
#176534=CARTESIAN_POINT('Ctrl Pts',(-28.7678363057078,81.5291068465773,
61.6800814496751));
#176535=CARTESIAN_POINT('Ctrl Pts',(-28.7507665891748,82.1645694268526,
62.0782275091685));
#176536=CARTESIAN_POINT('Ctrl Pts',(-28.7446895648506,82.3876760344657,
62.2279149754432));
#176537=CARTESIAN_POINT('Ctrl Pts',(-28.7305581875881,82.9046652249705,
62.5990232838268));
#176538=CARTESIAN_POINT('Ctrl Pts',(-28.7225807105516,83.1937714381268,
62.8259749995625));
#176539=CARTESIAN_POINT('Ctrl Pts',(-28.7013577352784,83.9441115759072,
63.4680045318863));
#176540=CARTESIAN_POINT('Ctrl Pts',(-28.6882685949821,84.3866748563063,
63.9049517853678));
#176541=CARTESIAN_POINT('Ctrl Pts',(-28.6666857942288,85.0510748040619,
64.6603255432425));
#176542=CARTESIAN_POINT('Ctrl Pts',(-28.6583249479937,85.2931207574033,
64.961113426));
#176543=CARTESIAN_POINT('Ctrl Pts',(-28.6410882186472,85.7535049093648,
65.5877304124733));
#176544=CARTESIAN_POINT('Ctrl Pts',(-28.63214885462,85.9714103310952,65.9138967139593));
#176545=CARTESIAN_POINT('Ctrl Pts',(-28.6167537591334,86.3191113527359,
66.4890147020966));
#176546=CARTESIAN_POINT('Ctrl Pts',(-28.6103288702727,86.4563168757537,
66.7334789894221));
#176547=CARTESIAN_POINT('Ctrl Pts',(-28.5984854509473,86.6980408423123,
67.1993015118161));
#176548=CARTESIAN_POINT('Ctrl Pts',(-28.5930704354805,86.8042213244609,
67.419152406551));
#176549=CARTESIAN_POINT('Ctrl Pts',(-28.5762221012571,87.1197468350586,
68.1228960845822));
#176550=CARTESIAN_POINT('Ctrl Pts',(-28.5650682168193,87.3058434984508,
68.6170223101508));
#176551=CARTESIAN_POINT('Ctrl Pts',(-28.5457936377573,87.5752215663412,
69.4876053155158));
#176552=CARTESIAN_POINT('Ctrl Pts',(-28.5376684111527,87.6727047519809,
69.8596919164948));
#176553=CARTESIAN_POINT('Ctrl Pts',(-28.5232331813806,87.8144021310478,
70.5161458065337));
#176554=CARTESIAN_POINT('Ctrl Pts',(-28.5169818665082,87.8658550860038,
70.7989828665514));
#176555=CARTESIAN_POINT('Ctrl Pts',(-28.4996699092958,87.9802350822815,
71.5701860550689));
#176556=CARTESIAN_POINT('Ctrl Pts',(-28.4882983323491,88.0251587755903,
72.0612388390642));
#176557=CARTESIAN_POINT('Ctrl Pts',(-28.4713222982358,88.0506123982403,
72.8005799439378));
#176558=CARTESIAN_POINT('Ctrl Pts',(-28.4656642202474,88.0520553470386,
73.0481475982963));
#176559=CARTESIAN_POINT('Ctrl Pts',(-28.4551716412926,88.0412888590141,
73.5141885267032));
#176560=CARTESIAN_POINT('Ctrl Pts',(-28.4503395549486,88.030653834725,73.7321861328932));
#176561=CARTESIAN_POINT('Ctrl Pts',(-28.4334128661627,87.9730180649228,
74.5067584769098));
#176562=CARTESIAN_POINT('Ctrl Pts',(-28.4217087262867,87.8953464065803,
75.060685681791));
#176563=CARTESIAN_POINT('Ctrl Pts',(-28.4001843683505,87.6892138892675,
76.0622437309167));
#176564=CARTESIAN_POINT('Ctrl Pts',(-28.3903751682219,87.5714840520253,
76.5121166723893));
#176565=CARTESIAN_POINT('Ctrl Pts',(-28.3753343901809,87.3620113754935,
77.1690380808749));
#176566=CARTESIAN_POINT('Ctrl Pts',(-28.3703382894102,87.2881121570046,
77.3818215717414));
#176567=CARTESIAN_POINT('Ctrl Pts',(-28.3539567018314,87.032071207605,78.0622424495177));
#176568=CARTESIAN_POINT('Ctrl Pts',(-28.3423086815491,86.8284778504005,
78.5218363055945));
#176569=CARTESIAN_POINT('Ctrl Pts',(-28.3257320467384,86.4970967377994,
79.1662564668239));
#176570=CARTESIAN_POINT('Ctrl Pts',(-28.3206683464067,86.3900996146686,
79.3617753846728));
#176571=CARTESIAN_POINT('Ctrl Pts',(-28.3110781464308,86.1746926264359,
79.7321581480111));
#176572=CARTESIAN_POINT('Ctrl Pts',(-28.3065585731675,86.0672566883146,
79.9070521614495));
#176573=CARTESIAN_POINT('Ctrl Pts',(-28.2903497051778,85.6606113672015,
80.5346701629311));
#176574=CARTESIAN_POINT('Ctrl Pts',(-28.2790534865079,85.3369588787352,
80.9710469484754));
#176575=CARTESIAN_POINT('Ctrl Pts',(-28.2617405571487,84.8055873283224,
81.6018369594899));
#176576=CARTESIAN_POINT('Ctrl Pts',(-28.2557863558243,84.6165958335401,
81.812028313147));
#176577=CARTESIAN_POINT('Ctrl Pts',(-28.2449075350388,84.2652088931614,
82.1784473410338));
#176578=CARTESIAN_POINT('Ctrl Pts',(-28.2400168935055,84.1051963462792,
82.3369738074407));
#176579=CARTESIAN_POINT('Ctrl Pts',(-28.2223958786166,83.5256814169202,
82.8824447742505));
#176580=CARTESIAN_POINT('Ctrl Pts',(-28.2092075896598,83.0847143411874,
83.2466708502592));
#176581=CARTESIAN_POINT('Ctrl Pts',(-28.1898112962602,82.3986096141907,
83.7415470218061));
#176582=CARTESIAN_POINT('Ctrl Pts',(-28.1835238643657,82.1702444803154,
83.8955205290103));
#176583=CARTESIAN_POINT('Ctrl Pts',(-28.172426025588,81.7524222984042,84.1581830692444));
#176584=CARTESIAN_POINT('Ctrl Pts',(-28.1675783568522,81.5646239048304,
84.2696982543368));
#176585=CARTESIAN_POINT('Ctrl Pts',(-28.1499587002885,80.8584550908841,
84.6648230738459));
#176586=CARTESIAN_POINT('Ctrl Pts',(-28.1377313665428,80.3231327240567,
84.9174692347079));
#176587=CARTESIAN_POINT('Ctrl Pts',(-28.120177029338,79.5443191346533,85.2226728645883));
#176588=CARTESIAN_POINT('Ctrl Pts',(-28.1149880891762,79.3128811832984,
85.305941847855));
#176589=CARTESIAN_POINT('Ctrl Pts',(-28.105027972566,78.8718287703843,85.450826165863));
#176590=CARTESIAN_POINT('Ctrl Pts',(-28.1002660041616,78.662662659087,85.5138227930762));
#176591=CARTESIAN_POINT('Ctrl Pts',(-28.084358923876,77.970561149516,85.7036742889627));
#176592=CARTESIAN_POINT('Ctrl Pts',(-28.0729223317712,77.4815190943867,
85.8084453208436));
#176593=CARTESIAN_POINT('Ctrl Pts',(-28.0508832707176,76.5299993537951,
85.9561309732578));
#176594=CARTESIAN_POINT('Ctrl Pts',(-28.0402809737513,76.0680803210234,
86.0029343227759));
#176595=CARTESIAN_POINT('Ctrl Pts',(-28.0252281641927,75.3909220703083,
86.0347769539215));
#176596=CARTESIAN_POINT('Ctrl Pts',(-28.0205423784486,75.1767369359267,
86.0394917040199));
#176597=CARTESIAN_POINT('Ctrl Pts',(-28.0070172332282,74.5475319527212,
86.0374732746602));
#176598=CARTESIAN_POINT('Ctrl Pts',(-27.9983748948165,74.133017053517,86.016020173507));
#176599=CARTESIAN_POINT('Ctrl Pts',(-27.9842063416753,73.459831027145,85.9489422438951));
#176600=CARTESIAN_POINT('Ctrl Pts',(-27.9787046285731,73.1999971494259,
85.9151310851981));
#176601=CARTESIAN_POINT('Ctrl Pts',(-27.9680786331366,72.7089387105117,
85.8362548591247));
#176602=CARTESIAN_POINT('Ctrl Pts',(-27.962959731273,72.4774716752162,85.7926708696398));
#176603=CARTESIAN_POINT('Ctrl Pts',(-27.9459079922839,71.7226864299946,
85.6295219740991));
#176604=CARTESIAN_POINT('Ctrl Pts',(-27.933669204793,71.204894921339,85.4840841649155));
#176605=CARTESIAN_POINT('Ctrl Pts',(-27.9131107191997,70.3528257095262,
85.1874098975274));
#176606=CARTESIAN_POINT('Ctrl Pts',(-27.9047868359488,70.0126814631457,
85.0528224317421));
#176607=CARTESIAN_POINT('Ctrl Pts',(-27.8904074149884,69.426970927856,84.7919520033186));
#176608=CARTESIAN_POINT('Ctrl Pts',(-27.8842971544598,69.178704676175,84.6717539983116));
#176609=CARTESIAN_POINT('Ctrl Pts',(-27.8698641651585,68.5902566395028,
84.3630061943237));
#176610=CARTESIAN_POINT('Ctrl Pts',(-27.8617102002911,68.254769317834,84.1669030613641));
#176611=CARTESIAN_POINT('Ctrl Pts',(-27.8453550084675,67.6000791285052,
83.7438474717693));
#176612=CARTESIAN_POINT('Ctrl Pts',(-27.837132829163,67.2807834941334,83.5164356122228));
#176613=CARTESIAN_POINT('Ctrl Pts',(-27.8216158902758,66.7164728185939,
83.0752714533215));
#176614=CARTESIAN_POINT('Ctrl Pts',(-27.8144342768204,66.4680829739782,
82.8658224671431));
#176615=CARTESIAN_POINT('Ctrl Pts',(-27.7925141076388,65.7427195640055,
82.2069105184709));
#176616=CARTESIAN_POINT('Ctrl Pts',(-27.7775244449321,65.2904168095573,
81.7301117030604));
#176617=CARTESIAN_POINT('Ctrl Pts',(-27.7543237430188,64.6387834351827,
80.9306647299601));
#176618=CARTESIAN_POINT('Ctrl Pts',(-27.7459456038654,64.4137660149623,
80.628877251408));
#176619=CARTESIAN_POINT('Ctrl Pts',(-27.7285710578544,63.9655724982218,
79.969189009831));
#176620=CARTESIAN_POINT('Ctrl Pts',(-27.7197240144243,63.7467831046844,
79.6100593961934));
#176621=CARTESIAN_POINT('Ctrl Pts',(-27.7023250909221,63.3523070043413,
78.8856638740414));
#176622=CARTESIAN_POINT('Ctrl Pts',(-27.6936986564019,63.1753358727586,
78.5210595402815));
#176623=CARTESIAN_POINT('Ctrl Pts',(-27.6675797083518,62.7034813042502,
77.4225764407909));
#176624=CARTESIAN_POINT('Ctrl Pts',(-27.649675103024,62.4568896885277,76.6677537942532));
#176625=CARTESIAN_POINT('Ctrl Pts',(-27.622778973032,62.1890845922095,75.5014481464094));
#176626=CARTESIAN_POINT('Ctrl Pts',(-27.6136892790897,62.1165761733617,
75.1015430110143));
#176627=CARTESIAN_POINT('Ctrl Pts',(-27.5967623749457,62.015285521393,74.3407693058522));
#176628=CARTESIAN_POINT('Ctrl Pts',(-27.588911682362,61.9825824542457,73.9804215063247));
#176629=CARTESIAN_POINT('Ctrl Pts',(-27.5726952476484,61.9462255563491,
73.2211702198871));
#176630=CARTESIAN_POINT('Ctrl Pts',(-27.5643023785364,61.9456694868364,
72.8232192864476));
#176631=CARTESIAN_POINT('Ctrl Pts',(-27.5329917923185,62.0097849875933,
71.3750406569346));
#176632=CARTESIAN_POINT('Ctrl Pts',(-27.5093033935215,62.1833553964862,
70.3293263596869));
#176633=CARTESIAN_POINT('Ctrl Pts',(-27.4749412181969,62.6153512025303,
68.8498644114641));
#176634=CARTESIAN_POINT('Ctrl Pts',(-27.4640850915678,62.7787328643152,
68.3879182399081));
#176635=CARTESIAN_POINT('Ctrl Pts',(-27.4356932887815,63.2809772079994,
67.1895048707421));
#176636=CARTESIAN_POINT('Ctrl Pts',(-27.4185930823565,63.6633232223783,
66.4766538853576));
#176637=CARTESIAN_POINT('Ctrl Pts',(-27.3825509135325,64.5707608461097,
65.1036229345754));
#176638=CARTESIAN_POINT('Ctrl Pts',(-27.363866715291,65.102041958874,64.4464312496956));
#176639=CARTESIAN_POINT('Ctrl Pts',(-27.3275858984294,66.2484712427984,
63.2771098842673));
#176640=CARTESIAN_POINT('Ctrl Pts',(-27.3099850543916,66.8589056351111,
62.7579304603558));
#176641=CARTESIAN_POINT('Ctrl Pts',(-27.2561001277643,68.8874815752587,
61.3386319068995));
#176642=CARTESIAN_POINT('Ctrl Pts',(-27.2193312238702,70.4484153494107,
60.6471229272152));
#176643=CARTESIAN_POINT('Ctrl Pts',(-27.163845282467,72.8976775687344,60.0821227070811));
#176644=CARTESIAN_POINT('Ctrl Pts',(-27.1454072056421,73.7258624050007,
59.9740771483805));
#176645=CARTESIAN_POINT('Ctrl Pts',(-27.0942944771862,76.0636964224413,
59.8985369954317));
#176646=CARTESIAN_POINT('Ctrl Pts',(-27.0619671031244,77.5720983174881,
60.1092423462382));
#176647=CARTESIAN_POINT('Ctrl Pts',(-27.020462786728,79.3446424713931,60.678195355492));
#176648=CARTESIAN_POINT('Ctrl Pts',(-27.0122985285325,79.6845914787547,
60.8032117456719));
#176649=CARTESIAN_POINT('Ctrl Pts',(-26.9871305006992,80.7306118381862,
61.239437844667));
#176650=CARTESIAN_POINT('Ctrl Pts',(-26.9704806532513,81.4149891932611,
61.6001714360441));
#176651=CARTESIAN_POINT('Ctrl Pts',(-26.9358799470581,82.7624597916229,
62.4688447909563));
#176652=CARTESIAN_POINT('Ctrl Pts',(-26.9179148479559,83.419644908176,62.9864356224054));
#176653=CARTESIAN_POINT('Ctrl Pts',(-26.8896489617799,84.3392982919,63.8646050038314));
#176654=CARTESIAN_POINT('Ctrl Pts',(-26.8796608922059,84.6415223812075,
64.1837672662168));
#176655=CARTESIAN_POINT('Ctrl Pts',(-26.8613952628632,85.1671283270705,
64.7991669455865));
#176656=CARTESIAN_POINT('Ctrl Pts',(-26.8532042088827,85.3946645605935,
65.0903585287338));
#176657=CARTESIAN_POINT('Ctrl Pts',(-26.8358997393618,85.8552599102491,
65.734769397251));
#176658=CARTESIAN_POINT('Ctrl Pts',(-26.8268048243646,86.0843151965931,
66.090858545665));
#176659=CARTESIAN_POINT('Ctrl Pts',(-26.8007583416444,86.6917107047555,
67.1434425426908));
#176660=CARTESIAN_POINT('Ctrl Pts',(-26.783872294885,87.0257464058268,67.8657205014914));
#176661=CARTESIAN_POINT('Ctrl Pts',(-26.7574958584136,87.4270111134863,
68.9894125338539));
#176662=CARTESIAN_POINT('Ctrl Pts',(-26.7484197851956,87.5445328786064,
69.3730634014937));
#176663=CARTESIAN_POINT('Ctrl Pts',(-26.7296221147459,87.7491128006321,
70.1712710306875));
#176664=CARTESIAN_POINT('Ctrl Pts',(-26.7199881481467,87.8340296633232,
70.5860658319642));
#176665=CARTESIAN_POINT('Ctrl Pts',(-26.7009018641838,87.9650356085774,
71.4411355472774));
#176666=CARTESIAN_POINT('Ctrl Pts',(-26.6914264830145,88.0093605486581,
71.8799832571119));
#176667=CARTESIAN_POINT('Ctrl Pts',(-26.6644730962213,88.0727815060036,
73.1416759569455));
#176668=CARTESIAN_POINT('Ctrl Pts',(-26.6471711075735,88.0366256560804,
73.9674584092148));
#176669=CARTESIAN_POINT('Ctrl Pts',(-26.6221879431741,87.8817029207814,
75.0896077926789));
#176670=CARTESIAN_POINT('Ctrl Pts',(-26.6152061766537,87.8284521936595,
75.3952408936558));
#176671=CARTESIAN_POINT('Ctrl Pts',(-26.5981209286503,87.6737666541221,
76.1278569934313));
#176672=CARTESIAN_POINT('Ctrl Pts',(-26.5879730360397,87.5615069598982,
76.5525448167818));
#176673=CARTESIAN_POINT('Ctrl Pts',(-26.5727315783776,87.3551027342262,
77.1974324033812));
#176674=CARTESIAN_POINT('Ctrl Pts',(-26.5674697523318,87.2762257092991,
77.4219902446079));
#176675=CARTESIAN_POINT('Ctrl Pts',(-26.551714967308,87.0178572943662,78.0971664379141));
#176676=CARTESIAN_POINT('Ctrl Pts',(-26.5414479421155,86.8189623764084,
78.5403282845433));
#176677=CARTESIAN_POINT('Ctrl Pts',(-26.5193723997868,86.3391411211965,
79.4682464492547));
#176678=CARTESIAN_POINT('Ctrl Pts',(-26.5075648013405,86.0502750435632,
79.948961822146));
#176679=CARTESIAN_POINT('Ctrl Pts',(-26.4901011932104,85.5956111489685,
80.6069925442744));
#176680=CARTESIAN_POINT('Ctrl Pts',(-26.4847749661921,85.4536682915792,
80.8008845086256));
#176681=CARTESIAN_POINT('Ctrl Pts',(-26.4733338461345,85.1429547905315,
81.2017922635603));
#176682=CARTESIAN_POINT('Ctrl Pts',(-26.4672136573702,84.9729538104197,
81.4078623196491));
#176683=CARTESIAN_POINT('Ctrl Pts',(-26.4503871463832,84.4896779366806,
81.9583567950162));
#176684=CARTESIAN_POINT('Ctrl Pts',(-26.4396561649543,84.1638512724422,
82.2917404998743));
#176685=CARTESIAN_POINT('Ctrl Pts',(-26.4240726942374,83.6463503031868,
82.7663707883053));
#176686=CARTESIAN_POINT('Ctrl Pts',(-26.4189237189563,83.4674861103605,
82.9214875466556));
#176687=CARTESIAN_POINT('Ctrl Pts',(-26.4073473207837,83.0507913278121,
83.2632709622442));
#176688=CARTESIAN_POINT('Ctrl Pts',(-26.4009613103596,82.8103684385238,
83.4467584999488));
#176689=CARTESIAN_POINT('Ctrl Pts',(-26.3827457350335,82.1046571584463,
83.9476350985173));
#176690=CARTESIAN_POINT('Ctrl Pts',(-26.3709709794553,81.6243515321666,
84.243935498527));
#176691=CARTESIAN_POINT('Ctrl Pts',(-26.3539767729892,80.9332015918654,
84.6115655225933));
#176692=CARTESIAN_POINT('Ctrl Pts',(-26.3491329449994,80.7366421684322,
84.7099033048351));
#176693=CARTESIAN_POINT('Ctrl Pts',(-26.338946675524,80.3253459523221,84.9029724294442));
#176694=CARTESIAN_POINT('Ctrl Pts',(-26.3336041944195,80.110275842259,84.9970073624504));
#176695=CARTESIAN_POINT('Ctrl Pts',(-26.3142319607583,79.3264514548815,
85.3149591532496));
#176696=CARTESIAN_POINT('Ctrl Pts',(-26.3000246950262,78.744007635783,85.5051243373986));
#176697=CARTESIAN_POINT('Ctrl Pts',(-26.2816122076784,77.9367555483608,
85.7060944034288));
#176698=CARTESIAN_POINT('Ctrl Pts',(-26.2768286949653,77.7214757596124,
85.7537910392488));
#176699=CARTESIAN_POINT('Ctrl Pts',(-26.2660720302795,77.2285041652266,
85.8498414943771));
#176700=CARTESIAN_POINT('Ctrl Pts',(-26.2601348364542,76.9500237034786,
85.8946831368301));
#176701=CARTESIAN_POINT('Ctrl Pts',(-26.2429700601151,76.138463532457,85.9985253292113));
#176702=CARTESIAN_POINT('Ctrl Pts',(-26.2317986248592,75.6023259005181,
86.0338074442609));
#176703=CARTESIAN_POINT('Ctrl Pts',(-26.2155065051407,74.8506832506398,
86.0374429040957));
#176704=CARTESIAN_POINT('Ctrl Pts',(-26.2107555598615,74.6352579008578,
86.0332104581162));
#176705=CARTESIAN_POINT('Ctrl Pts',(-26.2003641428551,74.1714666081721,
86.012729816208));
#176706=CARTESIAN_POINT('Ctrl Pts',(-26.1947078232235,73.9231713470529,
85.9947174873763));
#176707=CARTESIAN_POINT('Ctrl Pts',(-26.1741183630528,73.0272419081808,
85.9040947848472));
#176708=CARTESIAN_POINT('Ctrl Pts',(-26.1589940667163,72.3837514385232,
85.7902964704825));
#176709=CARTESIAN_POINT('Ctrl Pts',(-26.1398650436156,71.5455017237514,
85.5752119984921));
#176710=CARTESIAN_POINT('Ctrl Pts',(-26.1352370951203,71.3402287048517,
85.5170114831311));
#176711=CARTESIAN_POINT('Ctrl Pts',(-26.1249826355312,70.8823191795475,
85.3747761601401));
#176712=CARTESIAN_POINT('Ctrl Pts',(-26.1193885736418,70.6306924143436,
85.2879748852595));
#176713=CARTESIAN_POINT('Ctrl Pts',(-26.1032504285204,69.9103993676397,
85.0145340562684));
#176714=CARTESIAN_POINT('Ctrl Pts',(-26.0927587683217,69.4492339301159,
84.8081158674202));
#176715=CARTESIAN_POINT('Ctrl Pts',(-26.0768767947257,68.7979686602581,
84.4705736902692));
#176716=CARTESIAN_POINT('Ctrl Pts',(-26.0718192632528,68.5972638812067,
84.3598225197354));
#176717=CARTESIAN_POINT('Ctrl Pts',(-26.0604385782711,68.1581486434782,
84.10237796679));
#176718=CARTESIAN_POINT('Ctrl Pts',(-26.0540845086778,67.921209111272,83.9531453635371));
#176719=CARTESIAN_POINT('Ctrl Pts',(-26.0326176020567,67.1415381307353,
83.4266271577465));
#176720=CARTESIAN_POINT('Ctrl Pts',(-26.0173623862014,66.6216448893775,
83.015447269992));
#176721=CARTESIAN_POINT('Ctrl Pts',(-25.9978851098422,65.973547218442,82.4162631829118));
#176722=CARTESIAN_POINT('Ctrl Pts',(-25.9930886383386,65.8150472624552,
82.2619092271083));
#176723=CARTESIAN_POINT('Ctrl Pts',(-25.9825821331696,65.4714486242781,
81.9094715854228));
#176724=CARTESIAN_POINT('Ctrl Pts',(-25.9769067577913,65.2887395400715,
81.7098203747785));
#176725=CARTESIAN_POINT('Ctrl Pts',(-25.9616090100639,64.8125894617919,
81.15577405542));
#176726=CARTESIAN_POINT('Ctrl Pts',(-25.9520003131318,64.5312628947353,
80.7909775931263));
#176727=CARTESIAN_POINT('Ctrl Pts',(-25.9358139057098,64.1077298156168,
80.1779590637891));
#176728=CARTESIAN_POINT('Ctrl Pts',(-25.9294925541469,63.9532998099031,
79.938159223049));
#176729=CARTESIAN_POINT('Ctrl Pts',(-25.9143714584637,63.6068872801481,
79.3599371596408));
#176730=CARTESIAN_POINT('Ctrl Pts',(-25.9055075558728,63.4217170354802,
79.0173944753116));
#176731=CARTESIAN_POINT('Ctrl Pts',(-25.8852161328144,63.0330730830113,
78.2152563338669));
#176732=CARTESIAN_POINT('Ctrl Pts',(-25.8737953749455,62.8399720566537,
77.7505994263655));
#176733=CARTESIAN_POINT('Ctrl Pts',(-25.8573466709818,62.594885478589,77.0476217222832));
#176734=CARTESIAN_POINT('Ctrl Pts',(-25.8520771467528,62.5216288080039,
76.8167769541858));
#176735=CARTESIAN_POINT('Ctrl Pts',(-25.8392202706116,62.356130905073,76.238552697275));
#176736=CARTESIAN_POINT('Ctrl Pts',(-25.8317252506728,62.2718865056701,
75.8894256090391));
#176737=CARTESIAN_POINT('Ctrl Pts',(-25.8169810487476,62.1356880662047,
75.2015691474896));
#176738=CARTESIAN_POINT('Ctrl Pts',(-25.8097163405197,62.0824302136498,
74.8631149413459));
#176739=CARTESIAN_POINT('Ctrl Pts',(-25.7937780429484,61.9969305702283,
74.1360762109128));
#176740=CARTESIAN_POINT('Ctrl Pts',(-25.7850983229709,61.9686106220109,
73.7470119385911));
#176741=CARTESIAN_POINT('Ctrl Pts',(-25.7614694609691,61.9387668588439,
72.6965261009687));
#176742=CARTESIAN_POINT('Ctrl Pts',(-25.746365168282,61.9696615368098,72.0340609509725));
#176743=CARTESIAN_POINT('Ctrl Pts',(-25.7241830758666,62.0912090174244,
71.0485307984549));
#176744=CARTESIAN_POINT('Ctrl Pts',(-25.7168555428034,62.1444179674266,
70.7208169164824));
#176745=CARTESIAN_POINT('Ctrl Pts',(-25.704296129729,62.2596456587527,70.1518497829427));
#176746=CARTESIAN_POINT('Ctrl Pts',(-25.6990213326695,62.3160591499028,
69.9099172028483));
#176747=CARTESIAN_POINT('Ctrl Pts',(-25.6886754232146,62.4409224071355,
69.4365971656001));
#176748=CARTESIAN_POINT('Ctrl Pts',(-25.6835980324187,62.509009553304,69.2050318081367));
#176749=CARTESIAN_POINT('Ctrl Pts',(-25.6710176818858,62.6915976545898,
68.6422538530757));
#176750=CARTESIAN_POINT('Ctrl Pts',(-25.6634230092666,62.813162807868,68.3133358375227));
#176751=CARTESIAN_POINT('Ctrl Pts',(-25.6469308771572,63.1010327267764,
67.6207602958996));
#176752=CARTESIAN_POINT('Ctrl Pts',(-25.6380085508726,63.2712409369225,
67.2586855968152));
#176753=CARTESIAN_POINT('Ctrl Pts',(-25.6094806088747,63.8639870406997,
66.1334341852122));
#176754=CARTESIAN_POINT('Ctrl Pts',(-25.5897204907838,64.34705706191,65.4019308983917));
#176755=CARTESIAN_POINT('Ctrl Pts',(-25.5633040231181,65.114039605429,64.4631759975833));
#176756=CARTESIAN_POINT('Ctrl Pts',(-25.5560721227099,65.3388955919402,
64.2093238118185));
#176757=CARTESIAN_POINT('Ctrl Pts',(-25.5376324116602,65.938520962717,63.5839944296733));
#176758=CARTESIAN_POINT('Ctrl Pts',(-25.5262670521131,66.3264140418631,
63.226077368409));
#176759=CARTESIAN_POINT('Ctrl Pts',(-25.5015769521811,67.196543220476,62.5149302089825));
#176760=CARTESIAN_POINT('Ctrl Pts',(-25.4882596254439,67.6845399522126,
62.1686021886949));
#176761=CARTESIAN_POINT('Ctrl Pts',(-25.4563912935859,68.9029738909808,
61.4226452836094));
#176762=CARTESIAN_POINT('Ctrl Pts',(-25.4378456278295,69.653482210693,61.0554991545458));
#176763=CARTESIAN_POINT('Ctrl Pts',(-25.4108569344788,70.8205996163349,
60.6192454789367));
#176764=CARTESIAN_POINT('Ctrl Pts',(-25.402011059299,71.2151668380905,60.4933124186287));
#176765=CARTESIAN_POINT('Ctrl Pts',(-25.3752278174413,72.4071241617779,
60.1745015968442));
#176766=CARTESIAN_POINT('Ctrl Pts',(-25.3571272368688,73.2199161670816,
60.037475388827));
#176767=CARTESIAN_POINT('Ctrl Pts',(-25.3188691789373,74.9443395382244,
59.9095450364837));
#176768=CARTESIAN_POINT('Ctrl Pts',(-25.2986976872818,75.8576415839786,
59.9358960975145));
#176769=CARTESIAN_POINT('Ctrl Pts',(-25.2583479843491,77.6829440804511,
60.1832535935612));
#176770=CARTESIAN_POINT('Ctrl Pts',(-25.2381057548755,78.5905580872887,
60.409751827594));
#176771=CARTESIAN_POINT('Ctrl Pts',(-25.2177843835793,79.4626792952277,
60.7277886365121));
#176772=CARTESIAN_POINT('',(-25.21690938235,79.4632381180988,60.7262027183532));
#176773=CARTESIAN_POINT('Ctrl Pts',(-29.4261514861327,72.242088232536,85.74414017529));
#176774=CARTESIAN_POINT('Ctrl Pts',(-29.3779431821827,70.095650878086,85.28004229623));
#176775=CARTESIAN_POINT('Ctrl Pts',(-29.2815265742827,66.04485241176,83.24564128978));
#176776=CARTESIAN_POINT('Ctrl Pts',(-29.1369016624246,62.20076662219,77.634595795182));
#176777=CARTESIAN_POINT('Ctrl Pts',(-28.9922767505727,61.55056525346,70.864604569967));
#176778=CARTESIAN_POINT('Ctrl Pts',(-28.8476518387227,64.25574478693,64.624573520997));
#176779=CARTESIAN_POINT('Ctrl Pts',(-28.7030269268629,69.641577033905,60.47138590026));
#176780=CARTESIAN_POINT('Ctrl Pts',(-28.5584020150127,76.364284952381,59.44121987509));
#176781=CARTESIAN_POINT('Ctrl Pts',(-28.4137771031546,82.746616870673,61.79109721394));
#176782=CARTESIAN_POINT('Ctrl Pts',(-28.2691521913028,87.19622473785,66.934740200613));
#176783=CARTESIAN_POINT('Ctrl Pts',(-28.1245272794527,88.60296550284,73.5888484027236));
#176784=CARTESIAN_POINT('Ctrl Pts',(-27.9799023675929,86.61586754518,80.093271282679));
#176785=CARTESIAN_POINT('Ctrl Pts',(-27.8352774557427,81.730697090025,84.82520375033));
#176786=CARTESIAN_POINT('Ctrl Pts',(-27.6906525438927,75.1662677935533,
86.60406386368));
#176787=CARTESIAN_POINT('Ctrl Pts',(-27.5460276320329,68.560355920967,84.98603926299));
#176788=CARTESIAN_POINT('Ctrl Pts',(-27.4014027201827,63.56108732498,80.374815045269));
#176789=CARTESIAN_POINT('Ctrl Pts',(-27.2567778083246,61.41574231844,73.9208573383313));
#176790=CARTESIAN_POINT('Ctrl Pts',(-27.1121528964728,62.65956851573,67.234380562697));
#176791=CARTESIAN_POINT('Ctrl Pts',(-26.9675279846227,66.982240536617,61.98361091626));
#176792=CARTESIAN_POINT('Ctrl Pts',(-26.8229030727646,73.305283879178,59.47857635201));
#176793=CARTESIAN_POINT('Ctrl Pts',(-26.6782781609127,80.05114628266,60.34426435248));
#176794=CARTESIAN_POINT('Ctrl Pts',(-26.5336532490595,85.53678527666,64.36469220339));
#176795=CARTESIAN_POINT('Ctrl Pts',(-26.3890283372062,88.39357475485,70.536793074933));
#176796=CARTESIAN_POINT('Ctrl Pts',(-26.2444034253522,87.90876699715,77.320673726326));
#176797=CARTESIAN_POINT('Ctrl Pts',(-26.0997785134991,84.203317946944,83.02380642958));
#176798=CARTESIAN_POINT('Ctrl Pts',(-25.9551536016452,78.201709510007,86.22330197028));
#176799=CARTESIAN_POINT('Ctrl Pts',(-25.8105286897922,71.40129854677,86.12091018816));
#176800=CARTESIAN_POINT('Ctrl Pts',(-25.665903777939,65.49873617875,82.742176443924));
#176801=CARTESIAN_POINT('Ctrl Pts',(-25.5212788660852,61.96667080937,76.930072003796));
#176802=CARTESIAN_POINT('Ctrl Pts',(-25.3766539542322,61.68631520576,70.134664941592));
#176803=CARTESIAN_POINT('Ctrl Pts',(-25.2320290423791,64.72765802224,64.051391343194));
#176804=CARTESIAN_POINT('Ctrl Pts',(-25.0874041305261,70.331750046873,60.1978610671));
#176805=CARTESIAN_POINT('Ctrl Pts',(-24.942779218673,77.100997250995,59.53595519057));
#176806=CARTESIAN_POINT('Ctrl Pts',(-24.846362610771,81.263224902643,61.33139849116));
#176807=CARTESIAN_POINT('Ctrl Pts',(-24.79815430682,82.998435097713,62.6773649606));
#176808=CARTESIAN_POINT('Ctrl Pts',(-29.5486931499337,72.242088232536,85.74414017529));
#176809=CARTESIAN_POINT('Ctrl Pts',(-29.5004848459837,70.095650878086,85.28004229623));
#176810=CARTESIAN_POINT('Ctrl Pts',(-29.4040682380836,66.04485241176,83.24564128978));
#176811=CARTESIAN_POINT('Ctrl Pts',(-29.2594433262332,62.20076662219,77.634595795182));
#176812=CARTESIAN_POINT('Ctrl Pts',(-29.1148184143737,61.55056525346,70.864604569967));
#176813=CARTESIAN_POINT('Ctrl Pts',(-28.9701935025236,64.25574478693,64.624573520997));
#176814=CARTESIAN_POINT('Ctrl Pts',(-28.8255685906649,69.641577033905,60.47138590026));
#176815=CARTESIAN_POINT('Ctrl Pts',(-28.6809436788136,76.364284952381,59.44121987509));
#176816=CARTESIAN_POINT('Ctrl Pts',(-28.5363187669632,82.746616870673,61.79109721394));
#176817=CARTESIAN_POINT('Ctrl Pts',(-28.3916938551037,87.19622473785,66.934740200613));
#176818=CARTESIAN_POINT('Ctrl Pts',(-28.2470689432536,88.60296550284,73.5888484027236));
#176819=CARTESIAN_POINT('Ctrl Pts',(-28.1024440313949,86.61586754518,80.093271282679));
#176820=CARTESIAN_POINT('Ctrl Pts',(-27.9578191195436,81.730697090025,84.82520375033));
#176821=CARTESIAN_POINT('Ctrl Pts',(-27.8131942076936,75.1662677935533,
86.60406386368));
#176822=CARTESIAN_POINT('Ctrl Pts',(-27.6685692958349,68.560355920967,84.98603926299));
#176823=CARTESIAN_POINT('Ctrl Pts',(-27.5239443839836,63.56108732498,80.374815045269));
#176824=CARTESIAN_POINT('Ctrl Pts',(-27.3793194721332,61.41574231844,73.9208573383313));
#176825=CARTESIAN_POINT('Ctrl Pts',(-27.2346945602737,62.65956851573,67.234380562697));
#176826=CARTESIAN_POINT('Ctrl Pts',(-27.0900696484237,66.982240536617,61.98361091626));
#176827=CARTESIAN_POINT('Ctrl Pts',(-26.9454447365732,73.305283879178,59.47857635201));
#176828=CARTESIAN_POINT('Ctrl Pts',(-26.8008198247137,80.05114628266,60.34426435248));
#176829=CARTESIAN_POINT('Ctrl Pts',(-26.6561949128635,85.53678527666,64.36469220339));
#176830=CARTESIAN_POINT('Ctrl Pts',(-26.5115700010092,88.39357475485,70.536793074933));
#176831=CARTESIAN_POINT('Ctrl Pts',(-26.3669450891548,87.90876699715,77.320673726326));
#176832=CARTESIAN_POINT('Ctrl Pts',(-26.2223201773017,84.203317946944,83.02380642958));
#176833=CARTESIAN_POINT('Ctrl Pts',(-26.0776952654478,78.201709510007,86.22330197028));
#176834=CARTESIAN_POINT('Ctrl Pts',(-25.9330703535948,71.40129854677,86.12091018816));
#176835=CARTESIAN_POINT('Ctrl Pts',(-25.7884454417409,65.49873617875,82.742176443924));
#176836=CARTESIAN_POINT('Ctrl Pts',(-25.6438205298878,61.96667080937,76.930072003796));
#176837=CARTESIAN_POINT('Ctrl Pts',(-25.4991956180348,61.68631520576,70.134664941592));
#176838=CARTESIAN_POINT('Ctrl Pts',(-25.3545707061817,64.72765802224,64.051391343194));
#176839=CARTESIAN_POINT('Ctrl Pts',(-25.2099457943287,70.331750046873,60.1978610671));
#176840=CARTESIAN_POINT('Ctrl Pts',(-25.0653208824749,77.100997250995,59.53595519057));
#176841=CARTESIAN_POINT('Ctrl Pts',(-24.9689042745729,81.263224902643,61.33139849116));
#176842=CARTESIAN_POINT('Ctrl Pts',(-24.9206959706219,82.998435097713,62.6773649606));
#176843=CARTESIAN_POINT('Ctrl Pts',(-29.6712348137352,72.242088232536,85.74414017529));
#176844=CARTESIAN_POINT('Ctrl Pts',(-29.6230265097852,70.095650878086,85.28004229623));
#176845=CARTESIAN_POINT('Ctrl Pts',(-29.5266099018845,66.04485241176,83.24564128978));
#176846=CARTESIAN_POINT('Ctrl Pts',(-29.3819849900345,62.20076662219,77.634595795182));
#176847=CARTESIAN_POINT('Ctrl Pts',(-29.2373600781752,61.55056525346,70.864604569967));
#176848=CARTESIAN_POINT('Ctrl Pts',(-29.0927351663245,64.25574478693,64.624573520997));
#176849=CARTESIAN_POINT('Ctrl Pts',(-28.9481102544736,69.641577033905,60.47138590026));
#176850=CARTESIAN_POINT('Ctrl Pts',(-28.8034853426145,76.364284952381,59.44121987509));
#176851=CARTESIAN_POINT('Ctrl Pts',(-28.6588604307645,82.746616870673,61.79109721394));
#176852=CARTESIAN_POINT('Ctrl Pts',(-28.5142355189052,87.19622473785,66.934740200613));
#176853=CARTESIAN_POINT('Ctrl Pts',(-28.3696106070545,88.60296550284,73.5888484027236));
#176854=CARTESIAN_POINT('Ctrl Pts',(-28.2249856952036,86.61586754518,80.093271282679));
#176855=CARTESIAN_POINT('Ctrl Pts',(-28.0803607833445,81.730697090025,84.82520375033));
#176856=CARTESIAN_POINT('Ctrl Pts',(-27.9357358714945,75.1662677935533,
86.60406386368));
#176857=CARTESIAN_POINT('Ctrl Pts',(-27.7911109596436,68.560355920967,84.98603926299));
#176858=CARTESIAN_POINT('Ctrl Pts',(-27.6464860477845,63.56108732498,80.374815045269));
#176859=CARTESIAN_POINT('Ctrl Pts',(-27.5018611359345,61.41574231844,73.9208573383313));
#176860=CARTESIAN_POINT('Ctrl Pts',(-27.3572362240752,62.65956851573,67.234380562697));
#176861=CARTESIAN_POINT('Ctrl Pts',(-27.2126113122245,66.982240536617,61.98361091626));
#176862=CARTESIAN_POINT('Ctrl Pts',(-27.0679864003745,73.305283879178,59.47857635201));
#176863=CARTESIAN_POINT('Ctrl Pts',(-26.9233614885152,80.05114628266,60.34426435248));
#176864=CARTESIAN_POINT('Ctrl Pts',(-26.7787365766645,85.53678527666,64.36469220339));
#176865=CARTESIAN_POINT('Ctrl Pts',(-26.6341116648141,88.39357475485,70.536793074933));
#176866=CARTESIAN_POINT('Ctrl Pts',(-26.4894867529572,87.90876699715,77.320673726326));
#176867=CARTESIAN_POINT('Ctrl Pts',(-26.3448618411036,84.203317946944,83.02380642958));
#176868=CARTESIAN_POINT('Ctrl Pts',(-26.2002369292505,78.201709510007,86.22330197028));
#176869=CARTESIAN_POINT('Ctrl Pts',(-26.0556120173974,71.40129854677,86.12091018816));
#176870=CARTESIAN_POINT('Ctrl Pts',(-25.9109871055435,65.49873617875,82.742176443924));
#176871=CARTESIAN_POINT('Ctrl Pts',(-25.7663621936905,61.96667080937,76.930072003796));
#176872=CARTESIAN_POINT('Ctrl Pts',(-25.6217372818374,61.68631520576,70.134664941592));
#176873=CARTESIAN_POINT('Ctrl Pts',(-25.4771123699836,64.72765802224,64.051391343194));
#176874=CARTESIAN_POINT('Ctrl Pts',(-25.3324874581306,70.331750046873,60.1978610671));
#176875=CARTESIAN_POINT('Ctrl Pts',(-25.1878625462775,77.100997250995,59.53595519057));
#176876=CARTESIAN_POINT('Ctrl Pts',(-25.0914459383755,81.263224902643,61.33139849116));
#176877=CARTESIAN_POINT('Ctrl Pts',(-25.0432376344245,82.998435097713,62.6773649606));
#176878=CARTESIAN_POINT('Ctrl Pts',(-29.793776477544,72.242088232536,85.74414017529));
#176879=CARTESIAN_POINT('Ctrl Pts',(-29.745568173594,70.095650878086,85.28004229623));
#176880=CARTESIAN_POINT('Ctrl Pts',(-29.6491515656854,66.04485241176,83.24564128978));
#176881=CARTESIAN_POINT('Ctrl Pts',(-29.5045266538354,62.20076662219,77.634595795182));
#176882=CARTESIAN_POINT('Ctrl Pts',(-29.359901741984,61.55056525346,70.864604569967));
#176883=CARTESIAN_POINT('Ctrl Pts',(-29.2152768301254,64.25574478693,64.624573520997));
#176884=CARTESIAN_POINT('Ctrl Pts',(-29.0706519182754,69.641577033905,60.47138590026));
#176885=CARTESIAN_POINT('Ctrl Pts',(-28.9260270064154,76.364284952381,59.44121987509));
#176886=CARTESIAN_POINT('Ctrl Pts',(-28.7814020945654,82.746616870673,61.79109721394));
#176887=CARTESIAN_POINT('Ctrl Pts',(-28.636777182714,87.19622473785,66.934740200613));
#176888=CARTESIAN_POINT('Ctrl Pts',(-28.4921522708554,88.60296550284,73.5888484027236));
#176889=CARTESIAN_POINT('Ctrl Pts',(-28.3475273590054,86.61586754518,80.093271282679));
#176890=CARTESIAN_POINT('Ctrl Pts',(-28.2029024471454,81.730697090025,84.82520375033));
#176891=CARTESIAN_POINT('Ctrl Pts',(-28.0582775352954,75.1662677935533,
86.60406386368));
#176892=CARTESIAN_POINT('Ctrl Pts',(-27.9136526234454,68.560355920967,84.98603926299));
#176893=CARTESIAN_POINT('Ctrl Pts',(-27.7690277115854,63.56108732498,80.374815045269));
#176894=CARTESIAN_POINT('Ctrl Pts',(-27.6244027997354,61.41574231844,73.9208573383313));
#176895=CARTESIAN_POINT('Ctrl Pts',(-27.479777887884,62.65956851573,67.234380562697));
#176896=CARTESIAN_POINT('Ctrl Pts',(-27.3351529760254,66.982240536617,61.98361091626));
#176897=CARTESIAN_POINT('Ctrl Pts',(-27.1905280641754,73.305283879178,59.47857635201));
#176898=CARTESIAN_POINT('Ctrl Pts',(-27.045903152324,80.05114628266,60.34426435248));
#176899=CARTESIAN_POINT('Ctrl Pts',(-26.9012782404654,85.53678527666,64.36469220339));
#176900=CARTESIAN_POINT('Ctrl Pts',(-26.7566533286154,88.39357475485,70.536793074933));
#176901=CARTESIAN_POINT('Ctrl Pts',(-26.6120284167559,87.90876699715,77.320673726326));
#176902=CARTESIAN_POINT('Ctrl Pts',(-26.4674035049062,84.203317946944,83.02380642958));
#176903=CARTESIAN_POINT('Ctrl Pts',(-26.3227785930532,78.201709510007,86.22330197028));
#176904=CARTESIAN_POINT('Ctrl Pts',(-26.1781536811993,71.40129854677,86.12091018816));
#176905=CARTESIAN_POINT('Ctrl Pts',(-26.0335287693461,65.49873617875,82.742176443924));
#176906=CARTESIAN_POINT('Ctrl Pts',(-25.8889038574932,61.96667080937,76.930072003796));
#176907=CARTESIAN_POINT('Ctrl Pts',(-25.7442789456393,61.68631520576,70.134664941592));
#176908=CARTESIAN_POINT('Ctrl Pts',(-25.5996540337862,64.72765802224,64.051391343194));
#176909=CARTESIAN_POINT('Ctrl Pts',(-25.4550291219332,70.331750046873,60.1978610671));
#176910=CARTESIAN_POINT('Ctrl Pts',(-25.3104042100802,77.100997250995,59.53595519057));
#176911=CARTESIAN_POINT('Ctrl Pts',(-25.2139876021782,81.263224902643,61.33139849116));
#176912=CARTESIAN_POINT('Ctrl Pts',(-25.1657792982272,82.998435097713,62.6773649606));
#176913=CARTESIAN_POINT('Ctrl Pts',(-29.3655838523953,68.3986373253016,
84.2438270474911));
#176914=CARTESIAN_POINT('Ctrl Pts',(-29.3303036656744,67.0118618461396,
83.4317063126597));
#176915=CARTESIAN_POINT('Ctrl Pts',(-29.295627364516,65.7984777383591,82.3803230252724));
#176916=CARTESIAN_POINT('Ctrl Pts',(-29.2347381075076,64.0710938904411,
80.2099621171983));
#176917=CARTESIAN_POINT('Ctrl Pts',(-29.1967714573929,63.0876642002268,
78.7374991847509));
#176918=CARTESIAN_POINT('Ctrl Pts',(-29.1127653603425,62.0094805862012,
75.0668637575475));
#176919=CARTESIAN_POINT('Ctrl Pts',(-29.075894631943,61.849552996255,73.362907125417));
#176920=CARTESIAN_POINT('Ctrl Pts',(-28.9922442448893,62.2248483961828,
69.5720079624171));
#176921=CARTESIAN_POINT('Ctrl Pts',(-28.9538064145163,62.9148739729229,
67.918150971998));
#176922=CARTESIAN_POINT('Ctrl Pts',(-28.8854503569787,64.3835342434137,
65.1722907800826));
#176923=CARTESIAN_POINT('Ctrl Pts',(-28.8482263560423,65.5292543314931,
63.8773740095138));
#176924=CARTESIAN_POINT('Ctrl Pts',(-28.7869286879839,67.6922978786627,
62.1109491954587));
#176925=CARTESIAN_POINT('Ctrl Pts',(-28.749043597868,69.1574097871512,61.1249202595484));
#176926=CARTESIAN_POINT('Ctrl Pts',(-28.6656746731545,72.791210878067,60.0229950603654));
#176927=CARTESIAN_POINT('Ctrl Pts',(-28.6291541528474,74.4762656818076,
59.8442380189926));
#176928=CARTESIAN_POINT('Ctrl Pts',(-28.5552353989382,77.8296245530595,
60.1356096181981));
#176929=CARTESIAN_POINT('Ctrl Pts',(-28.5179385729896,79.4914698953371,
60.6227695423812));
#176930=CARTESIAN_POINT('Ctrl Pts',(-28.432590730343,82.9459183275816,62.4060056730255));
#176931=CARTESIAN_POINT('Ctrl Pts',(-28.3942903930222,84.2103440468305,
63.6694196806762));
#176932=CARTESIAN_POINT('Ctrl Pts',(-28.3368489710222,85.8953250158704,
65.6718124865958));
#176933=CARTESIAN_POINT('Ctrl Pts',(-28.2993959861414,86.8343667803122,
67.138410339181));
#176934=CARTESIAN_POINT('Ctrl Pts',(-28.2228502956742,87.8868735919899,
70.4626573346849));
#176935=CARTESIAN_POINT('Ctrl Pts',(-28.1861287854085,88.1538522357153,
72.1469332660725));
#176936=CARTESIAN_POINT('Ctrl Pts',(-28.1085461465717,87.8816167397,75.6693497096587));
#176937=CARTESIAN_POINT('Ctrl Pts',(-28.071489187918,87.4204639031838,77.326781740075));
#176938=CARTESIAN_POINT('Ctrl Pts',(-27.9868394695532,85.6965669402866,
80.7751238150649));
#176939=CARTESIAN_POINT('Ctrl Pts',(-27.9484187558418,84.4514930162676,
82.0646263543981));
#176940=CARTESIAN_POINT('Ctrl Pts',(-27.8840027503118,82.2328210086097,
83.9854448061145));
#176941=CARTESIAN_POINT('Ctrl Pts',(-27.8469128057308,80.7355565107899,
84.8353927582127));
#176942=CARTESIAN_POINT('Ctrl Pts',(-27.7827496034337,77.9600462808923,
85.7525454179823));
#176943=CARTESIAN_POINT('Ctrl Pts',(-27.7448787069659,76.2410030146933,
86.1552553504064));
#176944=CARTESIAN_POINT('Ctrl Pts',(-27.6613031356659,72.4438039999917,
85.8925693173151));
#176945=CARTESIAN_POINT('Ctrl Pts',(-27.6245645194847,70.7959511083946,
85.4545391189869));
#176946=CARTESIAN_POINT('Ctrl Pts',(-27.545723918875,67.5664106015694,83.8861011614419));
#176947=CARTESIAN_POINT('Ctrl Pts',(-27.5081701457295,66.2304310118682,
82.7623462776217));
#176948=CARTESIAN_POINT('Ctrl Pts',(-27.431506954629,63.9090167105023,80.1533697833607));
#176949=CARTESIAN_POINT('Ctrl Pts',(-27.3938450433659,63.1284302719079,
78.5852444941449));
#176950=CARTESIAN_POINT('Ctrl Pts',(-27.336564037718,62.2772781947343,76.1182439307806));
#176951=CARTESIAN_POINT('Ctrl Pts',(-27.2985997691107,61.8445740460357,
74.4007921117391));
#176952=CARTESIAN_POINT('Ctrl Pts',(-27.2144471677441,62.0716673767697,
70.5744157048113));
#176953=CARTESIAN_POINT('Ctrl Pts',(-27.1780151180435,62.4847242407732,
68.935483672655));
#176954=CARTESIAN_POINT('Ctrl Pts',(-27.1051166195486,63.8981388774045,
65.9319091457067));
#176955=CARTESIAN_POINT('Ctrl Pts',(-27.0686837698037,64.8969736487736,
64.5683559877304));
#176956=CARTESIAN_POINT('Ctrl Pts',(-26.9839443790261,67.7196119249671,
61.9357859485755));
#176957=CARTESIAN_POINT('Ctrl Pts',(-26.9459015379113,69.327603593445,61.1819992045566));
#176958=CARTESIAN_POINT('Ctrl Pts',(-26.8876102860954,71.813569601353,60.2477452459042));
#176959=CARTESIAN_POINT('Ctrl Pts',(-26.8502010969373,73.5127405961876,
59.8797505089315));
#176960=CARTESIAN_POINT('Ctrl Pts',(-26.776102883949,76.8860764812136,59.9992914624847));
#176961=CARTESIAN_POINT('Ctrl Pts',(-26.7384047115212,78.6141185724286,
60.295511445562));
#176962=CARTESIAN_POINT('Ctrl Pts',(-26.6585341496444,81.9242227082905,
61.8029934063736));
#176963=CARTESIAN_POINT('Ctrl Pts',(-26.6217434954712,83.3143614652629,
62.7946497723639));
#176964=CARTESIAN_POINT('Ctrl Pts',(-26.5367444780904,85.9809277806067,
65.6007532047945));
#176965=CARTESIAN_POINT('Ctrl Pts',(-26.4986415165783,86.7489790972207,
67.2052974950796));
#176966=CARTESIAN_POINT('Ctrl Pts',(-26.4362248200088,87.7833246297908,
69.8540188908578));
#176967=CARTESIAN_POINT('Ctrl Pts',(-26.399137480781,88.0825874756072,71.5493285777499));
#176968=CARTESIAN_POINT('Ctrl Pts',(-26.3345682468581,88.0180046780585,
74.4902614964474));
#176969=CARTESIAN_POINT('Ctrl Pts',(-26.2962027710616,87.8165600689918,
76.2685907288012));
#176970=CARTESIAN_POINT('Ctrl Pts',(-26.2116136533861,86.2603114685271,
79.7928374527051));
#176971=CARTESIAN_POINT('Ctrl Pts',(-26.1745142485159,85.2763652365629,
81.2065457467116));
#176972=CARTESIAN_POINT('Ctrl Pts',(-26.0976814723828,82.7596788106203,
83.6370669645292));
#176973=CARTESIAN_POINT('Ctrl Pts',(-26.061001678293,81.3005380198983,84.514815841502));
#176974=CARTESIAN_POINT('Ctrl Pts',(-25.9817789563582,77.9559060942714,
85.8700472606715));
#176975=CARTESIAN_POINT('Ctrl Pts',(-25.9440135851621,76.2063164733864,
86.0461011698092));
#176976=CARTESIAN_POINT('Ctrl Pts',(-25.8883468613302,73.6702296561183,
86.026800080011));
#176977=CARTESIAN_POINT('Ctrl Pts',(-25.8501294132486,71.8965454052951,
85.8493490383461));
#176978=CARTESIAN_POINT('Ctrl Pts',(-25.7675740621284,68.4365062298204,
84.3765890039499));
#176979=CARTESIAN_POINT('Ctrl Pts',(-25.7302992652139,66.9790706515215,
83.441711317101));
#176980=CARTESIAN_POINT('Ctrl Pts',(-25.6539646250139,64.5392499423534,
80.9658198961808));
#176981=CARTESIAN_POINT('Ctrl Pts',(-25.6173876023456,63.6010130518938,
79.5514735758964));
#176982=CARTESIAN_POINT('Ctrl Pts',(-25.5339424579599,62.1333165939061,
76.0457160962318));
#176983=CARTESIAN_POINT('Ctrl Pts',(-25.4960524688697,61.9605630472732,
74.2878474727087));
#176984=CARTESIAN_POINT('Ctrl Pts',(-25.4316021534887,61.9411497240743,
71.3516283557702));
#176985=CARTESIAN_POINT('Ctrl Pts',(-25.394425179123,62.2657958791927,69.6567021743647));
#176986=CARTESIAN_POINT('Ctrl Pts',(-25.3304167651469,63.3694437429962,
66.957686320141));
#176987=CARTESIAN_POINT('Ctrl Pts',(-25.2918432869613,64.1915570536306,
65.356393445582));
#176988=CARTESIAN_POINT('Ctrl Pts',(-25.2071469265163,66.9068391352455,
62.6169175361422));
#176989=CARTESIAN_POINT('Ctrl Pts',(-25.1702264504549,68.3236635254637,
61.6526283543061));
#176990=CARTESIAN_POINT('Ctrl Pts',(-25.0872961958142,71.7948914737712,
60.1648056900118));
#176991=CARTESIAN_POINT('Ctrl Pts',(-25.0495042431519,73.5443650049303,
59.9662747528024));
#176992=CARTESIAN_POINT('Ctrl Pts',(-24.9874702782534,76.3698133569276,
59.9123510791511));
#176993=CARTESIAN_POINT('Ctrl Pts',(-24.9527649126985,77.9545502963124,
60.1778193699471));
#176994=CARTESIAN_POINT('Ctrl Pts',(-24.9175248385795,79.4626737065055,
60.7277865984719));
#176995=CARTESIAN_POINT('Ctrl Pts',(-24.5840827087049,74.5742912897478,
60.79818693484));
#176996=CARTESIAN_POINT('Ctrl Pts',(-24.5542910420379,75.8420333362322,
60.75391640706));
#176997=CARTESIAN_POINT('Ctrl Pts',(-24.4947077087039,78.39120740833,61.06410883866));
#176998=CARTESIAN_POINT('Ctrl Pts',(-24.4053327087039,81.887755584948,62.68064695513));
#176999=CARTESIAN_POINT('Ctrl Pts',(-24.3159577087039,84.719288560893,65.292377040265));
#177000=CARTESIAN_POINT('Ctrl Pts',(-24.2265827087039,86.61250404011,68.647152239787));
#177001=CARTESIAN_POINT('Ctrl Pts',(-24.1372077087039,87.38460819383,72.4210925622802));
#177002=CARTESIAN_POINT('Ctrl Pts',(-24.0478327087039,86.9610641626,76.249849747832));
#177003=CARTESIAN_POINT('Ctrl Pts',(-23.9584577087039,85.38276101444,79.7637835434));
#177004=CARTESIAN_POINT('Ctrl Pts',(-23.8690827087039,82.802073437376,82.623647685499));
#177005=CARTESIAN_POINT('Ctrl Pts',(-23.7797077087039,79.468149063245,84.55334187238));
#177006=CARTESIAN_POINT('Ctrl Pts',(-23.6903327087039,75.702855490151,85.36656733984));
#177007=CARTESIAN_POINT('Ctrl Pts',(-23.6009577087039,71.869706029794,84.98481273641));
#177008=CARTESIAN_POINT('Ctrl Pts',(-23.5115827087039,68.338765023158,83.44493385557));
#177009=CARTESIAN_POINT('Ctrl Pts',(-23.4222077087039,65.450920651772,80.895595461536));
#177010=CARTESIAN_POINT('Ctrl Pts',(-23.3328327087039,63.48497452013,77.582918723914));
#177011=CARTESIAN_POINT('Ctrl Pts',(-23.2434577087039,62.63072526867,73.8267199037071));
#177012=CARTESIAN_POINT('Ctrl Pts',(-23.1540827087039,62.97064481461,69.989634282714));
#177013=CARTESIAN_POINT('Ctrl Pts',(-23.0647077087039,64.47191625279,66.442106209615));
#177014=CARTESIAN_POINT('Ctrl Pts',(-22.9753327087039,66.98960210332,63.5266252341));
#177015=CARTESIAN_POINT('Ctrl Pts',(-22.8859577087039,70.280637032969,61.52466108548));
#177016=CARTESIAN_POINT('Ctrl Pts',(-22.7965827087039,74.0272941491374,
60.62948969719));
#177017=CARTESIAN_POINT('Ctrl Pts',(-22.7072077087039,77.867859356231,60.92753373859));
#177018=CARTESIAN_POINT('Ctrl Pts',(-22.6178327087039,81.431552375351,62.39001909784));
#177019=CARTESIAN_POINT('Ctrl Pts',(-22.5284577087039,84.374323041932,64.875752825426));
#177020=CARTESIAN_POINT('Ctrl Pts',(-22.4390827087039,86.41206699382,68.144754346856));
#177021=CARTESIAN_POINT('Ctrl Pts',(-22.3497077087039,87.34805400249,71.881423944257));
#177022=CARTESIAN_POINT('Ctrl Pts',(-22.2603327087039,87.09192092988,75.725011748597));
#177023=CARTESIAN_POINT('Ctrl Pts',(-22.1709577087039,85.6683956707,79.304445669906));
#177024=CARTESIAN_POINT('Ctrl Pts',(-22.0815827087039,83.214909843509,82.274155867271));
#177025=CARTESIAN_POINT('Ctrl Pts',(-21.9922077087039,79.968330708787,84.34743715126));
#177026=CARTESIAN_POINT('Ctrl Pts',(-21.9028327087039,76.242093256469,85.32412840723));
#177027=CARTESIAN_POINT('Ctrl Pts',(-21.8134577087039,72.395940203395,85.10993678068));
#177028=CARTESIAN_POINT('Ctrl Pts',(-21.7240827087039,68.801191296739,83.72554100684));
#177029=CARTESIAN_POINT('Ctrl Pts',(-21.6347077087039,65.804894934405,81.304595020325));
#177030=CARTESIAN_POINT('Ctrl Pts',(-21.5453327087049,63.69632301805,78.080824582763));
#177031=CARTESIAN_POINT('Ctrl Pts',(-21.4559577087049,62.67904373127,74.365462660522));
#177032=CARTESIAN_POINT('Ctrl Pts',(-21.3665827087049,62.8512684251,70.517202012466));
#177033=CARTESIAN_POINT('Ctrl Pts',(-21.2772077087049,64.19636998435,66.907565859634));
#177034=CARTESIAN_POINT('Ctrl Pts',(-21.1878327087049,66.584488061824,63.885039861635));
#177035=CARTESIAN_POINT('Ctrl Pts',(-21.0984577087049,69.785066205781,61.74142821188));
#177036=CARTESIAN_POINT('Ctrl Pts',(-21.0090827087049,73.489110507031,60.68368194036));
#177037=CARTESIAN_POINT('Ctrl Pts',(-20.9197077087049,77.339020845536,60.81391920844));
#177038=CARTESIAN_POINT('Ctrl Pts',(-20.8303327087049,80.963114733938,62.11956649947));
#177039=CARTESIAN_POINT('Ctrl Pts',(-20.7409577087049,84.011510717237,64.474572505729));
#177040=CARTESIAN_POINT('Ctrl Pts',(-20.6515827087049,86.18990703204,67.651577519286));
#177041=CARTESIAN_POINT('Ctrl Pts',(-20.5622077087049,87.28799442708,71.343863455311));
#177042=CARTESIAN_POINT('Ctrl Pts',(-20.4728327087049,87.19976008168,75.194965383434));
#177043=CARTESIAN_POINT('Ctrl Pts',(-20.3834577087049,85.93372241786,78.833085776478));
#177044=CARTESIAN_POINT('Ctrl Pts',(-20.2940827087049,83.612108704975,81.90698901644));
#177045=CARTESIAN_POINT('Ctrl Pts',(-20.2047077087049,80.459054853646,84.11991078892));
#177046=CARTESIAN_POINT('Ctrl Pts',(-20.1153327087049,76.77896662795,85.25820864606));
#177047=CARTESIAN_POINT('Ctrl Pts',(-20.0259577087049,72.92713135283,85.21198772236));
#177048=CARTESIAN_POINT('Ctrl Pts',(-19.9365827087049,69.275417355079,83.98571033155));
#177049=CARTESIAN_POINT('Ctrl Pts',(-19.8472077087049,66.176372622231,81.697765160933));
#177050=CARTESIAN_POINT('Ctrl Pts',(-19.7578327087049,63.9291887075,78.569037653464));
#177051=CARTESIAN_POINT('Ctrl Pts',(-19.6684577087049,62.75081583481,74.90158503273));
#177052=CARTESIAN_POINT('Ctrl Pts',(-19.5790827087049,62.75501783514,71.049474737007));
#177053=CARTESIAN_POINT('Ctrl Pts',(-19.4897077087049,63.94138904505,67.384601665003));
#177054=CARTESIAN_POINT('Ctrl Pts',(-19.4003327087049,66.195393405158,64.260784146057));
#177055=CARTESIAN_POINT('Ctrl Pts',(-19.3109577087049,69.299422377156,61.97960566264));
#177056=CARTESIAN_POINT('Ctrl Pts',(-19.2215827087049,72.953802645656,60.7612973129));
#177057=CARTESIAN_POINT('Ctrl Pts',(-19.1322077087049,76.805730932023,60.72348241298));
#177058=CARTESIAN_POINT('Ctrl Pts',(-19.0428327087049,80.48332202154,61.86979685924));
#177059=CARTESIAN_POINT('Ctrl Pts',(-18.9534577087039,83.631559184886,64.089627347503));
#177060=CARTESIAN_POINT('Ctrl Pts',(-18.8938743753709,85.17478074676,66.1421806368));
#177061=CARTESIAN_POINT('Ctrl Pts',(-18.8640827087039,85.7703123683,67.262212718386));
#177062=CARTESIAN_POINT('Ctrl Pts',(-24.7409006782679,74.5637780077301,
60.49712592814));
#177063=CARTESIAN_POINT('Ctrl Pts',(-24.7111090116019,75.8628281513697,
60.45176209751));
#177064=CARTESIAN_POINT('Ctrl Pts',(-24.6515256782679,78.47495650485,60.76961502662));
#177065=CARTESIAN_POINT('Ctrl Pts',(-24.5621506782679,82.057855268582,62.42607509136));
#177066=CARTESIAN_POINT('Ctrl Pts',(-24.4727756782679,84.95931564794,65.102304338201));
#177067=CARTESIAN_POINT('Ctrl Pts',(-24.3834006782679,86.89928588639,68.539928906151));
#177068=CARTESIAN_POINT('Ctrl Pts',(-24.2940256782679,87.6904578875,72.4070702789702));
#177069=CARTESIAN_POINT('Ctrl Pts',(-24.2046506782679,87.25645403306,76.330382269486));
#177070=CARTESIAN_POINT('Ctrl Pts',(-24.1152756782679,85.63917318558,79.931096006583));
#177071=CARTESIAN_POINT('Ctrl Pts',(-24.0259006782679,82.994753071114,82.861587217225));
#177072=CARTESIAN_POINT('Ctrl Pts',(-23.9365256782679,79.578494259545,84.83893703977));
#177073=CARTESIAN_POINT('Ctrl Pts',(-23.8471506782679,75.7202131758358,
85.67224588461));
#177074=CARTESIAN_POINT('Ctrl Pts',(-23.7577756782679,71.792400439106,85.28106348769));
#177075=CARTESIAN_POINT('Ctrl Pts',(-23.6684006782679,68.174259481666,83.70315583141));
#177076=CARTESIAN_POINT('Ctrl Pts',(-23.5790256782679,65.215097043329,81.090859097905));
#177077=CARTESIAN_POINT('Ctrl Pts',(-23.4896506782679,63.20059999972,77.696372653464));
#177078=CARTESIAN_POINT('Ctrl Pts',(-23.4002756782679,62.32525424947,73.8474109262253));
#177079=CARTESIAN_POINT('Ctrl Pts',(-23.3109006782679,62.67356843231,69.915564821625));
#177080=CARTESIAN_POINT('Ctrl Pts',(-23.2215256782679,64.21191519837,66.280427164319));
#177081=CARTESIAN_POINT('Ctrl Pts',(-23.1321506782679,66.791777698665,63.292945609594));
#177082=CARTESIAN_POINT('Ctrl Pts',(-23.0427756782679,70.164087870074,61.24154104977));
#177083=CARTESIAN_POINT('Ctrl Pts',(-22.9534006782679,74.0032722518053,
60.32426255155));
#177084=CARTESIAN_POINT('Ctrl Pts',(-22.8640256782679,77.938683874199,60.62966707439));
#177085=CARTESIAN_POINT('Ctrl Pts',(-22.7746506782679,81.590385686263,62.12826990236));
#177086=CARTESIAN_POINT('Ctrl Pts',(-22.6852756782679,84.605830876964,64.675391191609));
#177087=CARTESIAN_POINT('Ctrl Pts',(-22.5959006782679,86.69389885636,68.0251238188));
#177088=CARTESIAN_POINT('Ctrl Pts',(-22.5065256782679,87.65300095559,71.854074030477));
#177089=CARTESIAN_POINT('Ctrl Pts',(-22.4171506782679,87.39054243283,75.792582896034));
#177090=CARTESIAN_POINT('Ctrl Pts',(-22.3277756782679,85.93186186169,79.460414346857));
#177091=CARTESIAN_POINT('Ctrl Pts',(-22.2384006782679,83.417784865457,82.503464365711));
#177092=CARTESIAN_POINT('Ctrl Pts',(-22.1490256782679,80.091028367167,84.62794730547));
#177093=CARTESIAN_POINT('Ctrl Pts',(-22.0596506782679,76.272767932331,85.62875888215));
#177094=CARTESIAN_POINT('Ctrl Pts',(-21.9702756782679,72.331630466779,85.4092775894));
#177095=CARTESIAN_POINT('Ctrl Pts',(-21.8809006782679,68.648105812461,83.99069284351));
#177096=CARTESIAN_POINT('Ctrl Pts',(-21.7915256782679,65.577813057976,81.509959290305));
#177097=CARTESIAN_POINT('Ctrl Pts',(-21.7021506782679,63.41716795007,78.206574771673));
#177098=CARTESIAN_POINT('Ctrl Pts',(-21.6127756782679,62.37476598252,74.399458448487));
#177099=CARTESIAN_POINT('Ctrl Pts',(-21.5234006782689,62.55124392917,70.456161338886));
#177100=CARTESIAN_POINT('Ctrl Pts',(-21.4340256782689,63.92956405242,66.757381783671));
#177101=CARTESIAN_POINT('Ctrl Pts',(-21.3446506782689,66.376658980107,63.660211627688));
#177102=CARTESIAN_POINT('Ctrl Pts',(-21.2552756782689,69.656278449357,61.4636614468));
#177103=CARTESIAN_POINT('Ctrl Pts',(-21.1659006782689,73.451797652123,60.37979312378));
#177104=CARTESIAN_POINT('Ctrl Pts',(-21.0765256782689,77.396785192848,60.51324672522));
#177105=CARTESIAN_POINT('Ctrl Pts',(-20.9871506782689,81.110379531183,61.85113821951));
#177106=CARTESIAN_POINT('Ctrl Pts',(-20.8977756782689,84.234058556389,64.264303341857));
#177107=CARTESIAN_POINT('Ctrl Pts',(-20.8084006782689,86.46625244275,67.519767519802));
#177108=CARTESIAN_POINT('Ctrl Pts',(-20.7190256782689,87.59145815176,71.303237973316));
#177109=CARTESIAN_POINT('Ctrl Pts',(-20.6296506782689,87.50104477518,75.2494465311));
#177110=CARTESIAN_POINT('Ctrl Pts',(-20.5402756782689,86.20374110555,78.977413771966));
#177111=CARTESIAN_POINT('Ctrl Pts',(-20.4509006782689,83.824792931074,82.127229979831));
#177112=CARTESIAN_POINT('Ctrl Pts',(-20.3615256782689,80.593871412118,84.39480196293));
#177113=CARTESIAN_POINT('Ctrl Pts',(-20.2721506782689,76.822899903006,85.5612111697));
#177114=CARTESIAN_POINT('Ctrl Pts',(-20.1827756782689,72.875939887522,85.51384877627));
#177115=CARTESIAN_POINT('Ctrl Pts',(-20.0934006782689,69.134043334935,84.25728729746));
#177116=CARTESIAN_POINT('Ctrl Pts',(-20.0040256782689,65.958464741074,81.912839141965));
#177117=CARTESIAN_POINT('Ctrl Pts',(-19.9146506782689,63.65578447949,78.706844729098));
#177118=CARTESIAN_POINT('Ctrl Pts',(-19.8252756782689,62.4483105665,74.948820873245));
#177119=CARTESIAN_POINT('Ctrl Pts',(-19.7359006782689,62.45261633923,71.001579045262));
#177120=CARTESIAN_POINT('Ctrl Pts',(-19.6465256782689,63.668286116,67.246198442551));
#177121=CARTESIAN_POINT('Ctrl Pts',(-19.5571506782689,65.977955260347,64.045235275048));
#177122=CARTESIAN_POINT('Ctrl Pts',(-19.4677756782689,69.158641183889,61.70772091653));
#177123=CARTESIAN_POINT('Ctrl Pts',(-19.3784006782689,72.903269853321,60.45932528185));
#177124=CARTESIAN_POINT('Ctrl Pts',(-19.2890256782679,76.850325177053,60.42057650697));
#177125=CARTESIAN_POINT('Ctrl Pts',(-19.1996506782679,80.618737880831,61.59520028015));
#177126=CARTESIAN_POINT('Ctrl Pts',(-19.1102756782679,83.844723759108,63.869851596353));
#177127=CARTESIAN_POINT('Ctrl Pts',(-19.0506923449349,85.42605664712,65.973094643852));
#177128=CARTESIAN_POINT('Ctrl Pts',(-19.0209006782679,86.0362954892,67.120786984341));
#177129=CARTESIAN_POINT('Ctrl Pts',(-24.8977186478319,74.5532647257124,
60.19606492144));
#177130=CARTESIAN_POINT('Ctrl Pts',(-24.8679269811659,75.8836229665074,
60.14960778797));
#177131=CARTESIAN_POINT('Ctrl Pts',(-24.8083436478319,78.558705601371,60.47512121458));
#177132=CARTESIAN_POINT('Ctrl Pts',(-24.7189686478319,82.227954952215,62.1715032276));
#177133=CARTESIAN_POINT('Ctrl Pts',(-24.6295936478319,85.19934273499,64.912231636138));
#177134=CARTESIAN_POINT('Ctrl Pts',(-24.5402186478319,87.18606773268,68.432705572515));
#177135=CARTESIAN_POINT('Ctrl Pts',(-24.4508436478319,87.99630758116,72.393047995661));
#177136=CARTESIAN_POINT('Ctrl Pts',(-24.3614686478319,87.55184390352,76.41091479114));
#177137=CARTESIAN_POINT('Ctrl Pts',(-24.2720936478319,85.89558535672,80.098408469768));
#177138=CARTESIAN_POINT('Ctrl Pts',(-24.1827186478319,83.187432704849,83.09952674895));
#177139=CARTESIAN_POINT('Ctrl Pts',(-24.0933436478319,79.688839455842,85.12453220716));
#177140=CARTESIAN_POINT('Ctrl Pts',(-24.0039686478319,75.7375708615167,
85.97792442938));
#177141=CARTESIAN_POINT('Ctrl Pts',(-23.9145936478319,71.715094848414,85.57731423897));
#177142=CARTESIAN_POINT('Ctrl Pts',(-23.8252186478319,68.00975394017,83.96137780724));
#177143=CARTESIAN_POINT('Ctrl Pts',(-23.7358436478319,64.97927343488,81.286122734268));
#177144=CARTESIAN_POINT('Ctrl Pts',(-23.6464686478319,62.91622547931,77.809826583006));
#177145=CARTESIAN_POINT('Ctrl Pts',(-23.5570936478319,62.01978323026,73.8681019487347));
#177146=CARTESIAN_POINT('Ctrl Pts',(-23.4677186478319,62.37649205001,69.841495360525));
#177147=CARTESIAN_POINT('Ctrl Pts',(-23.3783436478319,63.95191414396,66.118748119013));
#177148=CARTESIAN_POINT('Ctrl Pts',(-23.2889686478319,66.593953294018,63.059265985079));
#177149=CARTESIAN_POINT('Ctrl Pts',(-23.1995936478319,70.047538707191,60.95842101407));
#177150=CARTESIAN_POINT('Ctrl Pts',(-23.1102186478319,73.979250354488,60.01903540591));
#177151=CARTESIAN_POINT('Ctrl Pts',(-23.0208436478319,78.009508392183,60.33180041019));
#177152=CARTESIAN_POINT('Ctrl Pts',(-22.9314686478319,81.749218997189,61.8665207069));
#177153=CARTESIAN_POINT('Ctrl Pts',(-22.8420936478319,84.837338712008,64.475029557805));
#177154=CARTESIAN_POINT('Ctrl Pts',(-22.7527186478319,86.97573071891,67.905493290763));
#177155=CARTESIAN_POINT('Ctrl Pts',(-22.6633436478319,87.95794790869,71.826724116717));
#177156=CARTESIAN_POINT('Ctrl Pts',(-22.5739686478319,87.68916393577,75.860154043494));
#177157=CARTESIAN_POINT('Ctrl Pts',(-22.4845936478319,86.19532805268,79.616383023829));
#177158=CARTESIAN_POINT('Ctrl Pts',(-22.3952186478319,83.620659887387,82.732772864167));
#177159=CARTESIAN_POINT('Ctrl Pts',(-22.3058436478319,80.213726025524,84.90845745969));
#177160=CARTESIAN_POINT('Ctrl Pts',(-22.2164686478319,76.303442608167,85.93338935707));
#177161=CARTESIAN_POINT('Ctrl Pts',(-22.1270936478319,72.267320730135,85.70861839811));
#177162=CARTESIAN_POINT('Ctrl Pts',(-22.0377186478319,68.495020328158,84.25584468017));
#177163=CARTESIAN_POINT('Ctrl Pts',(-21.9483436478319,65.350731181526,81.715323560263));
#177164=CARTESIAN_POINT('Ctrl Pts',(-21.8589686478319,63.13801288209,78.332324960555));
#177165=CARTESIAN_POINT('Ctrl Pts',(-21.7695936478319,62.07048823376,74.43345423642));
#177166=CARTESIAN_POINT('Ctrl Pts',(-21.6802186478319,62.25121943325,70.395120665275));
#177167=CARTESIAN_POINT('Ctrl Pts',(-21.5908436478319,63.6627581205,66.607197707679));
#177168=CARTESIAN_POINT('Ctrl Pts',(-21.5014686478319,66.168829898414,63.435383393718));
#177169=CARTESIAN_POINT('Ctrl Pts',(-21.4120936478329,69.527490692963,61.18589468171));
#177170=CARTESIAN_POINT('Ctrl Pts',(-21.3227186478329,73.414484797248,60.07590430719));
#177171=CARTESIAN_POINT('Ctrl Pts',(-21.2333436478329,77.454549540195,60.212574242));
#177172=CARTESIAN_POINT('Ctrl Pts',(-21.1439686478329,81.257644328458,61.58270993957));
#177173=CARTESIAN_POINT('Ctrl Pts',(-21.0545936478329,84.456606395566,64.054034178009));
#177174=CARTESIAN_POINT('Ctrl Pts',(-20.9652186478329,86.74259785348,67.387957520349));
#177175=CARTESIAN_POINT('Ctrl Pts',(-20.8758436478329,87.89492187645,71.262612491355));
#177176=CARTESIAN_POINT('Ctrl Pts',(-20.7864686478329,87.80232946867,75.3039276788));
#177177=CARTESIAN_POINT('Ctrl Pts',(-20.6970936478329,86.47375979323,79.121741767484));
#177178=CARTESIAN_POINT('Ctrl Pts',(-20.6077186478329,84.03747715715,82.347470943245));
#177179=CARTESIAN_POINT('Ctrl Pts',(-20.5183436478329,80.728687970562,84.66969313695));
#177180=CARTESIAN_POINT('Ctrl Pts',(-20.4289686478329,76.866833178031,85.86421369334));
#177181=CARTESIAN_POINT('Ctrl Pts',(-20.3395936478329,72.824748422185,85.81570983017));
#177182=CARTESIAN_POINT('Ctrl Pts',(-20.2502186478329,68.992669314766,84.52886426336));
#177183=CARTESIAN_POINT('Ctrl Pts',(-20.1608436478329,65.740556859899,82.127913122978));
#177184=CARTESIAN_POINT('Ctrl Pts',(-20.0714686478329,63.38238025148,78.844651804709));
#177185=CARTESIAN_POINT('Ctrl Pts',(-19.9820936478329,62.14580529819,74.996056713737));
#177186=CARTESIAN_POINT('Ctrl Pts',(-19.8927186478329,62.15021484332,70.953683353497));
#177187=CARTESIAN_POINT('Ctrl Pts',(-19.8033436478329,63.39518318695,67.107795220083));
#177188=CARTESIAN_POINT('Ctrl Pts',(-19.7139686478329,65.760517115547,63.829686404028));
#177189=CARTESIAN_POINT('Ctrl Pts',(-19.6245936478329,69.017859990633,61.43583617042));
#177190=CARTESIAN_POINT('Ctrl Pts',(-19.5352186478319,72.852737060995,60.15735325081));
#177191=CARTESIAN_POINT('Ctrl Pts',(-19.4458436478319,76.894919422089,60.11767060096));
#177192=CARTESIAN_POINT('Ctrl Pts',(-19.3564686478319,80.754153740124,61.32060370107));
#177193=CARTESIAN_POINT('Ctrl Pts',(-19.2670936478319,84.05788833333,63.650075845204));
#177194=CARTESIAN_POINT('Ctrl Pts',(-19.2075103144989,85.67733254748,65.804008650901));
#177195=CARTESIAN_POINT('Ctrl Pts',(-19.1777186478319,86.3022786101,66.979361250291));
#177196=CARTESIAN_POINT('Ctrl Pts',(-25.0545366173959,74.5427514436947,
59.89500391474));
#177197=CARTESIAN_POINT('Ctrl Pts',(-25.0247449507299,75.9044177816449,
59.84745347843));
#177198=CARTESIAN_POINT('Ctrl Pts',(-24.9651616173959,78.642454697891,60.18062740255));
#177199=CARTESIAN_POINT('Ctrl Pts',(-24.8757866173959,82.398054635848,61.91693136384));
#177200=CARTESIAN_POINT('Ctrl Pts',(-24.7864116173959,85.43936982203,64.722158934074));
#177201=CARTESIAN_POINT('Ctrl Pts',(-24.6970366173959,87.47284957896,68.325482238879));
#177202=CARTESIAN_POINT('Ctrl Pts',(-24.6076616173959,88.30215727482,72.379025712351));
#177203=CARTESIAN_POINT('Ctrl Pts',(-24.5182866173959,87.84723377397,76.491447312794));
#177204=CARTESIAN_POINT('Ctrl Pts',(-24.4289116173959,86.15199752785,80.265720932952));
#177205=CARTESIAN_POINT('Ctrl Pts',(-24.3395366173959,83.380112338587,83.33746628068));
#177206=CARTESIAN_POINT('Ctrl Pts',(-24.2501616173959,79.799184652141,85.41012737455));
#177207=CARTESIAN_POINT('Ctrl Pts',(-24.1607866173959,75.7549285472015,
86.28360297416));
#177208=CARTESIAN_POINT('Ctrl Pts',(-24.0714116173959,71.637789257726,85.87356499026));
#177209=CARTESIAN_POINT('Ctrl Pts',(-23.9820366173959,67.845248398678,84.21959978308));
#177210=CARTESIAN_POINT('Ctrl Pts',(-23.8926616173959,64.74344982644,81.481386370637));
#177211=CARTESIAN_POINT('Ctrl Pts',(-23.8032866173959,62.6318509589,77.923280512555));
#177212=CARTESIAN_POINT('Ctrl Pts',(-23.7139116173959,61.71431221106,73.8887929712528));
#177213=CARTESIAN_POINT('Ctrl Pts',(-23.6245366173959,62.07941566771,69.767425899435));
#177214=CARTESIAN_POINT('Ctrl Pts',(-23.5351616173959,63.69191308954,65.957069073716));
#177215=CARTESIAN_POINT('Ctrl Pts',(-23.4457866173959,66.396128889362,62.82558636057));
#177216=CARTESIAN_POINT('Ctrl Pts',(-23.3564116173959,69.930989544296,60.67530097837));
#177217=CARTESIAN_POINT('Ctrl Pts',(-23.2670366173959,73.955228457156,59.71380826027));
#177218=CARTESIAN_POINT('Ctrl Pts',(-23.1776616173959,78.080332910152,60.03393374599));
#177219=CARTESIAN_POINT('Ctrl Pts',(-23.0882866173959,81.908052308101,61.60477151142));
#177220=CARTESIAN_POINT('Ctrl Pts',(-22.9989116173959,85.06884654704,64.274667923988));
#177221=CARTESIAN_POINT('Ctrl Pts',(-22.9095366173959,87.25756258145,67.785862762707));
#177222=CARTESIAN_POINT('Ctrl Pts',(-22.8201616173959,88.26289486179,71.799374202937));
#177223=CARTESIAN_POINT('Ctrl Pts',(-22.7307866173959,87.98778543871,75.927725190932));
#177224=CARTESIAN_POINT('Ctrl Pts',(-22.6414116173959,86.45879424367,79.77235170078));
#177225=CARTESIAN_POINT('Ctrl Pts',(-22.5520366173959,83.823534909334,82.962081362607));
#177226=CARTESIAN_POINT('Ctrl Pts',(-22.4626616173959,80.336423683903,85.1889676139));
#177227=CARTESIAN_POINT('Ctrl Pts',(-22.3732866173959,76.334117284029,86.23801983199));
#177228=CARTESIAN_POINT('Ctrl Pts',(-22.2839116173959,72.203010993519,86.00795920683));
#177229=CARTESIAN_POINT('Ctrl Pts',(-22.1945366173959,68.34193484388,84.52099651684));
#177230=CARTESIAN_POINT('Ctrl Pts',(-22.1051616173959,65.123649305097,81.920687830243));
#177231=CARTESIAN_POINT('Ctrl Pts',(-22.0157866173959,62.85885781411,78.458075149464));
#177232=CARTESIAN_POINT('Ctrl Pts',(-21.9264116173959,61.766210485,74.467450024384));
#177233=CARTESIAN_POINT('Ctrl Pts',(-21.8370366173959,61.95119493732,70.334079991696));
#177234=CARTESIAN_POINT('Ctrl Pts',(-21.7476616173959,63.39595218857,66.457013631716));
#177235=CARTESIAN_POINT('Ctrl Pts',(-21.6582866173959,65.961000816697,63.210555159771));
#177236=CARTESIAN_POINT('Ctrl Pts',(-21.5689116173959,69.398702936539,60.90812791663));
#177237=CARTESIAN_POINT('Ctrl Pts',(-21.4795366173959,73.377171942341,59.7720154906));
#177238=CARTESIAN_POINT('Ctrl Pts',(-21.3901616173959,77.512313887507,59.91190175878));
#177239=CARTESIAN_POINT('Ctrl Pts',(-21.3007866173969,81.404909125703,61.31428165962));
#177240=CARTESIAN_POINT('Ctrl Pts',(-21.2114116173969,84.679154234719,63.843765014137));
#177241=CARTESIAN_POINT('Ctrl Pts',(-21.1220366173969,87.0189432642,67.256147520865));
#177242=CARTESIAN_POINT('Ctrl Pts',(-21.0326616173969,88.19838560114,71.22198700936));
#177243=CARTESIAN_POINT('Ctrl Pts',(-20.9432866173969,88.10361416217,75.358408826466));
#177244=CARTESIAN_POINT('Ctrl Pts',(-20.8539116173969,86.74377848093,79.266069762973));
#177245=CARTESIAN_POINT('Ctrl Pts',(-20.7645366173969,84.25016138325,82.567711906636));
#177246=CARTESIAN_POINT('Ctrl Pts',(-20.6751616173969,80.863504529035,84.94458431096));
#177247=CARTESIAN_POINT('Ctrl Pts',(-20.5857866173969,76.910766453087,86.16721621697));
#177248=CARTESIAN_POINT('Ctrl Pts',(-20.4964116173969,72.773556956877,86.11757088408));
#177249=CARTESIAN_POINT('Ctrl Pts',(-20.4070366173969,68.851295294622,84.80044122928));
#177250=CARTESIAN_POINT('Ctrl Pts',(-20.3176616173969,65.522648978742,82.34298710401));
#177251=CARTESIAN_POINT('Ctrl Pts',(-20.2282866173969,63.10897602347,78.982458880342));
#177252=CARTESIAN_POINT('Ctrl Pts',(-20.1389116173969,61.84330002988,75.043292554251));
#177253=CARTESIAN_POINT('Ctrl Pts',(-20.0495366173969,61.84781334742,70.905787661752));
#177254=CARTESIAN_POINT('Ctrl Pts',(-19.9601616173959,63.12208025789,66.969391997631));
#177255=CARTESIAN_POINT('Ctrl Pts',(-19.8707866173959,65.543078970735,63.614137533019));
#177256=CARTESIAN_POINT('Ctrl Pts',(-19.7814116173959,68.877078797366,61.16395142431));
#177257=CARTESIAN_POINT('Ctrl Pts',(-19.6920366173959,72.80220426866,59.85538121976));
#177258=CARTESIAN_POINT('Ctrl Pts',(-19.6026616173959,76.939513667119,59.81476469495));
#177259=CARTESIAN_POINT('Ctrl Pts',(-19.5132866173959,80.889569599415,61.04600712199));
#177260=CARTESIAN_POINT('Ctrl Pts',(-19.4239116173959,84.271052907552,63.430300094054));
#177261=CARTESIAN_POINT('Ctrl Pts',(-19.3643282840629,85.92860844783,65.634922657953));
#177262=CARTESIAN_POINT('Ctrl Pts',(-19.3345366173959,86.568261731,66.837935516246));
#177263=CARTESIAN_POINT('Ctrl Pts',(-19.0011309998534,82.8754003805133,
63.605888350301));
#177264=CARTESIAN_POINT('Ctrl Pts',(-19.0704950494351,82.9610760105436,
63.5038382511702));
#177265=CARTESIAN_POINT('Ctrl Pts',(-19.1398591055042,83.0467520694653,
63.4017884960521));
#177266=CARTESIAN_POINT('Ctrl Pts',(-19.2784798309862,83.2179723873018,
63.1978476809956));
#177267=CARTESIAN_POINT('Ctrl Pts',(-19.3477365217846,83.3035166713306,
63.0959565885018));
#177268=CARTESIAN_POINT('Ctrl Pts',(-19.4169932345698,83.3890614012314,
62.9940658153935));
#177269=CARTESIAN_POINT('',(-24.5011471556111,79.1897367105132,61.4776867539786));
#177270=CARTESIAN_POINT('Ctrl Pts',(-18.9799062324529,82.659284818849,63.474668109995));
#177271=CARTESIAN_POINT('Ctrl Pts',(-18.9294356932999,84.248501099275,64.932060456454));
#177272=CARTESIAN_POINT('Ctrl Pts',(-18.8284946149979,86.5752695444,68.654743887637));
#177273=CARTESIAN_POINT('Ctrl Pts',(-18.7275535366989,86.69361007784,72.8921974616309));
#177274=CARTESIAN_POINT('Ctrl Pts',(-18.6770829975479,86.22929765373,74.847875926051));
#177275=CARTESIAN_POINT('Ctrl Pts',(-19.1367242020169,82.848190368771,63.240013146138));
#177276=CARTESIAN_POINT('Ctrl Pts',(-19.0862536628639,84.478747085231,64.730686006568));
#177277=CARTESIAN_POINT('Ctrl Pts',(-18.9853125845619,86.87012683464,68.542252716656));
#177278=CARTESIAN_POINT('Ctrl Pts',(-18.8843715062629,86.99947754428,72.8890389661518));
#177279=CARTESIAN_POINT('Ctrl Pts',(-18.8339009671119,86.52649715737,74.897076676965));
#177280=CARTESIAN_POINT('Ctrl Pts',(-19.2935421715809,83.037095918694,63.005358182281));
#177281=CARTESIAN_POINT('Ctrl Pts',(-19.2430716324269,84.708993071182,64.529311556686));
#177282=CARTESIAN_POINT('Ctrl Pts',(-19.1421305541259,87.16498412488,68.429761545683));
#177283=CARTESIAN_POINT('Ctrl Pts',(-19.0411894758269,87.3053450107,72.8858804706761));
#177284=CARTESIAN_POINT('Ctrl Pts',(-18.9907189366759,86.823696661,74.94627742788));
#177285=CARTESIAN_POINT('Ctrl Pts',(-19.4503601411449,83.226001468616,62.77070321842));
#177286=CARTESIAN_POINT('Ctrl Pts',(-19.3998896019909,84.939239057138,64.327937106799));
#177287=CARTESIAN_POINT('Ctrl Pts',(-19.2989485236899,87.45984141513,68.317270374702));
#177288=CARTESIAN_POINT('Ctrl Pts',(-19.1980074453909,87.61121247713,72.8827219751971));
#177289=CARTESIAN_POINT('Ctrl Pts',(-19.1475369062399,87.12089616464,74.995478178794));
#177290=CARTESIAN_POINT('Ctrl Pts',(-19.4175174361238,83.388929634868,62.9926155500965));
#177291=CARTESIAN_POINT('Ctrl Pts',(-19.4032204672393,83.8621876848378,
63.4414112721832));
#177292=CARTESIAN_POINT('Ctrl Pts',(-19.3888608262415,84.3009905168755,
63.9263196278537));
#177293=CARTESIAN_POINT('Ctrl Pts',(-19.3744395805123,84.7010622422469,
64.4413732028743));
#177294=CARTESIAN_POINT('Ctrl Pts',(-19.3705423958794,84.8091772698555,
64.5805608233731));
#177295=CARTESIAN_POINT('Ctrl Pts',(-19.3666407123037,84.9144636261772,
64.72194968504));
#177296=CARTESIAN_POINT('Ctrl Pts',(-19.3627345508503,85.0168365456723,
64.8654214859088));
#177297=CARTESIAN_POINT('Ctrl Pts',(-19.3583084311856,85.1328365619313,
65.0279911509682));
#177298=CARTESIAN_POINT('Ctrl Pts',(-19.3538768656123,85.2450706686846,
65.1931996793289));
#177299=CARTESIAN_POINT('Ctrl Pts',(-19.3494392777582,85.3534235182666,
65.3608767801899));
#177300=CARTESIAN_POINT('Ctrl Pts',(-19.3423986111134,85.5253358992735,
65.626912881322));
#177301=CARTESIAN_POINT('Ctrl Pts',(-19.3353359681688,85.6874616819676,
65.8991738812724));
#177302=CARTESIAN_POINT('Ctrl Pts',(-19.3282589746455,85.8393581862296,
66.1769664936222));
#177303=CARTESIAN_POINT('Ctrl Pts',(-19.3213083493066,85.9885423967203,
66.449798786603));
#177304=CARTESIAN_POINT('Ctrl Pts',(-19.3143438813069,86.1278596552626,
66.7279675738523));
#177305=CARTESIAN_POINT('Ctrl Pts',(-19.3073727951192,86.2568501668907,
67.0108436589344));
#177306=CARTESIAN_POINT('Ctrl Pts',(-19.29832459757,86.424274812026,67.3780057669402));
#177307=CARTESIAN_POINT('Ctrl Pts',(-19.2892464024017,86.5745484311984,
67.7536630701635));
#177308=CARTESIAN_POINT('Ctrl Pts',(-19.2801213644855,86.7062645729879,
68.1360633882202));
#177309=CARTESIAN_POINT('Ctrl Pts',(-19.2782027681902,86.7339587156302,
68.2164654468505));
#177310=CARTESIAN_POINT('Ctrl Pts',(-19.2762821010851,86.760832549227,68.2971654300741));
#177311=CARTESIAN_POINT('Ctrl Pts',(-19.2743592065957,86.7868731270772,
68.3781467925786));
#177312=CARTESIAN_POINT('Ctrl Pts',(-19.2735558745621,86.7977521589094,
68.4119785618106));
#177313=CARTESIAN_POINT('Ctrl Pts',(-19.272751612069,86.8084848102752,68.445859771803));
#177314=CARTESIAN_POINT('Ctrl Pts',(-19.2719468277685,86.819070927241,68.4797889760641));
#177315=CARTESIAN_POINT('Ctrl Pts',(-19.2713566720992,86.8268338233854,
68.5046695710729));
#177316=CARTESIAN_POINT('Ctrl Pts',(-19.270766235899,86.8345179219805,68.5295759752025));
#177317=CARTESIAN_POINT('Ctrl Pts',(-19.2701755446975,86.8421231642585,
68.5545076247401));
#177318=CARTESIAN_POINT('Ctrl Pts',(-19.2583305133496,86.9946298089418,
69.0544578010013));
#177319=CARTESIAN_POINT('Ctrl Pts',(-19.2464062952224,87.1153540390979,
69.564319294164));
#177320=CARTESIAN_POINT('Ctrl Pts',(-19.2344955395952,87.2038929865606,
70.0794616457638));
#177321=CARTESIAN_POINT('Ctrl Pts',(-19.2255648541586,87.2702794958154,
70.4657154185047));
#177322=CARTESIAN_POINT('Ctrl Pts',(-19.2166306713089,87.3186150091839,
70.8551919742187));
#177323=CARTESIAN_POINT('Ctrl Pts',(-19.2076647208652,87.3486597642837,
71.2459541183869));
#177324=CARTESIAN_POINT('Ctrl Pts',(-19.2044523919758,87.3594242264995,
71.3859567352262));
#177325=CARTESIAN_POINT('Ctrl Pts',(-19.2012374970565,87.3678345149059,
71.5260384699884));
#177326=CARTESIAN_POINT('Ctrl Pts',(-19.1980166927661,87.3738885371928,
71.666139079149));
#177327=CARTESIAN_POINT('Ctrl Pts',(-19.193379589662,87.3826047220359,71.8678467617762));
#177328=CARTESIAN_POINT('Ctrl Pts',(-19.1887351237912,87.3864339891829,
72.0695940567423));
#177329=CARTESIAN_POINT('Ctrl Pts',(-19.184087360571,87.3854106257393,72.2711996352709));
#177330=CARTESIAN_POINT('Ctrl Pts',(-19.1794322607388,87.3843856468905,
72.4731234533085));
#177331=CARTESIAN_POINT('Ctrl Pts',(-19.1747738531391,87.3784927198538,
72.6749058999744));
#177332=CARTESIAN_POINT('Ctrl Pts',(-19.1701162224715,87.3677144817021,
72.8763672965244));
#177333=CARTESIAN_POINT('Ctrl Pts',(-19.1691220913346,87.3654139596315,
72.9193674958705));
#177334=CARTESIAN_POINT('Ctrl Pts',(-19.1681279955927,87.362890688285,72.962353053272));
#177335=CARTESIAN_POINT('Ctrl Pts',(-19.1671339749643,87.3601441923391,
73.0053221826803));
#177336=CARTESIAN_POINT('Ctrl Pts',(-19.164564094539,87.3530435689029,73.1164119542731));
#177337=CARTESIAN_POINT('Ctrl Pts',(-19.1619911494633,87.344447828162,73.2274437727421));
#177338=CARTESIAN_POINT('Ctrl Pts',(-19.1594114054907,87.3343429044137,
73.3383711450185));
#177339=CARTESIAN_POINT('Ctrl Pts',(-19.1547191646531,87.315963275902,73.5401345570934));
#177340=CARTESIAN_POINT('Ctrl Pts',(-19.1500219576322,87.2926435057615,
73.7415587553322));
#177341=CARTESIAN_POINT('Ctrl Pts',(-19.1453140801817,87.2642981382976,
73.9423640347745));
#177342=CARTESIAN_POINT('Ctrl Pts',(-19.1406652548541,87.2363083140989,
74.1406505617326));
#177343=CARTESIAN_POINT('Ctrl Pts',(-19.1360060251019,87.2034181226359,
74.3383335922857));
#177344=CARTESIAN_POINT('Ctrl Pts',(-19.1313308986475,87.1655957877574,
74.5351501296208));
#177345=CARTESIAN_POINT('Ctrl Pts',(-19.129685292205,87.1522826338667,74.6044279480896));
#177346=CARTESIAN_POINT('Ctrl Pts',(-19.1280377161887,87.1383588610024,
74.6735984676939));
#177347=CARTESIAN_POINT('Ctrl Pts',(-19.1263879310737,87.1238246165211,
74.7426504105179));
#177348=CARTESIAN_POINT('Ctrl Pts',(-19.7210834129279,83.3320088770948,
62.9389668654546));
#177349=CARTESIAN_POINT('Ctrl Pts',(-19.0031848503602,83.3320088770948,
62.9389668654546));
#177350=CARTESIAN_POINT('Ctrl Pts',(-19.7210834129279,84.1021422518589,
63.6603901351978));
#177351=CARTESIAN_POINT('Ctrl Pts',(-19.0031848503602,84.1021422518589,
63.6603901351978));
#177352=CARTESIAN_POINT('Ctrl Pts',(-19.7210834129279,84.7817891561514,
64.4762669802466));
#177353=CARTESIAN_POINT('Ctrl Pts',(-19.0031848503602,84.7817891561514,
64.4762669802466));
#177354=CARTESIAN_POINT('Ctrl Pts',(-19.7210834129279,85.9590960090797,
66.2981609192099));
#177355=CARTESIAN_POINT('Ctrl Pts',(-19.0031848503602,85.9590960090797,
66.2981609192099));
#177356=CARTESIAN_POINT('Ctrl Pts',(-19.7210834129279,86.4453006331497,
67.315919751713));
#177357=CARTESIAN_POINT('Ctrl Pts',(-19.0031848503602,86.4453006331497,
67.315919751713));
#177358=CARTESIAN_POINT('Ctrl Pts',(-19.7210834129279,87.1284456210047,
69.4403738334441));
#177359=CARTESIAN_POINT('Ctrl Pts',(-19.0031848503602,87.1284456210047,
69.4403738334441));
#177360=CARTESIAN_POINT('Ctrl Pts',(-19.7210834129279,87.3257156024833,
70.5513335535036));
#177361=CARTESIAN_POINT('Ctrl Pts',(-19.0031848503602,87.3257156024833,
70.5513335535036));
#177362=CARTESIAN_POINT('Ctrl Pts',(-19.7210834129279,87.3979750045476,
72.2235418419717));
#177363=CARTESIAN_POINT('Ctrl Pts',(-19.0031848503602,87.3979750045476,
72.2235418419717));
#177364=CARTESIAN_POINT('Ctrl Pts',(-19.7210834129279,87.3848332607061,
72.7841104016103));
#177365=CARTESIAN_POINT('Ctrl Pts',(-19.0031848503602,87.3848332607061,
72.7841104016103));
#177366=CARTESIAN_POINT('Ctrl Pts',(-19.7210834129279,87.2890617556199,
73.8354475183249));
#177367=CARTESIAN_POINT('Ctrl Pts',(-19.0031848503602,87.2890617556199,
73.8354475183249));
#177368=CARTESIAN_POINT('Ctrl Pts',(-19.7210834129279,87.2139739637454,
74.3287972481997));
#177369=CARTESIAN_POINT('Ctrl Pts',(-19.0031848503602,87.2139739637454,
74.3287972481997));
#177370=CARTESIAN_POINT('Ctrl Pts',(-19.7210834129279,87.1076595086348,
74.8182427933889));
#177371=CARTESIAN_POINT('Ctrl Pts',(-19.0031848503602,87.1076595086348,
74.8182427933889));
#177372=CARTESIAN_POINT('Ctrl Pts',(-19.7175219896828,83.3888301557713,
62.9925212140073));
#177373=CARTESIAN_POINT('Ctrl Pts',(-19.7032357686156,83.8619600719994,
63.4411857890303));
#177374=CARTESIAN_POINT('Ctrl Pts',(-19.6888822186524,84.3006547083239,
63.9259433661352));
#177375=CARTESIAN_POINT('Ctrl Pts',(-19.674461721319,84.7006418514101,64.4408320198575));
#177376=CARTESIAN_POINT('Ctrl Pts',(-19.6707792859391,84.8027830448213,
64.5723145999207));
#177377=CARTESIAN_POINT('Ctrl Pts',(-19.6670924849655,84.9023999937689,
64.7057617926793));
#177378=CARTESIAN_POINT('Ctrl Pts',(-19.6634013247513,84.9994212391248,
64.8410738773966));
#177379=CARTESIAN_POINT('Ctrl Pts',(-19.6587526282975,85.1216110908412,
65.0114877234196));
#177380=CARTESIAN_POINT('Ctrl Pts',(-19.6540986130407,85.2396562484237,
65.1848208107002));
#177381=CARTESIAN_POINT('Ctrl Pts',(-19.6494392777599,85.3534235182665,
65.3608767801898));
#177382=CARTESIAN_POINT('Ctrl Pts',(-19.6424230631589,85.5247388522517,
65.6259889451812));
#177383=CARTESIAN_POINT('Ctrl Pts',(-19.6354021244995,85.68633772351,65.8972863128462));
#177384=CARTESIAN_POINT('Ctrl Pts',(-19.6283648699484,85.8377823502123,
66.1740854297724));
#177385=CARTESIAN_POINT('Ctrl Pts',(-19.621843385339,85.9781273945805,66.43059756356));
#177386=CARTESIAN_POINT('Ctrl Pts',(-19.6153078888228,86.1097519757193,
66.6918353088855));
#177387=CARTESIAN_POINT('Ctrl Pts',(-19.6087491550728,86.2322746523157,
66.9572772307433));
#177388=CARTESIAN_POINT('Ctrl Pts',(-19.5999665130593,86.3963418104133,
67.3127240995923));
#177389=CARTESIAN_POINT('Ctrl Pts',(-19.5911412883923,86.5441725466508,
67.6759164140595));
#177390=CARTESIAN_POINT('Ctrl Pts',(-19.5822984309476,86.6745701714822,
68.0451907180569));
#177391=CARTESIAN_POINT('Ctrl Pts',(-19.579653377885,86.7135743778791,68.1556471101027));
#177392=CARTESIAN_POINT('Ctrl Pts',(-19.5770067471956,86.7510191125115,
68.26664746382));
#177393=CARTESIAN_POINT('Ctrl Pts',(-19.5743592065984,86.7868731270772,
68.3781467925785));
#177394=CARTESIAN_POINT('Ctrl Pts',(-19.5735592697391,86.7977061801516,
68.4118355764103));
#177395=CARTESIAN_POINT('Ctrl Pts',(-19.5727597867005,86.8083930780443,
68.4455702452619));
#177396=CARTESIAN_POINT('Ctrl Pts',(-19.571960356956,86.8189337354123,68.4793492961659));
#177397=CARTESIAN_POINT('Ctrl Pts',(-19.5719568884247,86.8189794687629,
68.4794958552583));
#177398=CARTESIAN_POINT('Ctrl Pts',(-19.5719534198934,86.8190251993725,
68.4796424152244));
#177399=CARTESIAN_POINT('Ctrl Pts',(-19.5719499513622,86.819070927241,68.4797889760641));
#177400=CARTESIAN_POINT('Ctrl Pts',(-19.5599906187491,86.9767384694338,
68.9851238653064));
#177401=CARTESIAN_POINT('Ctrl Pts',(-19.5480134164975,87.1018196188291,
69.5008432106858));
#177402=CARTESIAN_POINT('Ctrl Pts',(-19.5359444704607,87.193903283335,70.0221345398778));
#177403=CARTESIAN_POINT('Ctrl Pts',(-19.5269013179855,87.2629007431023,
70.4127334338933));
#177404=CARTESIAN_POINT('Ctrl Pts',(-19.5178062838736,87.3134180275645,
70.8067205289831));
#177405=CARTESIAN_POINT('Ctrl Pts',(-19.5086971906096,87.3452097472485,
71.2020880584462));
#177406=CARTESIAN_POINT('Ctrl Pts',(-19.5051350676615,87.3576419412074,
71.3566970528696));
#177407=CARTESIAN_POINT('Ctrl Pts',(-19.5015738726351,87.3672022426337,
71.511406589515));
#177408=CARTESIAN_POINT('Ctrl Pts',(-19.4980166927664,87.3738885371928,
71.666139079149));
#177409=CARTESIAN_POINT('Ctrl Pts',(-19.4934105162435,87.3825465905272,
71.8665014975215));
#177410=CARTESIAN_POINT('Ctrl Pts',(-19.4888065269328,87.386382737324,72.0669026460856));
#177411=CARTESIAN_POINT('Ctrl Pts',(-19.4841972065756,87.3854304240733,
72.2671719933372));
#177412=CARTESIAN_POINT('Ctrl Pts',(-19.4795811934391,87.3844767280543,
72.4677321336821));
#177413=CARTESIAN_POINT('Ctrl Pts',(-19.4749598337635,87.3787206699474,
72.6681608773103));
#177414=CARTESIAN_POINT('Ctrl Pts',(-19.4703255764928,87.3681440282755,
72.8682892798773));
#177415=CARTESIAN_POINT('Ctrl Pts',(-19.4694361642207,87.3661141463868,
72.9066981654557));
#177416=CARTESIAN_POINT('Ctrl Pts',(-19.4685462768817,87.3639065508694,
72.9450959748942));
#177417=CARTESIAN_POINT('Ctrl Pts',(-19.4676558610962,87.3615208940382,
72.9834814859482));
#177418=CARTESIAN_POINT('Ctrl Pts',(-19.4649097591887,87.35416336862,73.1018649724439));
#177419=CARTESIAN_POINT('Ctrl Pts',(-19.4621600849288,87.3451095527422,
73.2201796537156));
#177420=CARTESIAN_POINT('Ctrl Pts',(-19.4594114054906,87.3343429044137,
73.3383711450185));
#177421=CARTESIAN_POINT('Ctrl Pts',(-19.4546834481501,87.3158233734374,
73.5416703443159));
#177422=CARTESIAN_POINT('Ctrl Pts',(-19.4499407562388,87.2922895922582,
73.7446106609143));
#177423=CARTESIAN_POINT('Ctrl Pts',(-19.4451892350924,87.2636549340332,
73.9469144504035));
#177424=CARTESIAN_POINT('Ctrl Pts',(-19.4404973026353,87.2353793822287,
74.1466811539214));
#177425=CARTESIAN_POINT('Ctrl Pts',(-19.4357967610088,87.2021300366619,
74.3458271887575));
#177426=CARTESIAN_POINT('Ctrl Pts',(-19.4310932961472,87.1638740066269,
74.5440915419293));
#177427=CARTESIAN_POINT('Ctrl Pts',(-19.4295207442365,87.1510835223988,
74.6103790547719));
#177428=CARTESIAN_POINT('Ctrl Pts',(-19.4279478655589,87.1377338036843,
74.6765680641747));
#177429=CARTESIAN_POINT('Ctrl Pts',(-19.4263748726166,87.1238249181727,
74.7426489773759));
#177430=CARTESIAN_POINT('Ctrl Pts',(-19.6963598728939,83.226001468616,62.77070321842));
#177431=CARTESIAN_POINT('Ctrl Pts',(-19.6458893337409,84.939239057138,64.327937106799));
#177432=CARTESIAN_POINT('Ctrl Pts',(-19.5449482554399,87.45984141513,68.317270374702));
#177433=CARTESIAN_POINT('Ctrl Pts',(-19.4440071771409,87.61121247713,72.8827219751971));
#177434=CARTESIAN_POINT('Ctrl Pts',(-19.3935366379889,87.12089616464,74.995478178794));
#177435=CARTESIAN_POINT('Ctrl Pts',(-19.8531778424579,83.037095918694,63.005358182281));
#177436=CARTESIAN_POINT('Ctrl Pts',(-19.8027073033049,84.708993071182,64.529311556686));
#177437=CARTESIAN_POINT('Ctrl Pts',(-19.7017662250039,87.16498412488,68.429761545683));
#177438=CARTESIAN_POINT('Ctrl Pts',(-19.6008251467039,87.3053450107,72.8858804706761));
#177439=CARTESIAN_POINT('Ctrl Pts',(-19.5503546075529,86.823696661,74.94627742788));
#177440=CARTESIAN_POINT('Ctrl Pts',(-20.0099958120219,82.848190368771,63.240013146138));
#177441=CARTESIAN_POINT('Ctrl Pts',(-19.9595252728689,84.478747085231,64.730686006568));
#177442=CARTESIAN_POINT('Ctrl Pts',(-19.8585841945679,86.87012683464,68.542252716656));
#177443=CARTESIAN_POINT('Ctrl Pts',(-19.7576431162679,86.99947754428,72.8890389661519));
#177444=CARTESIAN_POINT('Ctrl Pts',(-19.7071725771169,86.52649715737,74.897076676965));
#177445=CARTESIAN_POINT('Ctrl Pts',(-20.1668137815859,82.659284818849,63.474668109995));
#177446=CARTESIAN_POINT('Ctrl Pts',(-20.1163432424329,84.248501099275,64.932060456454));
#177447=CARTESIAN_POINT('Ctrl Pts',(-20.0154021641319,86.5752695444,68.654743887637));
#177448=CARTESIAN_POINT('Ctrl Pts',(-19.9144610858319,86.69361007784,72.8921974616309));
#177449=CARTESIAN_POINT('Ctrl Pts',(-19.8639905466809,86.22929765373,74.847875926051));
#177450=CARTESIAN_POINT('Ctrl Pts',(-19.7180890220136,83.3888904642227,
62.9941398919268));
#177451=CARTESIAN_POINT('Ctrl Pts',(-19.7872818648352,83.3034260995692,
63.0959359304728));
#177452=CARTESIAN_POINT('Ctrl Pts',(-19.8564746782248,83.2179621899393,
63.1977322762277));
#177453=CARTESIAN_POINT('Ctrl Pts',(-19.9950718297746,83.0467739441428,
63.4016368653651));
#177454=CARTESIAN_POINT('Ctrl Pts',(-20.0644762132755,82.9610495545407,
63.5037451776019));
#177455=CARTESIAN_POINT('Ctrl Pts',(-20.1338805884022,82.8753255974315,
63.6058538308433));
#177456=CARTESIAN_POINT('Ctrl Pts',(-25.3005363491459,74.5427514436947,
59.89500391474));
#177457=CARTESIAN_POINT('Ctrl Pts',(-25.2707446824789,75.9044177816449,
59.84745347843));
#177458=CARTESIAN_POINT('Ctrl Pts',(-25.2111613491459,78.642454697891,60.18062740255));
#177459=CARTESIAN_POINT('Ctrl Pts',(-25.1217863491459,82.398054635848,61.91693136384));
#177460=CARTESIAN_POINT('Ctrl Pts',(-25.0324113491459,85.43936982203,64.722158934074));
#177461=CARTESIAN_POINT('Ctrl Pts',(-24.9430363491459,87.47284957896,68.325482238879));
#177462=CARTESIAN_POINT('Ctrl Pts',(-24.8536613491459,88.30215727482,72.3790257123511));
#177463=CARTESIAN_POINT('Ctrl Pts',(-24.7642863491459,87.84723377397,76.491447312794));
#177464=CARTESIAN_POINT('Ctrl Pts',(-24.6749113491459,86.15199752785,80.265720932952));
#177465=CARTESIAN_POINT('Ctrl Pts',(-24.5855363491449,83.380112338587,83.33746628068));
#177466=CARTESIAN_POINT('Ctrl Pts',(-24.4961613491449,79.799184652141,85.41012737455));
#177467=CARTESIAN_POINT('Ctrl Pts',(-24.4067863491449,75.7549285472016,
86.28360297416));
#177468=CARTESIAN_POINT('Ctrl Pts',(-24.3174113491449,71.637789257726,85.87356499026));
#177469=CARTESIAN_POINT('Ctrl Pts',(-24.2280363491449,67.845248398678,84.21959978308));
#177470=CARTESIAN_POINT('Ctrl Pts',(-24.1386613491449,64.74344982644,81.481386370637));
#177471=CARTESIAN_POINT('Ctrl Pts',(-24.0492863491449,62.6318509589,77.923280512555));
#177472=CARTESIAN_POINT('Ctrl Pts',(-23.9599113491449,61.71431221106,73.8887929712529));
#177473=CARTESIAN_POINT('Ctrl Pts',(-23.8705363491449,62.07941566771,69.767425899435));
#177474=CARTESIAN_POINT('Ctrl Pts',(-23.7811613491449,63.69191308954,65.957069073716));
#177475=CARTESIAN_POINT('Ctrl Pts',(-23.6917863491449,66.396128889362,62.82558636057));
#177476=CARTESIAN_POINT('Ctrl Pts',(-23.6024113491449,69.930989544296,60.67530097837));
#177477=CARTESIAN_POINT('Ctrl Pts',(-23.5130363491449,73.955228457156,59.71380826027));
#177478=CARTESIAN_POINT('Ctrl Pts',(-23.4236613491449,78.080332910152,60.03393374599));
#177479=CARTESIAN_POINT('Ctrl Pts',(-23.3342863491449,81.908052308101,61.60477151142));
#177480=CARTESIAN_POINT('Ctrl Pts',(-23.2449113491459,85.06884654704,64.274667923988));
#177481=CARTESIAN_POINT('Ctrl Pts',(-23.1555363491459,87.25756258145,67.785862762707));
#177482=CARTESIAN_POINT('Ctrl Pts',(-23.0661613491459,88.26289486179,71.799374202937));
#177483=CARTESIAN_POINT('Ctrl Pts',(-22.9767863491459,87.98778543871,75.927725190932));
#177484=CARTESIAN_POINT('Ctrl Pts',(-22.8874113491459,86.45879424367,79.77235170078));
#177485=CARTESIAN_POINT('Ctrl Pts',(-22.7980363491459,83.823534909334,82.962081362607));
#177486=CARTESIAN_POINT('Ctrl Pts',(-22.7086613491459,80.336423683903,85.1889676139));
#177487=CARTESIAN_POINT('Ctrl Pts',(-22.6192863491459,76.334117284029,86.23801983199));
#177488=CARTESIAN_POINT('Ctrl Pts',(-22.5299113491459,72.203010993519,86.00795920683));
#177489=CARTESIAN_POINT('Ctrl Pts',(-22.4405363491459,68.34193484388,84.52099651684));
#177490=CARTESIAN_POINT('Ctrl Pts',(-22.3511613491459,65.123649305097,81.920687830243));
#177491=CARTESIAN_POINT('Ctrl Pts',(-22.2617863491459,62.85885781411,78.458075149464));
#177492=CARTESIAN_POINT('Ctrl Pts',(-22.1724113491459,61.766210485,74.467450024384));
#177493=CARTESIAN_POINT('Ctrl Pts',(-22.0830363491459,61.95119493732,70.334079991696));
#177494=CARTESIAN_POINT('Ctrl Pts',(-21.9936613491459,63.39595218857,66.457013631716));
#177495=CARTESIAN_POINT('Ctrl Pts',(-21.9042863491459,65.961000816697,63.210555159771));
#177496=CARTESIAN_POINT('Ctrl Pts',(-21.8149113491459,69.398702936539,60.90812791663));
#177497=CARTESIAN_POINT('Ctrl Pts',(-21.7255363491459,73.377171942341,59.7720154906));
#177498=CARTESIAN_POINT('Ctrl Pts',(-21.6361613491459,77.512313887507,59.91190175878));
#177499=CARTESIAN_POINT('Ctrl Pts',(-21.5467863491459,81.404909125703,61.31428165962));
#177500=CARTESIAN_POINT('Ctrl Pts',(-21.4574113491459,84.679154234719,63.843765014137));
#177501=CARTESIAN_POINT('Ctrl Pts',(-21.3680363491459,87.0189432642,67.256147520865));
#177502=CARTESIAN_POINT('Ctrl Pts',(-21.2786613491459,88.19838560114,71.22198700936));
#177503=CARTESIAN_POINT('Ctrl Pts',(-21.1892863491459,88.10361416217,75.358408826466));
#177504=CARTESIAN_POINT('Ctrl Pts',(-21.0999113491459,86.74377848093,79.266069762973));
#177505=CARTESIAN_POINT('Ctrl Pts',(-21.0105363491459,84.25016138325,82.567711906636));
#177506=CARTESIAN_POINT('Ctrl Pts',(-20.9211613491459,80.863504529035,84.94458431096));
#177507=CARTESIAN_POINT('Ctrl Pts',(-20.8317863491459,76.910766453087,86.16721621697));
#177508=CARTESIAN_POINT('Ctrl Pts',(-20.7424113491459,72.773556956877,86.11757088408));
#177509=CARTESIAN_POINT('Ctrl Pts',(-20.6530363491459,68.851295294622,84.80044122928));
#177510=CARTESIAN_POINT('Ctrl Pts',(-20.5636613491459,65.522648978742,82.34298710401));
#177511=CARTESIAN_POINT('Ctrl Pts',(-20.4742863491459,63.10897602347,78.982458880342));
#177512=CARTESIAN_POINT('Ctrl Pts',(-20.3849113491459,61.84330002988,75.043292554251));
#177513=CARTESIAN_POINT('Ctrl Pts',(-20.2955363491459,61.84781334742,70.905787661752));
#177514=CARTESIAN_POINT('Ctrl Pts',(-20.2061613491459,63.12208025789,66.969391997631));
#177515=CARTESIAN_POINT('Ctrl Pts',(-20.1167863491459,65.543078970735,63.614137533019));
#177516=CARTESIAN_POINT('Ctrl Pts',(-20.0274113491459,68.877078797366,61.16395142431));
#177517=CARTESIAN_POINT('Ctrl Pts',(-19.9380363491459,72.80220426866,59.85538121976));
#177518=CARTESIAN_POINT('Ctrl Pts',(-19.8486613491459,76.939513667119,59.81476469495));
#177519=CARTESIAN_POINT('Ctrl Pts',(-19.7592863491459,80.889569599415,61.04600712199));
#177520=CARTESIAN_POINT('Ctrl Pts',(-19.6699113491459,84.271052907551,63.430300094054));
#177521=CARTESIAN_POINT('Ctrl Pts',(-19.6103280158119,85.92860844783,65.634922657953));
#177522=CARTESIAN_POINT('Ctrl Pts',(-19.5805363491459,86.568261731,66.837935516246));
#177523=CARTESIAN_POINT('Ctrl Pts',(-25.4573543187099,74.5532647257124,
60.19606492144));
#177524=CARTESIAN_POINT('Ctrl Pts',(-25.4275626520429,75.8836229665074,
60.14960778797));
#177525=CARTESIAN_POINT('Ctrl Pts',(-25.3679793187099,78.558705601371,60.47512121458));
#177526=CARTESIAN_POINT('Ctrl Pts',(-25.2786043187099,82.227954952215,62.1715032276));
#177527=CARTESIAN_POINT('Ctrl Pts',(-25.1892293187099,85.19934273499,64.912231636138));
#177528=CARTESIAN_POINT('Ctrl Pts',(-25.0998543187099,87.18606773268,68.432705572515));
#177529=CARTESIAN_POINT('Ctrl Pts',(-25.0104793187089,87.99630758116,72.393047995661));
#177530=CARTESIAN_POINT('Ctrl Pts',(-24.9211043187089,87.55184390352,76.41091479114));
#177531=CARTESIAN_POINT('Ctrl Pts',(-24.8317293187089,85.89558535672,80.098408469768));
#177532=CARTESIAN_POINT('Ctrl Pts',(-24.7423543187089,83.187432704849,83.09952674895));
#177533=CARTESIAN_POINT('Ctrl Pts',(-24.6529793187089,79.688839455842,85.12453220716));
#177534=CARTESIAN_POINT('Ctrl Pts',(-24.5636043187089,75.7375708615168,
85.97792442938));
#177535=CARTESIAN_POINT('Ctrl Pts',(-24.4742293187089,71.715094848414,85.57731423897));
#177536=CARTESIAN_POINT('Ctrl Pts',(-24.3848543187089,68.00975394017,83.96137780724));
#177537=CARTESIAN_POINT('Ctrl Pts',(-24.2954793187089,64.97927343488,81.286122734268));
#177538=CARTESIAN_POINT('Ctrl Pts',(-24.2061043187089,62.91622547931,77.809826583006));
#177539=CARTESIAN_POINT('Ctrl Pts',(-24.1167293187089,62.01978323026,73.8681019487348));
#177540=CARTESIAN_POINT('Ctrl Pts',(-24.0273543187089,62.37649205001,69.841495360525));
#177541=CARTESIAN_POINT('Ctrl Pts',(-23.9379793187089,63.95191414396,66.118748119013));
#177542=CARTESIAN_POINT('Ctrl Pts',(-23.8486043187089,66.593953294018,63.059265985079));
#177543=CARTESIAN_POINT('Ctrl Pts',(-23.7592293187089,70.047538707191,60.95842101407));
#177544=CARTESIAN_POINT('Ctrl Pts',(-23.6698543187089,73.979250354488,60.01903540591));
#177545=CARTESIAN_POINT('Ctrl Pts',(-23.5804793187089,78.009508392183,60.33180041019));
#177546=CARTESIAN_POINT('Ctrl Pts',(-23.4911043187089,81.749218997189,61.8665207069));
#177547=CARTESIAN_POINT('Ctrl Pts',(-23.4017293187089,84.837338712008,64.475029557805));
#177548=CARTESIAN_POINT('Ctrl Pts',(-23.3123543187089,86.97573071891,67.905493290763));
#177549=CARTESIAN_POINT('Ctrl Pts',(-23.2229793187089,87.95794790869,71.826724116717));
#177550=CARTESIAN_POINT('Ctrl Pts',(-23.1336043187099,87.68916393577,75.860154043494));
#177551=CARTESIAN_POINT('Ctrl Pts',(-23.0442293187099,86.19532805268,79.616383023829));
#177552=CARTESIAN_POINT('Ctrl Pts',(-22.9548543187099,83.620659887386,82.732772864167));
#177553=CARTESIAN_POINT('Ctrl Pts',(-22.8654793187099,80.213726025524,84.90845745969));
#177554=CARTESIAN_POINT('Ctrl Pts',(-22.7761043187099,76.303442608167,85.93338935707));
#177555=CARTESIAN_POINT('Ctrl Pts',(-22.6867293187099,72.267320730135,85.70861839811));
#177556=CARTESIAN_POINT('Ctrl Pts',(-22.5973543187099,68.495020328158,84.25584468017));
#177557=CARTESIAN_POINT('Ctrl Pts',(-22.5079793187099,65.350731181526,81.715323560263));
#177558=CARTESIAN_POINT('Ctrl Pts',(-22.4186043187099,63.13801288209,78.332324960555));
#177559=CARTESIAN_POINT('Ctrl Pts',(-22.3292293187099,62.07048823376,74.43345423642));
#177560=CARTESIAN_POINT('Ctrl Pts',(-22.2398543187099,62.25121943325,70.395120665275));
#177561=CARTESIAN_POINT('Ctrl Pts',(-22.1504793187099,63.6627581205,66.607197707679));
#177562=CARTESIAN_POINT('Ctrl Pts',(-22.0611043187099,66.168829898414,63.435383393718));
#177563=CARTESIAN_POINT('Ctrl Pts',(-21.9717293187099,69.527490692963,61.18589468171));
#177564=CARTESIAN_POINT('Ctrl Pts',(-21.8823543187099,73.414484797248,60.07590430719));
#177565=CARTESIAN_POINT('Ctrl Pts',(-21.7929793187099,77.454549540195,60.212574242));
#177566=CARTESIAN_POINT('Ctrl Pts',(-21.7036043187099,81.257644328458,61.58270993957));
#177567=CARTESIAN_POINT('Ctrl Pts',(-21.6142293187099,84.456606395566,64.054034178009));
#177568=CARTESIAN_POINT('Ctrl Pts',(-21.5248543187099,86.74259785348,67.387957520349));
#177569=CARTESIAN_POINT('Ctrl Pts',(-21.4354793187099,87.89492187645,71.262612491355));
#177570=CARTESIAN_POINT('Ctrl Pts',(-21.3461043187099,87.80232946867,75.3039276788));
#177571=CARTESIAN_POINT('Ctrl Pts',(-21.2567293187099,86.47375979323,79.121741767484));
#177572=CARTESIAN_POINT('Ctrl Pts',(-21.1673543187099,84.03747715715,82.347470943245));
#177573=CARTESIAN_POINT('Ctrl Pts',(-21.0779793187099,80.728687970562,84.66969313695));
#177574=CARTESIAN_POINT('Ctrl Pts',(-20.9886043187099,76.866833178031,85.86421369334));
#177575=CARTESIAN_POINT('Ctrl Pts',(-20.8992293187099,72.824748422185,85.81570983017));
#177576=CARTESIAN_POINT('Ctrl Pts',(-20.8098543187099,68.992669314766,84.52886426336));
#177577=CARTESIAN_POINT('Ctrl Pts',(-20.7204793187099,65.740556859899,82.127913122978));
#177578=CARTESIAN_POINT('Ctrl Pts',(-20.6311043187099,63.38238025148,78.844651804709));
#177579=CARTESIAN_POINT('Ctrl Pts',(-20.5417293187099,62.14580529819,74.996056713737));
#177580=CARTESIAN_POINT('Ctrl Pts',(-20.4523543187099,62.15021484332,70.953683353497));
#177581=CARTESIAN_POINT('Ctrl Pts',(-20.3629793187099,63.39518318695,67.107795220083));
#177582=CARTESIAN_POINT('Ctrl Pts',(-20.2736043187099,65.760517115547,63.829686404028));
#177583=CARTESIAN_POINT('Ctrl Pts',(-20.1842293187099,69.017859990633,61.43583617042));
#177584=CARTESIAN_POINT('Ctrl Pts',(-20.0948543187099,72.852737060995,60.15735325081));
#177585=CARTESIAN_POINT('Ctrl Pts',(-20.0054793187099,76.894919422089,60.11767060096));
#177586=CARTESIAN_POINT('Ctrl Pts',(-19.9161043187099,80.754153740124,61.32060370107));
#177587=CARTESIAN_POINT('Ctrl Pts',(-19.8267293187099,84.057888333329,63.650075845203));
#177588=CARTESIAN_POINT('Ctrl Pts',(-19.7671459853759,85.67733254748,65.804008650901));
#177589=CARTESIAN_POINT('Ctrl Pts',(-19.7373543187099,86.3022786101,66.979361250291));
#177590=CARTESIAN_POINT('Ctrl Pts',(-25.6141722882739,74.5637780077301,
60.49712592814));
#177591=CARTESIAN_POINT('Ctrl Pts',(-25.5843806216069,75.8628281513697,
60.45176209751));
#177592=CARTESIAN_POINT('Ctrl Pts',(-25.5247972882739,78.47495650485,60.76961502662));
#177593=CARTESIAN_POINT('Ctrl Pts',(-25.4354222882739,82.057855268582,62.42607509136));
#177594=CARTESIAN_POINT('Ctrl Pts',(-25.3460472882739,84.95931564794,65.102304338201));
#177595=CARTESIAN_POINT('Ctrl Pts',(-25.2566722882729,86.89928588639,68.539928906151));
#177596=CARTESIAN_POINT('Ctrl Pts',(-25.1672972882729,87.6904578875,72.4070702789702));
#177597=CARTESIAN_POINT('Ctrl Pts',(-25.0779222882729,87.25645403306,76.330382269486));
#177598=CARTESIAN_POINT('Ctrl Pts',(-24.9885472882729,85.63917318558,79.931096006583));
#177599=CARTESIAN_POINT('Ctrl Pts',(-24.8991722882729,82.994753071114,82.861587217225));
#177600=CARTESIAN_POINT('Ctrl Pts',(-24.8097972882729,79.578494259545,84.83893703977));
#177601=CARTESIAN_POINT('Ctrl Pts',(-24.7204222882729,75.7202131758358,
85.67224588461));
#177602=CARTESIAN_POINT('Ctrl Pts',(-24.6310472882729,71.792400439106,85.28106348769));
#177603=CARTESIAN_POINT('Ctrl Pts',(-24.5416722882729,68.174259481666,83.70315583141));
#177604=CARTESIAN_POINT('Ctrl Pts',(-24.4522972882729,65.215097043329,81.090859097905));
#177605=CARTESIAN_POINT('Ctrl Pts',(-24.3629222882729,63.20059999972,77.696372653464));
#177606=CARTESIAN_POINT('Ctrl Pts',(-24.2735472882729,62.32525424947,73.8474109262254));
#177607=CARTESIAN_POINT('Ctrl Pts',(-24.1841722882729,62.67356843231,69.915564821625));
#177608=CARTESIAN_POINT('Ctrl Pts',(-24.0947972882729,64.21191519837,66.280427164319));
#177609=CARTESIAN_POINT('Ctrl Pts',(-24.0054222882729,66.791777698664,63.292945609594));
#177610=CARTESIAN_POINT('Ctrl Pts',(-23.9160472882729,70.164087870074,61.24154104977));
#177611=CARTESIAN_POINT('Ctrl Pts',(-23.8266722882729,74.0032722518052,
60.32426255155));
#177612=CARTESIAN_POINT('Ctrl Pts',(-23.7372972882729,77.938683874199,60.62966707439));
#177613=CARTESIAN_POINT('Ctrl Pts',(-23.6479222882729,81.590385686263,62.12826990236));
#177614=CARTESIAN_POINT('Ctrl Pts',(-23.5585472882729,84.605830876964,64.675391191609));
#177615=CARTESIAN_POINT('Ctrl Pts',(-23.4691722882729,86.69389885636,68.0251238188));
#177616=CARTESIAN_POINT('Ctrl Pts',(-23.3797972882729,87.65300095559,71.854074030477));
#177617=CARTESIAN_POINT('Ctrl Pts',(-23.2904222882729,87.39054243283,75.792582896034));
#177618=CARTESIAN_POINT('Ctrl Pts',(-23.2010472882729,85.93186186169,79.460414346857));
#177619=CARTESIAN_POINT('Ctrl Pts',(-23.1116722882729,83.417784865457,82.503464365711));
#177620=CARTESIAN_POINT('Ctrl Pts',(-23.0222972882739,80.091028367167,84.62794730547));
#177621=CARTESIAN_POINT('Ctrl Pts',(-22.9329222882739,76.272767932331,85.62875888215));
#177622=CARTESIAN_POINT('Ctrl Pts',(-22.8435472882739,72.331630466779,85.4092775894));
#177623=CARTESIAN_POINT('Ctrl Pts',(-22.7541722882739,68.648105812461,83.99069284351));
#177624=CARTESIAN_POINT('Ctrl Pts',(-22.6647972882739,65.577813057976,81.509959290305));
#177625=CARTESIAN_POINT('Ctrl Pts',(-22.5754222882739,63.41716795007,78.206574771673));
#177626=CARTESIAN_POINT('Ctrl Pts',(-22.4860472882739,62.37476598252,74.399458448487));
#177627=CARTESIAN_POINT('Ctrl Pts',(-22.3966722882739,62.55124392917,70.456161338886));
#177628=CARTESIAN_POINT('Ctrl Pts',(-22.3072972882739,63.92956405242,66.757381783671));
#177629=CARTESIAN_POINT('Ctrl Pts',(-22.2179222882739,66.376658980107,63.660211627688));
#177630=CARTESIAN_POINT('Ctrl Pts',(-22.1285472882739,69.656278449357,61.4636614468));
#177631=CARTESIAN_POINT('Ctrl Pts',(-22.0391722882739,73.451797652123,60.37979312378));
#177632=CARTESIAN_POINT('Ctrl Pts',(-21.9497972882739,77.396785192848,60.51324672522));
#177633=CARTESIAN_POINT('Ctrl Pts',(-21.8604222882739,81.110379531183,61.85113821951));
#177634=CARTESIAN_POINT('Ctrl Pts',(-21.7710472882739,84.234058556389,64.264303341857));
#177635=CARTESIAN_POINT('Ctrl Pts',(-21.6816722882739,86.46625244275,67.519767519802));
#177636=CARTESIAN_POINT('Ctrl Pts',(-21.5922972882739,87.59145815176,71.303237973316));
#177637=CARTESIAN_POINT('Ctrl Pts',(-21.5029222882739,87.50104477518,75.2494465311));
#177638=CARTESIAN_POINT('Ctrl Pts',(-21.4135472882739,86.20374110555,78.977413771966));
#177639=CARTESIAN_POINT('Ctrl Pts',(-21.3241722882739,83.824792931074,82.127229979831));
#177640=CARTESIAN_POINT('Ctrl Pts',(-21.2347972882739,80.593871412118,84.39480196293));
#177641=CARTESIAN_POINT('Ctrl Pts',(-21.1454222882739,76.822899903006,85.5612111697));
#177642=CARTESIAN_POINT('Ctrl Pts',(-21.0560472882739,72.875939887522,85.51384877627));
#177643=CARTESIAN_POINT('Ctrl Pts',(-20.9666722882739,69.134043334935,84.25728729746));
#177644=CARTESIAN_POINT('Ctrl Pts',(-20.8772972882739,65.958464741074,81.912839141965));
#177645=CARTESIAN_POINT('Ctrl Pts',(-20.7879222882739,63.65578447949,78.706844729098));
#177646=CARTESIAN_POINT('Ctrl Pts',(-20.6985472882739,62.4483105665,74.948820873245));
#177647=CARTESIAN_POINT('Ctrl Pts',(-20.6091722882739,62.45261633923,71.001579045262));
#177648=CARTESIAN_POINT('Ctrl Pts',(-20.5197972882739,63.668286116,67.246198442551));
#177649=CARTESIAN_POINT('Ctrl Pts',(-20.4304222882739,65.977955260347,64.045235275048));
#177650=CARTESIAN_POINT('Ctrl Pts',(-20.3410472882739,69.158641183889,61.70772091653));
#177651=CARTESIAN_POINT('Ctrl Pts',(-20.2516722882739,72.903269853321,60.45932528185));
#177652=CARTESIAN_POINT('Ctrl Pts',(-20.1622972882739,76.850325177053,60.42057650697));
#177653=CARTESIAN_POINT('Ctrl Pts',(-20.0729222882739,80.618737880831,61.59520028015));
#177654=CARTESIAN_POINT('Ctrl Pts',(-19.9835472882739,83.844723759108,63.869851596353));
#177655=CARTESIAN_POINT('Ctrl Pts',(-19.9239639549399,85.42605664712,65.973094643852));
#177656=CARTESIAN_POINT('Ctrl Pts',(-19.8941722882739,86.0362954892,67.120786984341));
#177657=CARTESIAN_POINT('Ctrl Pts',(-25.7709902578379,74.5742912897478,
60.79818693484));
#177658=CARTESIAN_POINT('Ctrl Pts',(-25.7411985911709,75.8420333362322,
60.75391640706));
#177659=CARTESIAN_POINT('Ctrl Pts',(-25.6816152578379,78.39120740833,61.06410883866));
#177660=CARTESIAN_POINT('Ctrl Pts',(-25.5922402578369,81.887755584948,62.68064695513));
#177661=CARTESIAN_POINT('Ctrl Pts',(-25.5028652578369,84.719288560893,65.292377040265));
#177662=CARTESIAN_POINT('Ctrl Pts',(-25.4134902578369,86.61250404011,68.647152239787));
#177663=CARTESIAN_POINT('Ctrl Pts',(-25.3241152578369,87.38460819383,72.4210925622802));
#177664=CARTESIAN_POINT('Ctrl Pts',(-25.2347402578369,86.9610641626,76.249849747832));
#177665=CARTESIAN_POINT('Ctrl Pts',(-25.1453652578369,85.38276101444,79.7637835434));
#177666=CARTESIAN_POINT('Ctrl Pts',(-25.0559902578369,82.802073437376,82.623647685499));
#177667=CARTESIAN_POINT('Ctrl Pts',(-24.9666152578369,79.468149063245,84.55334187238));
#177668=CARTESIAN_POINT('Ctrl Pts',(-24.8772402578369,75.702855490151,85.36656733984));
#177669=CARTESIAN_POINT('Ctrl Pts',(-24.7878652578369,71.869706029794,84.98481273641));
#177670=CARTESIAN_POINT('Ctrl Pts',(-24.6984902578369,68.338765023158,83.44493385557));
#177671=CARTESIAN_POINT('Ctrl Pts',(-24.6091152578369,65.450920651772,80.895595461536));
#177672=CARTESIAN_POINT('Ctrl Pts',(-24.5197402578369,63.48497452013,77.582918723914));
#177673=CARTESIAN_POINT('Ctrl Pts',(-24.4303652578369,62.63072526867,73.8267199037072));
#177674=CARTESIAN_POINT('Ctrl Pts',(-24.3409902578369,62.97064481461,69.989634282714));
#177675=CARTESIAN_POINT('Ctrl Pts',(-24.2516152578369,64.47191625279,66.442106209615));
#177676=CARTESIAN_POINT('Ctrl Pts',(-24.1622402578369,66.98960210332,63.526625234101));
#177677=CARTESIAN_POINT('Ctrl Pts',(-24.0728652578369,70.280637032969,61.52466108548));
#177678=CARTESIAN_POINT('Ctrl Pts',(-23.9834902578369,74.0272941491374,
60.62948969719));
#177679=CARTESIAN_POINT('Ctrl Pts',(-23.8941152578369,77.867859356231,60.92753373859));
#177680=CARTESIAN_POINT('Ctrl Pts',(-23.8047402578369,81.431552375351,62.39001909784));
#177681=CARTESIAN_POINT('Ctrl Pts',(-23.7153652578369,84.374323041932,64.875752825426));
#177682=CARTESIAN_POINT('Ctrl Pts',(-23.6259902578369,86.41206699382,68.144754346856));
#177683=CARTESIAN_POINT('Ctrl Pts',(-23.5366152578369,87.34805400249,71.881423944257));
#177684=CARTESIAN_POINT('Ctrl Pts',(-23.4472402578369,87.09192092988,75.725011748597));
#177685=CARTESIAN_POINT('Ctrl Pts',(-23.3578652578369,85.6683956707,79.304445669906));
#177686=CARTESIAN_POINT('Ctrl Pts',(-23.2684902578369,83.214909843509,82.274155867272));
#177687=CARTESIAN_POINT('Ctrl Pts',(-23.1791152578369,79.968330708787,84.34743715126));
#177688=CARTESIAN_POINT('Ctrl Pts',(-23.0897402578369,76.242093256469,85.32412840723));
#177689=CARTESIAN_POINT('Ctrl Pts',(-23.0003652578379,72.395940203395,85.10993678068));
#177690=CARTESIAN_POINT('Ctrl Pts',(-22.9109902578379,68.801191296739,83.72554100684));
#177691=CARTESIAN_POINT('Ctrl Pts',(-22.8216152578379,65.804894934405,81.304595020325));
#177692=CARTESIAN_POINT('Ctrl Pts',(-22.7322402578379,63.69632301805,78.080824582763));
#177693=CARTESIAN_POINT('Ctrl Pts',(-22.6428652578379,62.67904373127,74.365462660522));
#177694=CARTESIAN_POINT('Ctrl Pts',(-22.5534902578379,62.8512684251,70.517202012466));
#177695=CARTESIAN_POINT('Ctrl Pts',(-22.4641152578379,64.19636998435,66.907565859634));
#177696=CARTESIAN_POINT('Ctrl Pts',(-22.3747402578379,66.584488061824,63.885039861635));
#177697=CARTESIAN_POINT('Ctrl Pts',(-22.2853652578379,69.785066205781,61.74142821188));
#177698=CARTESIAN_POINT('Ctrl Pts',(-22.1959902578379,73.489110507031,60.68368194036));
#177699=CARTESIAN_POINT('Ctrl Pts',(-22.1066152578379,77.339020845536,60.81391920844));
#177700=CARTESIAN_POINT('Ctrl Pts',(-22.0172402578379,80.963114733938,62.11956649947));
#177701=CARTESIAN_POINT('Ctrl Pts',(-21.9278652578379,84.011510717237,64.474572505729));
#177702=CARTESIAN_POINT('Ctrl Pts',(-21.8384902578379,86.18990703204,67.651577519286));
#177703=CARTESIAN_POINT('Ctrl Pts',(-21.7491152578379,87.28799442708,71.343863455311));
#177704=CARTESIAN_POINT('Ctrl Pts',(-21.6597402578379,87.19976008168,75.194965383434));
#177705=CARTESIAN_POINT('Ctrl Pts',(-21.5703652578379,85.93372241786,78.833085776477));
#177706=CARTESIAN_POINT('Ctrl Pts',(-21.4809902578379,83.612108704975,81.90698901644));
#177707=CARTESIAN_POINT('Ctrl Pts',(-21.3916152578379,80.459054853646,84.11991078892));
#177708=CARTESIAN_POINT('Ctrl Pts',(-21.3022402578379,76.77896662795,85.25820864606));
#177709=CARTESIAN_POINT('Ctrl Pts',(-21.2128652578379,72.92713135283,85.21198772236));
#177710=CARTESIAN_POINT('Ctrl Pts',(-21.1234902578379,69.27541735508,83.98571033155));
#177711=CARTESIAN_POINT('Ctrl Pts',(-21.0341152578379,66.176372622231,81.697765160933));
#177712=CARTESIAN_POINT('Ctrl Pts',(-20.9447402578379,63.9291887075,78.569037653464));
#177713=CARTESIAN_POINT('Ctrl Pts',(-20.8553652578379,62.75081583481,74.90158503273));
#177714=CARTESIAN_POINT('Ctrl Pts',(-20.7659902578379,62.75501783514,71.049474737007));
#177715=CARTESIAN_POINT('Ctrl Pts',(-20.6766152578379,63.94138904505,67.384601665003));
#177716=CARTESIAN_POINT('Ctrl Pts',(-20.5872402578379,66.195393405158,64.260784146057));
#177717=CARTESIAN_POINT('Ctrl Pts',(-20.4978652578379,69.299422377156,61.97960566264));
#177718=CARTESIAN_POINT('Ctrl Pts',(-20.4084902578379,72.953802645656,60.7612973129));
#177719=CARTESIAN_POINT('Ctrl Pts',(-20.3191152578379,76.805730932023,60.72348241298));
#177720=CARTESIAN_POINT('Ctrl Pts',(-20.2297402578379,80.48332202154,61.86979685924));
#177721=CARTESIAN_POINT('Ctrl Pts',(-20.1403652578379,83.631559184886,64.089627347503));
#177722=CARTESIAN_POINT('Ctrl Pts',(-20.0807819245039,85.17478074676,66.1421806368));
#177723=CARTESIAN_POINT('Ctrl Pts',(-20.0509902578369,85.7703123683,67.262212718386));
#177724=CARTESIAN_POINT('Ctrl Pts',(-29.0130799422609,72.422116845822,84.91151378796));
#177725=CARTESIAN_POINT('Ctrl Pts',(-28.9648716383109,70.415792799191,84.47771089461));
#177726=CARTESIAN_POINT('Ctrl Pts',(-28.8684550304109,66.629418901909,82.576109782766));
#177727=CARTESIAN_POINT('Ctrl Pts',(-28.7238301185509,63.03626406749,77.331337332641));
#177728=CARTESIAN_POINT('Ctrl Pts',(-28.5792052067009,62.42850598941,71.003271823318));
#177729=CARTESIAN_POINT('Ctrl Pts',(-28.4345802948509,64.95709911941,65.170572201634));
#177730=CARTESIAN_POINT('Ctrl Pts',(-28.2899553829909,69.991359600301,61.28849282187));
#177731=CARTESIAN_POINT('Ctrl Pts',(-28.1453304711409,76.275228322274,60.32557309628));
#177732=CARTESIAN_POINT('Ctrl Pts',(-28.0007055592909,82.240939818442,62.52205714543));
#177733=CARTESIAN_POINT('Ctrl Pts',(-27.8560806474309,86.40008997649,67.329937790089));
#177734=CARTESIAN_POINT('Ctrl Pts',(-27.7114557355809,87.71500271706,73.5496847895006));
#177735=CARTESIAN_POINT('Ctrl Pts',(-27.5668308237209,85.85761684592,79.629517497618));
#177736=CARTESIAN_POINT('Ctrl Pts',(-27.4222059118709,81.291336383219,84.05256291155));
#177737=CARTESIAN_POINT('Ctrl Pts',(-27.2775810000209,75.1554143062945,
85.71530411088));
#177738=CARTESIAN_POINT('Ctrl Pts',(-27.1329560881609,68.980717517489,84.20289954075));
#177739=CARTESIAN_POINT('Ctrl Pts',(-26.9883311763109,64.30778691511,79.892682886532));
#177740=CARTESIAN_POINT('Ctrl Pts',(-26.8437062644609,62.30248391102,73.860021128897));
#177741=CARTESIAN_POINT('Ctrl Pts',(-26.6990813526009,63.46511668212,67.610018484104));
#177742=CARTESIAN_POINT('Ctrl Pts',(-26.5544564407489,67.505617003827,62.70200410244));
#177743=CARTESIAN_POINT('Ctrl Pts',(-26.4098315288959,73.41591011336,60.36049104895));
#177744=CARTESIAN_POINT('Ctrl Pts',(-26.2652066170419,79.721421861612,61.1696694061));
#177745=CARTESIAN_POINT('Ctrl Pts',(-26.1205817051879,84.848973989789,64.927655195095));
#177746=CARTESIAN_POINT('Ctrl Pts',(-25.9759567933349,87.5192803998,70.696858927558));
#177747=CARTESIAN_POINT('Ctrl Pts',(-25.8313318814809,87.06611950964,77.037907200944));
#177748=CARTESIAN_POINT('Ctrl Pts',(-25.6867069696279,83.602551603711,82.368755669438));
#177749=CARTESIAN_POINT('Ctrl Pts',(-25.5420820577749,77.992711046048,85.35939726776));
#177750=CARTESIAN_POINT('Ctrl Pts',(-25.3974571459209,71.636211512424,85.26368932913));
#177751=CARTESIAN_POINT('Ctrl Pts',(-25.2528322340679,66.118951578813,82.105509685936));
#177752=CARTESIAN_POINT('Ctrl Pts',(-25.1082073222149,62.81744936158,76.672802844726));
#177753=CARTESIAN_POINT('Ctrl Pts',(-24.9635824103609,62.55539457204,70.320980571748));
#177754=CARTESIAN_POINT('Ctrl Pts',(-24.8189574985079,65.398207204844,64.634805721403));
#177755=CARTESIAN_POINT('Ctrl Pts',(-24.6743325866549,70.636480087695,61.03282290959));
#177756=CARTESIAN_POINT('Ctrl Pts',(-24.5297076748019,76.963850143509,60.4141243606));
#177757=CARTESIAN_POINT('Ctrl Pts',(-24.4332910668999,80.854379446751,62.092366244));
#177758=CARTESIAN_POINT('Ctrl Pts',(-24.3850827629489,82.476320069947,63.350471861665));
#177759=CARTESIAN_POINT('Ctrl Pts',(-29.1698979118309,72.358453566317,85.2059543519));
#177760=CARTESIAN_POINT('Ctrl Pts',(-29.1216896078809,70.302581436659,84.76143828298));
#177761=CARTESIAN_POINT('Ctrl Pts',(-29.0252729999709,66.42269943008,82.812875320713));
#177762=CARTESIAN_POINT('Ctrl Pts',(-28.8806480881209,62.74080821513,77.438578220143));
#177763=CARTESIAN_POINT('Ctrl Pts',(-28.7360231762609,62.11804097252,70.954235106618));
#177764=CARTESIAN_POINT('Ctrl Pts',(-28.5913982644109,64.70908011794,64.977491413082));
#177765=CARTESIAN_POINT('Ctrl Pts',(-28.4467733525609,69.867666455716,60.99954038599));
#177766=CARTESIAN_POINT('Ctrl Pts',(-28.3021484407009,76.306721300137,60.01284044075));
#177767=CARTESIAN_POINT('Ctrl Pts',(-28.1575235288509,82.419761723069,62.26356875528));
#177768=CARTESIAN_POINT('Ctrl Pts',(-28.0128986170009,86.68162605518,67.190184591183));
#177769=CARTESIAN_POINT('Ctrl Pts',(-27.8682737051409,88.02901181812,73.5635341660382));
#177770=CARTESIAN_POINT('Ctrl Pts',(-27.7236487932909,86.12575603404,79.793514132931));
#177771=CARTESIAN_POINT('Ctrl Pts',(-27.5790238814309,81.446706926677,84.32579086559));
#177772=CARTESIAN_POINT('Ctrl Pts',(-27.4343989695809,75.1592524105996,
86.02959504233));
#177773=CARTESIAN_POINT('Ctrl Pts',(-27.2897740577309,68.832065604203,84.47984020103));
#177774=CARTESIAN_POINT('Ctrl Pts',(-27.1451491458709,64.04373253039,80.063178641754));
#177775=CARTESIAN_POINT('Ctrl Pts',(-27.0005242340209,61.98890665889,73.8815345568893));
#177776=CARTESIAN_POINT('Ctrl Pts',(-26.8558993221709,63.18025175349,67.477182144676));
#177777=CARTESIAN_POINT('Ctrl Pts',(-26.7112744103109,67.320536078556,62.44795967377));
#177778=CARTESIAN_POINT('Ctrl Pts',(-26.5666494984599,73.376789505017,60.04862072552));
#177779=CARTESIAN_POINT('Ctrl Pts',(-26.4220245866059,79.838021870863,60.87778251281));
#177780=CARTESIAN_POINT('Ctrl Pts',(-26.2773996747519,85.092203782,64.728575339723));
#177781=CARTESIAN_POINT('Ctrl Pts',(-26.1327747628989,87.82845595185,70.640255052583));
#177782=CARTESIAN_POINT('Ctrl Pts',(-25.9881498510449,87.36410382194,77.137901551893));
#177783=CARTESIAN_POINT('Ctrl Pts',(-25.8435249391919,83.814999808094,82.600400400082));
#177784=CARTESIAN_POINT('Ctrl Pts',(-25.6989000273379,78.066618895403,85.66489874077));
#177785=CARTESIAN_POINT('Ctrl Pts',(-25.5542751154849,71.553139552267,85.56682720345));
#177786=CARTESIAN_POINT('Ctrl Pts',(-25.4096502036319,65.899625630305,82.330653306324));
#177787=CARTESIAN_POINT('Ctrl Pts',(-25.2650252917779,62.51658967167,76.763780595904));
#177788=CARTESIAN_POINT('Ctrl Pts',(-25.1204003799249,62.24806318954,70.25509402282));
#177789=CARTESIAN_POINT('Ctrl Pts',(-24.9757754680719,65.161081787626,64.428493669391));
#177790=CARTESIAN_POINT('Ctrl Pts',(-24.8311505562189,70.528718807919,60.73755646174));
#177791=CARTESIAN_POINT('Ctrl Pts',(-24.6865256443659,77.01234929305,60.10357856287));
#177792=CARTESIAN_POINT('Ctrl Pts',(-24.5901090364639,80.998958922529,61.82326622784));
#177793=CARTESIAN_POINT('Ctrl Pts',(-24.5419007325129,82.66095491405,63.112441961868));
#177794=CARTESIAN_POINT('Ctrl Pts',(-29.3267158813909,72.294790286804,85.50039491585));
#177795=CARTESIAN_POINT('Ctrl Pts',(-29.2785075774409,70.189370074118,85.04516567134));
#177796=CARTESIAN_POINT('Ctrl Pts',(-29.1820909695409,66.215979958243,83.04964085865));
#177797=CARTESIAN_POINT('Ctrl Pts',(-29.0374660576809,62.44535236276,77.545819107633));
#177798=CARTESIAN_POINT('Ctrl Pts',(-28.8928411458309,61.80757595563,70.905198389902));
#177799=CARTESIAN_POINT('Ctrl Pts',(-28.7482162339709,64.46106111648,64.784410624515));
#177800=CARTESIAN_POINT('Ctrl Pts',(-28.6035913221209,69.743973311151,60.7105879501));
#177801=CARTESIAN_POINT('Ctrl Pts',(-28.4589664102709,76.338214278025,59.70010778522));
#177802=CARTESIAN_POINT('Ctrl Pts',(-28.3143414984109,82.59858362772,62.00508036515));
#177803=CARTESIAN_POINT('Ctrl Pts',(-28.1697165865609,86.96316213389,67.050431392305));
#177804=CARTESIAN_POINT('Ctrl Pts',(-28.0250916747109,88.34302091918,73.5773835426106));
#177805=CARTESIAN_POINT('Ctrl Pts',(-27.8804667628509,86.39389522214,79.957510768277));
#177806=CARTESIAN_POINT('Ctrl Pts',(-27.7358418510009,81.6020774701,84.59901881965));
#177807=CARTESIAN_POINT('Ctrl Pts',(-27.5912169391409,75.163090514862,86.34388597378));
#177808=CARTESIAN_POINT('Ctrl Pts',(-27.4465920272909,68.683413690878,84.75678086128));
#177809=CARTESIAN_POINT('Ctrl Pts',(-27.3019671154409,63.77967814565,80.233674396936));
#177810=CARTESIAN_POINT('Ctrl Pts',(-27.1573422035809,61.67532940676,73.903047984833));
#177811=CARTESIAN_POINT('Ctrl Pts',(-27.0127172917309,62.89538682488,67.344345805202));
#177812=CARTESIAN_POINT('Ctrl Pts',(-26.8680923798809,67.135455153326,62.19391524507));
#177813=CARTESIAN_POINT('Ctrl Pts',(-26.7234674680209,73.337668896726,59.73675040207));
#177814=CARTESIAN_POINT('Ctrl Pts',(-26.5788425561709,79.954621880163,60.58589561953));
#177815=CARTESIAN_POINT('Ctrl Pts',(-26.4342176443159,85.33543357425,64.52949548439));
#177816=CARTESIAN_POINT('Ctrl Pts',(-26.2895927324629,88.1376315039,70.583651177657));
#177817=CARTESIAN_POINT('Ctrl Pts',(-26.1449678206089,87.66208813423,77.237895902889));
#177818=CARTESIAN_POINT('Ctrl Pts',(-26.0003429087559,84.027448012443,82.832045130756));
#177819=CARTESIAN_POINT('Ctrl Pts',(-25.8557179969019,78.140526744715,85.9704002138));
#177820=CARTESIAN_POINT('Ctrl Pts',(-25.7110930850489,71.470067592072,85.86996507777));
#177821=CARTESIAN_POINT('Ctrl Pts',(-25.5664681731959,65.680299681772,82.555796926686));
#177822=CARTESIAN_POINT('Ctrl Pts',(-25.4218432613419,62.21572998176,76.854758347052));
#177823=CARTESIAN_POINT('Ctrl Pts',(-25.2772183494889,61.94073180705,70.189207473868));
#177824=CARTESIAN_POINT('Ctrl Pts',(-25.1325934376359,64.92395637042,64.222181617367));
#177825=CARTESIAN_POINT('Ctrl Pts',(-24.9879685257829,70.420957528155,60.44229001389));
#177826=CARTESIAN_POINT('Ctrl Pts',(-24.8433436139299,77.060848442593,59.79303276515));
#177827=CARTESIAN_POINT('Ctrl Pts',(-24.7469270060279,81.143538398306,61.55416621167));
#177828=CARTESIAN_POINT('Ctrl Pts',(-24.6987187020769,82.845589758148,62.87441206207));
#177829=CARTESIAN_POINT('Ctrl Pts',(-29.4835338509509,72.2311270073,85.79483547979));
#177830=CARTESIAN_POINT('Ctrl Pts',(-29.4353255470009,70.076158711586,85.32889305971));
#177831=CARTESIAN_POINT('Ctrl Pts',(-29.3389089391009,66.009260486414,83.2864063966));
#177832=CARTESIAN_POINT('Ctrl Pts',(-29.1942840272509,62.14989651041,77.653059995135));
#177833=CARTESIAN_POINT('Ctrl Pts',(-29.0496591153909,61.49711093875,70.856161673202));
#177834=CARTESIAN_POINT('Ctrl Pts',(-28.9050342035409,64.21304211501,64.591329835963));
#177835=CARTESIAN_POINT('Ctrl Pts',(-28.7604092916909,69.620280166566,60.42163551422));
#177836=CARTESIAN_POINT('Ctrl Pts',(-28.6157843798309,76.369707255888,59.38737512969));
#177837=CARTESIAN_POINT('Ctrl Pts',(-28.4711594679809,82.777405532348,61.74659197501));
#177838=CARTESIAN_POINT('Ctrl Pts',(-28.3265345561209,87.24469821258,66.9106781934));
#177839=CARTESIAN_POINT('Ctrl Pts',(-28.1819096442709,88.65703002025,73.5912329191485));
#177840=CARTESIAN_POINT('Ctrl Pts',(-28.0372847324209,86.66203441026,80.12150740359));
#177841=CARTESIAN_POINT('Ctrl Pts',(-27.8926598205609,81.757448013558,84.87224677369));
#177842=CARTESIAN_POINT('Ctrl Pts',(-27.7480349087109,75.1669286191668,
86.65817690523));
#177843=CARTESIAN_POINT('Ctrl Pts',(-27.6034099968509,68.534761777592,85.03372152155));
#177844=CARTESIAN_POINT('Ctrl Pts',(-27.4587850850009,63.51562376093,80.404170152158));
#177845=CARTESIAN_POINT('Ctrl Pts',(-27.3141601731509,61.36175215463,73.924561412825));
#177846=CARTESIAN_POINT('Ctrl Pts',(-27.1695352612909,62.61052189625,67.211509465773));
#177847=CARTESIAN_POINT('Ctrl Pts',(-27.0249103494409,66.950374228055,61.9398708164));
#177848=CARTESIAN_POINT('Ctrl Pts',(-26.8802854375909,73.298548288383,59.42488007864));
#177849=CARTESIAN_POINT('Ctrl Pts',(-26.7356605257309,80.071221889414,60.29400872623));
#177850=CARTESIAN_POINT('Ctrl Pts',(-26.5910356138809,85.57866336647,64.330415629018));
#177851=CARTESIAN_POINT('Ctrl Pts',(-26.4464107020269,88.44680705594,70.527047302681));
#177852=CARTESIAN_POINT('Ctrl Pts',(-26.3017857901729,87.96007244653,77.337890253839));
#177853=CARTESIAN_POINT('Ctrl Pts',(-26.1571608783199,84.239896216826,83.0636898614));
#177854=CARTESIAN_POINT('Ctrl Pts',(-26.0125359664659,78.21443459407,86.27590168681));
#177855=CARTESIAN_POINT('Ctrl Pts',(-25.8679110546129,71.386995631916,86.17310295209));
#177856=CARTESIAN_POINT('Ctrl Pts',(-25.7232861427599,65.460973733264,82.780940547073));
#177857=CARTESIAN_POINT('Ctrl Pts',(-25.5786612309059,61.91487029185,76.94573609823));
#177858=CARTESIAN_POINT('Ctrl Pts',(-25.4340363190529,61.63340042455,70.12332092494));
#177859=CARTESIAN_POINT('Ctrl Pts',(-25.2894114071999,64.6868309532,64.015869565355));
#177860=CARTESIAN_POINT('Ctrl Pts',(-25.1447864953469,70.313196248379,60.14702356604));
#177861=CARTESIAN_POINT('Ctrl Pts',(-25.0001615834929,77.109347592134,59.48248696742));
#177862=CARTESIAN_POINT('Ctrl Pts',(-24.9037449755909,81.288117874084,61.28506619551));
#177863=CARTESIAN_POINT('Ctrl Pts',(-24.8555366716399,83.03022460225,62.63638216227));
#177864=CARTESIAN_POINT('Origin',(-18.5675364832709,75.,72.98888938658));
#177865=CARTESIAN_POINT('Origin',(-16.5675364832709,75.,72.98888938658));
#221638=UNCERTAINTY_MEASURE_WITH_UNIT(LENGTH_MEASURE(0.01),#221663,
'DISTANCE_ACCURACY_VALUE',
'Maximum model space distance between geometric entities at asserted c
onnectivities');
#221647=UNCERTAINTY_MEASURE_WITH_UNIT(LENGTH_MEASURE(0.01),#221663,
'DISTANCE_ACCURACY_VALUE',
'Maximum model space distance between geometric entities at asserted c
onnectivities');
#221653=(
GEOMETRIC_REPRESENTATION_CONTEXT(3)
GLOBAL_UNCERTAINTY_ASSIGNED_CONTEXT((#221638))
GLOBAL_UNIT_ASSIGNED_CONTEXT((#221663,#221665,#221666))
REPRESENTATION_CONTEXT('','3D')
);
#221662=(
GEOMETRIC_REPRESENTATION_CONTEXT(3)
GLOBAL_UNCERTAINTY_ASSIGNED_CONTEXT((#221647))
GLOBAL_UNIT_ASSIGNED_CONTEXT((#221663,#221665,#221666))
REPRESENTATION_CONTEXT('','3D')
);
#221663=(
LENGTH_UNIT()
NAMED_UNIT(*)
SI_UNIT(.MILLI.,.METRE.)
);
#221665=(
NAMED_UNIT(*)
PLANE_ANGLE_UNIT()
SI_UNIT($,.RADIAN.)
);
#221666=(
NAMED_UNIT(*)
SI_UNIT($,.STERADIAN.)
SOLID_ANGLE_UNIT()
);
#221672=SHAPE_DEFINITION_REPRESENTATION(#221686,#221713);
#221686=PRODUCT_DEFINITION_SHAPE('',$,#221728);
#221713=SHAPE_REPRESENTATION('',(#80667),#221653);
#221722=PRODUCT_DEFINITION_CONTEXT('part definition',#221766,'design');
#221728=PRODUCT_DEFINITION('2026-10-05-23-02-34-900','Coupling Nut',#221742,
#221722);
#221742=PRODUCT_DEFINITION_FORMATION('',$,#221773);
#221766=APPLICATION_CONTEXT(
'Core Data for Automotive Mechanical Design Process');
#221767=PRODUCT_CONTEXT('part definition',#221766,'mechanical');
#221773=PRODUCT('2026-10-05-23-02-34-900','Coupling Nut',$,(#221767));
#221783=PRESENTATION_STYLE_ASSIGNMENT((#221785));
#221785=SURFACE_STYLE_USAGE(.BOTH.,#221787);
#221787=SURFACE_SIDE_STYLE('',(#221789));
#221789=SURFACE_STYLE_FILL_AREA(#221791);
#221791=FILL_AREA_STYLE('Opaque(202,209,238)',(#221793));
#221793=FILL_AREA_STYLE_COLOUR('Opaque(202,209,238)',#221795);
#221795=COLOUR_RGB('Opaque(202,209,238)', 0.09019608, 0.27058824, 0.51372549);
ENDSEC;
END-ISO-10303-21;
